ISO-10303-21;
HEADER;
FILE_DESCRIPTION (('STEP AP214'),
    '1' );
FILE_NAME ('5. Joint.step',
    '2026-10-09T14:04:53',
    ( '' ),
    ( '' ),
    'SwSTEP 2.0',
    'SolidWorks 2021',
    '' );
FILE_SCHEMA (( 'AUTOMOTIVE_DESIGN' ));
ENDSEC;

DATA;
#24=ORIENTED_EDGE ( 'NONE', *, *, #26895, .F. ) ;
#49=( GEOMETRIC_REPRESENTATION_CONTEXT ( 3 ) GLOBAL_UNCERTAINTY_ASSIGNED_CONTEXT ( ( #34894 ) ) GLOBAL_UNIT_ASSIGNED_CONTEXT ( ( #91410, #78925, #30403 ) ) REPRESENTATION_CONTEXT ( 'NONE', 'WORKASPACE' ) );
#53=CARTESIAN_POINT ( 'NONE',  ( -11.45206486516558009, 14.70585775886807056, 9.862607668232977076 ) ) ;
#73=CARTESIAN_POINT ( 'NONE',  ( -10.88549210619159346, 9.040369729539051491, -10.02153587380511190 ) ) ;
#132=CARTESIAN_POINT ( 'NONE',  ( 16.14595037822613932, 12.99999999999999467, 8.749999999999944933 ) ) ;
#205=ADVANCED_FACE ( 'NONE', ( #45454 ), #41693, .T. ) ;
#409=( NAMED_UNIT ( * ) PLANE_ANGLE_UNIT ( ) SI_UNIT ( $, .RADIAN. ) );
#467=( NAMED_UNIT ( * ) SI_UNIT ( $, .STERADIAN. ) SOLID_ANGLE_UNIT ( ) );
#469=CARTESIAN_POINT ( 'NONE',  ( 13.30905003209610982, 22.18330274843690475, 4.016012902930523154 ) ) ;
#513=CARTESIAN_POINT ( 'NONE',  ( -15.57949638806330839, 22.99924373907892061, -0.5870217286331953499 ) ) ;
#526=STYLED_ITEM ( 'NONE', ( #63722 ), #78240 ) ;
#529=CARTESIAN_POINT ( 'NONE',  ( 14.13631897826462236, 21.04363150066026478, -5.954641296519788796 ) ) ;
#620=( NAMED_UNIT ( * ) SI_UNIT ( $, .STERADIAN. ) SOLID_ANGLE_UNIT ( ) );
#638=COLOUR_RGB ( '', 0.40784314, 0.44705882, 0.49803922) ;
#647=CARTESIAN_POINT ( 'NONE',  ( -14.58934900096693354, 5.487773041254725648, 6.668063844683933539 ) ) ;
#649=CARTESIAN_POINT ( 'NONE',  ( -19.50000000000000000, 12.99999999999999289, 0.000000000000000000 ) ) ;
#672=STYLED_ITEM ( 'NONE', ( #57049 ), #18131 ) ;
#676=CIRCLE ( 'NONE', #59253, 0.5000000000000004441 ) ;
#678=CARTESIAN_POINT ( 'NONE',  ( 16.05785784214672773, 4.775831776474238843, 3.710403933782425057 ) ) ;
#701=SURFACE_STYLE_FILL_AREA ( #18011 ) ;
#745=SURFACE_STYLE_FILL_AREA ( #27776 ) ;
#793=CIRCLE ( 'NONE', #40490, 2.000000000000000000 ) ;
#811=FACE_BOUND ( 'NONE', #67326, .T. ) ;
#825=DIRECTION ( 'NONE',  ( -1.000000000000000000, 0.000000000000000000, 0.000000000000000000 ) ) ;
#829=EDGE_LOOP ( 'NONE', ( #39657, #74387, #10029, #30615 ) ) ;
#884=VECTOR ( 'NONE', #9584, 1000.000000000000000 ) ;
#891=EDGE_LOOP ( 'NONE', ( #92580, #59792, #70176, #70030 ) ) ;
#939=DIRECTION ( 'NONE',  ( 0.000000000000000000, 0.000000000000000000, 1.000000000000000000 ) ) ;
#945=CARTESIAN_POINT ( 'NONE',  ( 15.19395690307707802, 3.423339800906996633, -3.910915912796353311 ) ) ;
#995=ORIENTED_EDGE ( 'NONE', *, *, #54153, .T. ) ;
#999=CARTESIAN_POINT ( 'NONE',  ( 13.75102621199263098, 22.92510964053082390, 1.258367125183780466 ) ) ;
#1033=EDGE_LOOP ( 'NONE', ( #58622, #71478, #91327, #14523 ) ) ;
#1052=CARTESIAN_POINT ( 'NONE',  ( -13.79622750027070488, 22.99942056476660213, -0.5183817344751221468 ) ) ;
#1077=APPLICATION_CONTEXT ( 'automotive_design' ) ;
#1161=CARTESIAN_POINT ( 'NONE',  ( 0.000000000000000000, 34.00000000000000711, 0.000000000000000000 ) ) ;
#1216=ORIENTED_EDGE ( 'NONE', *, *, #7066, .T. ) ;
#1304=ORIENTED_EDGE ( 'NONE', *, *, #24647, .T. ) ;
#1339=CARTESIAN_POINT ( 'NONE',  ( -14.84237598262832769, 1.406801708887335245, -2.172554589303035577 ) ) ;
#1367=CARTESIAN_POINT ( 'NONE',  ( -14.29190075645216318, 6.456385560668112866, -7.561819230143454362 ) ) ;
#1395=AXIS2_PLACEMENT_3D ( 'NONE', #72416, #22310, #39003 ) ;
#1445=CARTESIAN_POINT ( 'NONE',  ( 14.98982670280988039, 2.030473042282394225, 0.4147640935944429397 ) ) ;
#1451=DIRECTION ( 'NONE',  ( 0.000000000000000000, 0.000000000000000000, -1.000000000000000000 ) ) ;
#1486=CARTESIAN_POINT ( 'NONE',  ( 6.705159343100833169, 9.539515232900985353, 2.022944797798714944 ) ) ;
#1501=CARTESIAN_POINT ( 'NONE',  ( 0.000000000000000000, 34.00000000000000000, 0.000000000000000000 ) ) ;
#1519=AXIS2_PLACEMENT_3D ( 'NONE', #92753, #35621, #18911 ) ;
#1532=VERTEX_POINT ( 'NONE', #48626 ) ;
#1554=FACE_OUTER_BOUND ( 'NONE', #56896, .T. ) ;
#1556=CARTESIAN_POINT ( 'NONE',  ( 13.58541053222488060, 24.75820122212995500, 0.5865258224344345184 ) ) ;
#1559=AXIS2_PLACEMENT_3D ( 'NONE', #13097, #27758, #28820 ) ;
#1599=CARTESIAN_POINT ( 'NONE',  ( -15.26425464274176491, 22.59372108562831016, -2.835904228628532309 ) ) ;
#1623=DIRECTION ( 'NONE',  ( 0.000000000000000000, 1.000000000000000000, 0.000000000000000000 ) ) ;
#1656=CARTESIAN_POINT ( 'NONE',  ( 6.322210203194782885, 15.64510924972225681, 3.011395388464980005 ) ) ;
#1663=FILL_AREA_STYLE_COLOUR ( '', #80458 ) ;
#1721=ORIENTED_EDGE ( 'NONE', *, *, #73541, .F. ) ;
#1741=CARTESIAN_POINT ( 'NONE',  ( -14.29190075645648683, 6.456385560661901835, 7.561819230138081771 ) ) ;
#1742=CARTESIAN_POINT ( 'NONE',  ( 14.29190075645216673, 6.456385560668102208, 7.561819230143447257 ) ) ;
#1798=DIRECTION ( 'NONE',  ( -1.000000000000000000, -0.000000000000000000, -0.000000000000000000 ) ) ;
#1812=CARTESIAN_POINT ( 'NONE',  ( 18.00000000000000355, 12.99999999999999289, 0.000000000000000000 ) ) ;
#1886=( LENGTH_UNIT ( ) NAMED_UNIT ( * ) SI_UNIT ( .MILLI., .METRE. ) );
#1902=CARTESIAN_POINT ( 'NONE',  ( -1.489880555935389612E-15, 34.19642918197134662, -12.16579798332631412 ) ) ;
#1965=( NAMED_UNIT ( * ) SI_UNIT ( $, .STERADIAN. ) SOLID_ANGLE_UNIT ( ) );
#1981=CARTESIAN_POINT ( 'NONE',  ( 0.000000000000000000, -6.938893903907228378E-15, 0.000000000000000000 ) ) ;
#1988=CARTESIAN_POINT ( 'NONE',  ( 14.65167870846204323, 2.576877453026212628, 3.244758155286363799 ) ) ;
#1989=ORIENTED_EDGE ( 'NONE', *, *, #13590, .F. ) ;
#2016=VECTOR ( 'NONE', #91954, 1000.000000000000000 ) ;
#2040=ORIENTED_EDGE ( 'NONE', *, *, #37938, .T. ) ;
#2092=CARTESIAN_POINT ( 'NONE',  ( 13.55263786699659256, 24.70009625497336003, 1.189294995871621685 ) ) ;
#2131=CARTESIAN_POINT ( 'NONE',  ( -13.30705700582391593, 22.17985797309225759, -4.023645276857861219 ) ) ;
#2144=COLOUR_RGB ( '', 0.66274510, 0.83137255, 0.94901961) ;
#2147=FACE_OUTER_BOUND ( 'NONE', #44985, .T. ) ;
#2192=FILL_AREA_STYLE ('',( #1663 ) ) ;
#2209=FILL_AREA_STYLE ('',( #35158 ) ) ;
#2229=CIRCLE ( 'NONE', #60849, 1.000000000000000000 ) ;
#2286=DIRECTION ( 'NONE',  ( -1.000000000000000000, 0.000000000000000000, 0.000000000000000000 ) ) ;
#2292=CIRCLE ( 'NONE', #41891, 1.000000000000000888 ) ;
#2396=EDGE_LOOP ( 'NONE', ( #64019, #88196 ) ) ;
#2423=CARTESIAN_POINT ( 'NONE',  ( -15.47565679866127653, 2.746345986930186278, -1.655435732240887026 ) ) ;
#2441=CARTESIAN_POINT ( 'NONE',  ( -1.722054852581828306E-15, 24.73290587908618932, -14.06164498842270483 ) ) ;
#2489=MECHANICAL_DESIGN_GEOMETRIC_PRESENTATION_REPRESENTATION('',(#672),#12794);
#2530=SURFACE_SIDE_STYLE ('',( #77502 ) ) ;
#2541=MECHANICAL_DESIGN_GEOMETRIC_PRESENTATION_REPRESENTATION('',(#4249),#73113);
#2630=CARTESIAN_POINT ( 'NONE',  ( 14.29190075645217206, 6.456385560668103984, 7.561819230143444592 ) ) ;
#2632=CARTESIAN_POINT ( 'NONE',  ( 10.65954291562494660, 18.20485743982220939, 9.432410022334257960 ) ) ;
#2672=CARTESIAN_POINT ( 'NONE',  ( -11.11678473387292598, 19.57455013713238046, 8.700105968029125947 ) ) ;
#2679=CARTESIAN_POINT ( 'NONE',  ( -18.00000000000000355, 12.99999999999999467, 7.500000000000000000 ) ) ;
#2702=CARTESIAN_POINT ( 'NONE',  ( -16.10302234481894601, 5.501632350617743583, 4.770674012961006127 ) ) ;
#2757=ORIENTED_EDGE ( 'NONE', *, *, #22073, .F. ) ;
#2889=DIRECTION ( 'NONE',  ( 0.000000000000000000, 0.000000000000000000, 1.000000000000000000 ) ) ;
#2942=EDGE_CURVE ( 'NONE', #74862, #76857, #36953, .T. ) ;
#2952=CARTESIAN_POINT ( 'NONE',  ( -14.97625732068919469, 1.268789641109800748, -0.8714310519133426913 ) ) ;
#2956=( NAMED_UNIT ( * ) SI_UNIT ( $, .STERADIAN. ) SOLID_ANGLE_UNIT ( ) );
#2970=DIRECTION ( 'NONE',  ( -0.000000000000000000, -1.000000000000000000, -0.000000000000000000 ) ) ;
#3025=CARTESIAN_POINT ( 'NONE',  ( -14.44581512912408705, 5.963299184987270074, 7.135127315202455911 ) ) ;
#3028=DIRECTION ( 'NONE',  ( 0.000000000000000000, 0.000000000000000000, -1.000000000000000000 ) ) ;
#3034=TOROIDAL_SURFACE ( 'NONE', #73617, 9.500000000000000000, 2.000000000000000000 ) ;
#3042=FILL_AREA_STYLE_COLOUR ( '', #61310 ) ;
#3073=EDGE_CURVE ( 'NONE', #12309, #49969, #66876, .T. ) ;
#3101=EDGE_CURVE ( 'NONE', #43916, #92807, #26758, .T. ) ;
#3129=EDGE_LOOP ( 'NONE', ( #93239, #96111, #27042, #10278 ) ) ;
#3150=ORIENTED_EDGE ( 'NONE', *, *, #81419, .T. ) ;
#3155=ORIENTED_EDGE ( 'NONE', *, *, #80792, .F. ) ;
#3177=CARTESIAN_POINT ( 'NONE',  ( 12.35931481849550195, 17.95192587946648288, 8.704851652794047823 ) ) ;
#3195=CIRCLE ( 'NONE', #103061, 2.000000000000000444 ) ;
#3224=CARTESIAN_POINT ( 'NONE',  ( -11.22818708771012375, 17.69611070818088905, 8.853064228155091087 ) ) ;
#3279=CARTESIAN_POINT ( 'NONE',  ( 6.984140731825568160, 16.97242079111239832, 0.5385323539060852260 ) ) ;
#3356=CARTESIAN_POINT ( 'NONE',  ( -14.11595029532502465, 2.410436752314748521, -5.024000119269296682 ) ) ;
#3368=ORIENTED_EDGE ( 'NONE', *, *, #4688, .F. ) ;
#3396=( GEOMETRIC_REPRESENTATION_CONTEXT ( 3 ) GLOBAL_UNCERTAINTY_ASSIGNED_CONTEXT ( ( #26806 ) ) GLOBAL_UNIT_ASSIGNED_CONTEXT ( ( #28727, #13547, #60546 ) ) REPRESENTATION_CONTEXT ( 'NONE', 'WORKASPACE' ) );
#3412=CARTESIAN_POINT ( 'NONE',  ( -16.10302234481879680, 5.501632350609884980, -4.770674012950244069 ) ) ;
#3413=ORIENTED_EDGE ( 'NONE', *, *, #53423, .F. ) ;
#3447=CARTESIAN_POINT ( 'NONE',  ( -12.39315421835605768, 18.01515667718084757, -8.658431383304368012 ) ) ;
#3451=EDGE_CURVE ( 'NONE', #51169, #24752, #92456, .T. ) ;
#3453=SURFACE_STYLE_FILL_AREA ( #77875 ) ;
#3455=CARTESIAN_POINT ( 'NONE',  ( 14.87468076903141245, 23.07153947554854767, -1.073492826214703433 ) ) ;
#3469=ORIENTED_EDGE ( 'NONE', *, *, #85599, .F. ) ;
#3503=DIRECTION ( 'NONE',  ( 0.000000000000000000, 0.000000000000000000, 1.000000000000000000 ) ) ;
#3507=FILL_AREA_STYLE ('',( #53121 ) ) ;
#3616=EDGE_CURVE ( 'NONE', #63378, #63934, #71810, .T. ) ;
#3642=( LENGTH_UNIT ( ) NAMED_UNIT ( * ) SI_UNIT ( .MILLI., .METRE. ) );
#3690=ORIENTED_EDGE ( 'NONE', *, *, #21568, .T. ) ;
#3721=CARTESIAN_POINT ( 'NONE',  ( 10.63959103012515506, 13.00689338755777591, 10.01966540347888390 ) ) ;
#3755=B_SPLINE_CURVE_WITH_KNOTS ( 'NONE', 3,
 ( #61787, #31019, #30474, #38053, #78999, #6158, #55755, #39091, #36988, #13721, #55239, #78468, #4589, #63898, #37524, #88687, #70911, #71971, #70388, #88163, #103286, #29434, #29947, #14247, #62831, #47153, #69856, #62310, #95201, #79526, #95722, #80047, #45063, #96787, #77946, #21861, #22918, #28913, #94682, #21334, #13186, #54703, #87636, #46630, #5640, #72495, #56287, #32602, #16932, #64939, #48732, #25035, #32064, #56832, #57890, #89756, #14783, #41722, #15852, #97295, #15321, #33128, #73540, #23451, #81623, #8818, #99402, #25586, #106445, #33650, #23990, #49267, #48208, #97832, #7748, #90277, #74607, #58445, #65474, #89224, #80576, #57356, #64426, #40658, #81111, #16378 ),
 .UNSPECIFIED., .F., .F.,
 ( 4, 2, 2, 2, 2, 2, 2, 2, 2, 2, 2, 2, 2, 2, 2, 2, 2, 2, 2, 2, 2, 2, 2, 2, 2, 2, 2, 2, 2, 2, 2, 2, 2, 2, 2, 2, 2, 2, 2, 2, 2, 2, 4 ),
 ( 0.02397150411713972612, 0.02592718538678167456, 0.02788286665642362300, 0.02983854792606556797, 0.03081638856088654219, 0.03179422919570751294, 0.03374991046534946137, 0.03570559173499140287, 0.03766127300463335131, 0.03863911363945431859, 0.03961695427427529281, 0.04059479490909626009, 0.04157263554391722737, 0.04352831681355916194, 0.04450615744838013615, 0.04548399808320111037, 0.04743967935284304493, 0.04939536062248497950, 0.05135104189212691406, 0.05232888252694787440, 0.05330672316176883474, 0.05428456379658980202, 0.05526240443141076236, 0.05721808570105269692, 0.05819592633587366420, 0.05917376697069462455, 0.06112944824033656605, 0.06308512950997849367, 0.06504081077962042823, 0.06699649204926236279, 0.06895217331890429735, 0.06993001395372527851, 0.07090785458854624579, 0.07286353585818819423, 0.07481921712783012879, 0.07677489839747206335, 0.07873057966711399791, 0.07970842030193497907, 0.08068626093675593247, 0.08264194220639786703, 0.08361978284121884819, 0.08459762347603982935, 0.08655330474568176391 ),
 .UNSPECIFIED. ) ;
#3762=CARTESIAN_POINT ( 'NONE',  ( -11.44045018991158003, 13.03826302799688186, 10.01684603989913747 ) ) ;
#3808=EDGE_CURVE ( 'NONE', #18205, #51545, #103887, .T. ) ;
#3844=CARTESIAN_POINT ( 'NONE',  ( 13.45742156688652713, 5.393973166499471006, -6.521729985601480095 ) ) ;
#3980=DIRECTION ( 'NONE',  ( 1.000000000000000000, 0.000000000000000000, 0.000000000000000000 ) ) ;
#3989=CARTESIAN_POINT ( 'NONE',  ( 16.10335319434522461, 21.83248469006533199, -0.8773453446276189283 ) ) ;
#4100=( NAMED_UNIT ( * ) SI_UNIT ( $, .STERADIAN. ) SOLID_ANGLE_UNIT ( ) );
#4180=CARTESIAN_POINT ( 'NONE',  ( 15.50079525336341391, 2.626985771264193747, -0.7904007780842380315 ) ) ;
#4197=CARTESIAN_POINT ( 'NONE',  ( -14.29190075645216318, 6.456385560668112866, -7.561819230143454362 ) ) ;
#4229=ORIENTED_EDGE ( 'NONE', *, *, #19401, .T. ) ;
#4240=CARTESIAN_POINT ( 'NONE',  ( 10.82293865544385980, 16.07063780477403370, 9.522976597001717280 ) ) ;
#4249=STYLED_ITEM ( 'NONE', ( #59422 ), #85702 ) ;
#4251=CARTESIAN_POINT ( 'NONE',  ( -14.29190075645648683, 6.456385560661901835, 7.561819230138081771 ) ) ;
#4265=CARTESIAN_POINT ( 'NONE',  ( -14.11571568429507018, 5.211159435679596719, 3.514002131789491390 ) ) ;
#4283=CARTESIAN_POINT ( 'NONE',  ( -11.67857513420520554, 18.91569503322274315, 8.075412257376374470 ) ) ;
#4360=EDGE_CURVE ( 'NONE', #77575, #24576, #11605, .T. ) ;
#4363=CARTESIAN_POINT ( 'NONE',  ( 14.21497376764425091, 4.168734049602408120, -4.751813484541924204 ) ) ;
#4471=FILL_AREA_STYLE ('',( #12019 ) ) ;
#4511=CARTESIAN_POINT ( 'NONE',  ( 14.81542429969936592, 22.88666905516098282, 2.089502384928102252 ) ) ;
#4516=( NAMED_UNIT ( * ) SI_UNIT ( $, .STERADIAN. ) SOLID_ANGLE_UNIT ( ) );
#4522=CARTESIAN_POINT ( 'NONE',  ( 15.37029426978700641, 3.165964433755443785, 3.249157221777043691 ) ) ;
#4587=ORIENTED_EDGE ( 'NONE', *, *, #84416, .F. ) ;
#4589=CARTESIAN_POINT ( 'NONE',  ( 10.88898873136430900, 9.029852970804380874, 10.01842208923438093 ) ) ;
#4593=PRESENTATION_STYLE_ASSIGNMENT (( #43984 ) ) ;
#4637=ORIENTED_EDGE ( 'NONE', *, *, #3451, .F. ) ;
#4640=CARTESIAN_POINT ( 'NONE',  ( -10.15339062455847774, 12.11279177272005114, 10.55309804651484917 ) ) ;
#4688=EDGE_CURVE ( 'NONE', #23419, #51169, #94179, .T. ) ;
#4695=CARTESIAN_POINT ( 'NONE',  ( 12.28614183020320993, 9.928251283239491798, -9.534296537348968315 ) ) ;
#4701=CIRCLE ( 'NONE', #42561, 12.16579798332631945 ) ;
#4731=DIRECTION ( 'NONE',  ( -0.06744659395726224083, -0.6445107564549500401, 0.7616146281272652141 ) ) ;
#4753=ORIENTED_EDGE ( 'NONE', *, *, #82521, .T. ) ;
#4759=CARTESIAN_POINT ( 'NONE',  ( 0.000000000000000000, 0.9999999999999943379, -13.99700487351915612 ) ) ;
#4773=CARTESIAN_POINT ( 'NONE',  ( 11.83113230997336096, 21.33428827753630586, 7.412539468226875705 ) ) ;
#4807=EDGE_CURVE ( 'NONE', #51545, #71001, #102800, .T. ) ;
#4817=CARTESIAN_POINT ( 'NONE',  ( -11.96408628757766124, 19.58595713499403246, 7.540478412421575349 ) ) ;
#4836=COLOUR_RGB ( '', 0.40784314, 0.44705882, 0.49803922) ;
#4939=SURFACE_SIDE_STYLE ('',( #71249 ) ) ;
#4950=CARTESIAN_POINT ( 'NONE',  ( -15.04954976391476151, 5.409063359390556158, -6.531832031858459509 ) ) ;
#5002=DIRECTION ( 'NONE',  ( 1.000000000000000000, 0.000000000000000000, 0.000000000000000000 ) ) ;
#5016=CARTESIAN_POINT ( 'NONE',  ( 1.775369994829482681E-15, -3.035766082959412415E-15, 13.99700487351915612 ) ) ;
#5032=DIRECTION ( 'NONE',  ( 0.000000000000000000, 1.000000000000000000, 0.000000000000000000 ) ) ;
#5043=EDGE_LOOP ( 'NONE', ( #5173, #101488, #106168, #47632 ) ) ;
#5050=CARTESIAN_POINT ( 'NONE',  ( 15.64030048137924744, 21.26710225494773709, -5.626279437266589412 ) ) ;
#5061=CARTESIAN_POINT ( 'NONE',  ( 15.50532557111870346, 2.637300882400162472, -0.8493220884092024248 ) ) ;
#5163=CARTESIAN_POINT ( 'NONE',  ( -16.07816244837682262, 5.101897851420679864, 4.232350007288137483 ) ) ;
#5167=CARTESIAN_POINT ( 'NONE',  ( -13.29658299777914365, 24.24203747270784248, -3.158285168994459990 ) ) ;
#5173=ORIENTED_EDGE ( 'NONE', *, *, #83164, .F. ) ;
#5174=STYLED_ITEM ( 'NONE', ( #88841 ), #46357 ) ;
#5224=CARTESIAN_POINT ( 'NONE',  ( 12.04984095491230001, 10.49891318694633036, -9.702198819609494151 ) ) ;
#5236=CARTESIAN_POINT ( 'NONE',  ( 5.839745530781595306, 11.94268483786961710, 3.859993546116442076 ) ) ;
#5237=DIRECTION ( 'NONE',  ( -1.000000000000000000, -0.000000000000000000, -0.000000000000000000 ) ) ;
#5246=AXIS2_PLACEMENT_3D ( 'NONE', #45040, #43430, #3503 ) ;
#5248=CARTESIAN_POINT ( 'NONE',  ( 15.28599664425438931, 3.173649883747179157, -3.309198297947178347 ) ) ;
#5290=VERTEX_POINT ( 'NONE', #21740 ) ;
#5294=EDGE_CURVE ( 'NONE', #21676, #78587, #86478, .T. ) ;
#5311=CARTESIAN_POINT ( 'NONE',  ( 13.92939803725944259, 2.720116051143699476, 5.535782246604351364 ) ) ;
#5341=COLOUR_RGB ( '', 0.66274510, 0.83137255, 0.94901961) ;
#5378=CARTESIAN_POINT ( 'NONE',  ( 19.50000000000000000, 12.99999999999999289, -6.999999999999999112 ) ) ;
#5413=UNCERTAINTY_MEASURE_WITH_UNIT (LENGTH_MEASURE( 1.000000000000000082E-05 ), #8374, 'distance_accuracy_value', 'NONE');
#5424=CARTESIAN_POINT ( 'NONE',  ( -6.769785244694102921, 16.58291839180370175, 1.797443303175164209 ) ) ;
#5485=EDGE_CURVE ( 'NONE', #53038, #87076, #104833, .T. ) ;
#5487=CARTESIAN_POINT ( 'NONE',  ( -14.36577178753972994, 3.159923610478025058, 4.257245723753212197 ) ) ;
#5567=CARTESIAN_POINT ( 'NONE',  ( 14.89114929831721135, 23.12273819885287551, 0.2580741681286142231 ) ) ;
#5617=EDGE_CURVE ( 'NONE', #1532, #98241, #63186, .T. ) ;
#5618=CARTESIAN_POINT ( 'NONE',  ( 14.29190075645216851, 12.99999999999999289, 0.000000000000000000 ) ) ;
#5619=CARTESIAN_POINT ( 'NONE',  ( -16.14595037814582312, 20.48432867205941932, 4.554748808009636996 ) ) ;
#5631=STYLED_ITEM ( 'NONE', ( #31255 ), #51855 ) ;
#5640=CARTESIAN_POINT ( 'NONE',  ( 13.59280763750475884, 24.77127418736844788, 0.3411334247565424582 ) ) ;
#5685=CARTESIAN_POINT ( 'NONE',  ( -11.68076828077231788, 20.99435049431988531, 7.705273641827774966 ) ) ;
#5749=FILL_AREA_STYLE_COLOUR ( '', #83777 ) ;
#5754=CARTESIAN_POINT ( 'NONE',  ( 14.29190075645216851, 12.99999999999999289, 0.000000000000000000 ) ) ;
#5760=CARTESIAN_POINT ( 'NONE',  ( 14.95236164052716354, 4.204970931308103843, -5.179833178256462389 ) ) ;
#5817=ADVANCED_FACE ( 'NONE', ( #88521 ), #47507, .T. ) ;
#5819=CARTESIAN_POINT ( 'NONE',  ( -16.02741078272298481, 4.186345391436172569, -2.546409592408216405 ) ) ;
#5835=ORIENTED_EDGE ( 'NONE', *, *, #53165, .F. ) ;
#5859=CARTESIAN_POINT ( 'NONE',  ( -15.05442749816165104, 5.404963020241716265, 6.510488844712470247 ) ) ;
#5860=EDGE_CURVE ( 'NONE', #55614, #29736, #105103, .T. ) ;
#5873=ORIENTED_EDGE ( 'NONE', *, *, #32065, .T. ) ;
#5927=UNCERTAINTY_MEASURE_WITH_UNIT (LENGTH_MEASURE( 1.000000000000000082E-05 ), #83278, 'distance_accuracy_value', 'NONE');
#5933=CARTESIAN_POINT ( 'NONE',  ( -6.984126283073809560, 16.97239697123576718, 0.5389771161762291207 ) ) ;
#5937=CARTESIAN_POINT ( 'NONE',  ( 11.78141822354596790, 19.16435779204854839, -7.887621174215590614 ) ) ;
#5958=EDGE_LOOP ( 'NONE', ( #32627, #79300 ) ) ;
#5985=CARTESIAN_POINT ( 'NONE',  ( -10.65671340344253615, 14.86024801717850075, -9.830563606247649133 ) ) ;
#6001=CARTESIAN_POINT ( 'NONE',  ( 20.00000000000000000, 12.99999999999999289, 7.500000000000000000 ) ) ;
#6025=CARTESIAN_POINT ( 'NONE',  ( -16.14595037866548566, 6.775806037742684751, -6.185188124845088176 ) ) ;
#6050=CARTESIAN_POINT ( 'NONE',  ( -11.42046787539988983, 14.07301214197669736, 9.944540719455840616 ) ) ;
#6088=DIRECTION ( 'NONE',  ( 0.000000000000000000, 0.000000000000000000, 1.000000000000000000 ) ) ;
#6140=CARTESIAN_POINT ( 'NONE',  ( -14.89114929831680811, 23.12273819885389869, 0.2580741681018605682 ) ) ;
#6158=CARTESIAN_POINT ( 'NONE',  ( 12.52134978615753624, 5.248113740467461596, 8.137638698453219632 ) ) ;
#6223=AXIS2_PLACEMENT_3D ( 'NONE', #81237, #64553, #73684 ) ;
#6240=SURFACE_SIDE_STYLE ('',( #32690 ) ) ;
#6263=AXIS2_PLACEMENT_3D ( 'NONE', #74279, #89938, #25240 ) ;
#6267=PRESENTATION_STYLE_ASSIGNMENT (( #19347 ) ) ;
#6276=CIRCLE ( 'NONE', #102778, 14.99698745252234566 ) ;
#6278=CARTESIAN_POINT ( 'NONE',  ( 15.88092429543898199, 3.778118985502688432, -3.597070451748276554 ) ) ;
#6307=FILL_AREA_STYLE ('',( #6850 ) ) ;
#6328=ORIENTED_EDGE ( 'NONE', *, *, #37600, .T. ) ;
#6338=CARTESIAN_POINT ( 'NONE',  ( 11.76188850610210324, 11.37617155923007850, 9.883422334778840579 ) ) ;
#6375=DIRECTION ( 'NONE',  ( 0.000000000000000000, -1.000000000000000000, 0.000000000000000000 ) ) ;
#6396=FILL_AREA_STYLE ('',( #96496 ) ) ;
#6429=CIRCLE ( 'NONE', #82196, 1.000000000000000888 ) ;
#6468=CARTESIAN_POINT ( 'NONE',  ( 13.51938198577379779, 20.10480383923402314, -7.057786160369816209 ) ) ;
#6515=CARTESIAN_POINT ( 'NONE',  ( -10.68634199976106913, 15.16085412443461600, -9.768909368315327413 ) ) ;
#6522=CARTESIAN_POINT ( 'NONE',  ( 14.29190075645216851, 6.456385560668102208, -7.561819230143448145 ) ) ;
#6552=CARTESIAN_POINT ( 'NONE',  ( -16.07816244837236752, 5.101897851396789640, -4.232350007281748816 ) ) ;
#6567=( GEOMETRIC_REPRESENTATION_CONTEXT ( 3 ) GLOBAL_UNCERTAINTY_ASSIGNED_CONTEXT ( ( #77244 ) ) GLOBAL_UNIT_ASSIGNED_CONTEXT ( ( #64804, #88557, #104192 ) ) REPRESENTATION_CONTEXT ( 'NONE', 'WORKASPACE' ) );
#6579=CARTESIAN_POINT ( 'NONE',  ( -12.01355111023868361, 17.09226180711344156, 9.133437940809011835 ) ) ;
#6621=CARTESIAN_POINT ( 'NONE',  ( -16.01293590580086601, 3.745177866445512205, 0.6593600975892003335 ) ) ;
#6636=CARTESIAN_POINT ( 'NONE',  ( 15.29749241881251720, 3.521433830170186408, -3.946287723025023730 ) ) ;
#6805=CARTESIAN_POINT ( 'NONE',  ( 13.94300157694754461, 6.957367296339416640, 7.995343388762901959 ) ) ;
#6850=FILL_AREA_STYLE_COLOUR ( '', #51650 ) ;
#6855=DIRECTION ( 'NONE',  ( 0.000000000000000000, 0.000000000000000000, -1.000000000000000000 ) ) ;
#6885=CARTESIAN_POINT ( 'NONE',  ( 14.21511914782685082, 4.168509763117726585, 4.751336337983421032 ) ) ;
#6914=( LENGTH_UNIT ( ) NAMED_UNIT ( * ) SI_UNIT ( .MILLI., .METRE. ) );
#6916=EDGE_CURVE ( 'NONE', #58722, #77575, #94222, .T. ) ;
#6923=CARTESIAN_POINT ( 'NONE',  ( -11.95123837978005987, 10.78773100921685568, 9.767553402682516150 ) ) ;
#7002=CARTESIAN_POINT ( 'NONE',  ( 10.88589977545114351, 9.036462124315177036, -10.02161580976883215 ) ) ;
#7023=CARTESIAN_POINT ( 'NONE',  ( -14.82123240307241296, 22.90480191141017485, -2.008241678658511997 ) ) ;
#7041=CARTESIAN_POINT ( 'NONE',  ( 14.91461412207629422, 1.322532983912315885, -1.774597446655453048 ) ) ;
#7050=CARTESIAN_POINT ( 'NONE',  ( -13.94870603575048129, 6.950772033844307529, -7.980207832019492464 ) ) ;
#7060=CARTESIAN_POINT ( 'NONE',  ( -14.46400437353393009, 2.949852469129314869, 3.921916857617072871 ) ) ;
#7066=EDGE_CURVE ( 'NONE', #27686, #93080, #32641, .T. ) ;
#7113=CARTESIAN_POINT ( 'NONE',  ( -12.45419940525628988, 18.15241938591149662, 8.579672614547556364 ) ) ;
#7148=CARTESIAN_POINT ( 'NONE',  ( -16.03930365250128176, 4.449877915869574707, -3.144092084174250346 ) ) ;
#7164=CARTESIAN_POINT ( 'NONE',  ( -14.91461412207421411, 1.322532983914281868, 1.774597446674108792 ) ) ;
#7177=ORIENTED_EDGE ( 'NONE', *, *, #54153, .F. ) ;
#7200=EDGE_CURVE ( 'NONE', #77985, #38642, #44323, .T. ) ;
#7228=DIRECTION ( 'NONE',  ( 0.000000000000000000, 0.000000000000000000, 1.000000000000000000 ) ) ;
#7273=DIRECTION ( 'NONE',  ( 1.000000000000000000, -0.000000000000000000, -0.000000000000000000 ) ) ;
#7324=CARTESIAN_POINT ( 'NONE',  ( 14.01122214394832177, 20.85898477414747632, 6.193124377965379068 ) ) ;
#7358=ORIENTED_EDGE ( 'NONE', *, *, #59904, .F. ) ;
#7407=CARTESIAN_POINT ( 'NONE',  ( 12.99054989286523032, 8.523705905438497155, 8.946233657869846922 ) ) ;
#7451=( NAMED_UNIT ( * ) SI_UNIT ( $, .STERADIAN. ) SOLID_ANGLE_UNIT ( ) );
#7513=ORIENTED_EDGE ( 'NONE', *, *, #11088, .F. ) ;
#7522=CARTESIAN_POINT ( 'NONE',  ( 11.66163491649460582, 15.90954947651264817, -9.571573500822044167 ) ) ;
#7561=CARTESIAN_POINT ( 'NONE',  ( 14.11595029532510104, 2.410436752314617959, -5.024000119269091513 ) ) ;
#7569=CARTESIAN_POINT ( 'NONE',  ( -11.45800518213875563, 9.451812037517163034, -9.373485686765249625 ) ) ;
#7605=ADVANCED_FACE ( 'NONE', ( #52569 ), #37644, .T. ) ;
#7608=CARTESIAN_POINT ( 'NONE',  ( -15.82318872385282127, 4.444012391137944995, -4.874853782837179850 ) ) ;
#7653=CARTESIAN_POINT ( 'NONE',  ( -10.07965646519730996, 12.76099312266119057, 10.57234460686555089 ) ) ;
#7673=SURFACE_STYLE_FILL_AREA ( #48667 ) ;
#7691=CARTESIAN_POINT ( 'NONE',  ( -14.68536286785258405, 1.589102881333048334, -3.051189359061289963 ) ) ;
#7702=CARTESIAN_POINT ( 'NONE',  ( 9.797174393178825657E-16, -3.035766082959412415E-15, -8.000000000000000000 ) ) ;
#7748=CARTESIAN_POINT ( 'NONE',  ( 11.53713417953937537, 7.347077458742750089, -9.367700058475382008 ) ) ;
#7828=TOROIDAL_SURFACE ( 'NONE', #76732, 9.500000000000000000, 2.000000000000000000 ) ;
#7857=CARTESIAN_POINT ( 'NONE',  ( 12.67395752198872572, 18.60270564220093448, 8.290360506785944494 ) ) ;
#7903=UNCERTAINTY_MEASURE_WITH_UNIT (LENGTH_MEASURE( 1.000000000000000082E-05 ), #56106, 'distance_accuracy_value', 'NONE');
#7907=CARTESIAN_POINT ( 'NONE',  ( 0.000000000000000000, 0.9999999999999970024, 0.000000000000000000 ) ) ;
#7945=STYLED_ITEM ( 'NONE', ( #20410 ), #28364 ) ;
#7970=FACE_OUTER_BOUND ( 'NONE', #3129, .T. ) ;
#7985=AXIS2_PLACEMENT_3D ( 'NONE', #89132, #105832, #81531 ) ;
#8008=CARTESIAN_POINT ( 'NONE',  ( 15.12883790376646509, 3.606441264071186037, -4.265930408067698743 ) ) ;
#8066=CARTESIAN_POINT ( 'NONE',  ( 11.77243489797928611, 11.38584543533899662, -9.872918751301874352 ) ) ;
#8082=ADVANCED_FACE ( 'NONE', ( #48052 ), #23833, .T. ) ;
#8103=COLOUR_RGB ( '', 0.08235294, 0.09019608, 0.10196078) ;
#8107=SURFACE_SIDE_STYLE ('',( #48562 ) ) ;
#8109=CARTESIAN_POINT ( 'NONE',  ( -13.59364004637736123, 24.77274705659938547, 0.5873110997852482029 ) ) ;
#8127=STYLED_ITEM ( 'NONE', ( #75941 ), #26207 ) ;
#8198=CARTESIAN_POINT ( 'NONE',  ( -11.54938679239317345, 7.303627399110830254, 9.359616978869953030 ) ) ;
#8215=CARTESIAN_POINT ( 'NONE',  ( -15.94096206886600875, 3.082184004823651957, -0.3571785271768571635 ) ) ;
#8232=CARTESIAN_POINT ( 'NONE',  ( -14.99580413333973539, 1.250310433696842249, 0.8744943966991981510 ) ) ;
#8328=EDGE_LOOP ( 'NONE', ( #99980, #42592, #54426, #52255 ) ) ;
#8334=ORIENTED_EDGE ( 'NONE', *, *, #47314, .F. ) ;
#8340=ORIENTED_EDGE ( 'NONE', *, *, #3616, .T. ) ;
#8363=CARTESIAN_POINT ( 'NONE',  ( -6.925180474901644345, 9.132181797818848423, 1.053794444618463721 ) ) ;
#8370=CARTESIAN_POINT ( 'NONE',  ( -19.50000000000000000, 12.99999999999999289, -7.500000000000000000 ) ) ;
#8374=( LENGTH_UNIT ( ) NAMED_UNIT ( * ) SI_UNIT ( .MILLI., .METRE. ) );
#8396=CARTESIAN_POINT ( 'NONE',  ( 11.69515844949617644, 11.66155101967946983, 9.916752703385080636 ) ) ;
#8445=DIRECTION ( 'NONE',  ( 0.000000000000000000, 0.000000000000000000, -1.000000000000000000 ) ) ;
#8451=CARTESIAN_POINT ( 'NONE',  ( 16.14595037822608603, 20.73084165115993827, 4.192529328850663539 ) ) ;
#8482=CARTESIAN_POINT ( 'NONE',  ( 0.000000000000000000, 35.00000000000000000, 0.000000000000000000 ) ) ;
#8542=CARTESIAN_POINT ( 'NONE',  ( 15.30823401445614884, 3.112986885589654751, 3.167215778812773941 ) ) ;
#8600=CARTESIAN_POINT ( 'NONE',  ( 12.93869051862456310, 23.58149963681356454, -4.611847144011028909 ) ) ;
#8614=( GEOMETRIC_REPRESENTATION_CONTEXT ( 3 ) GLOBAL_UNCERTAINTY_ASSIGNED_CONTEXT ( ( #64625 ) ) GLOBAL_UNIT_ASSIGNED_CONTEXT ( ( #65092, #82336, #39774 ) ) REPRESENTATION_CONTEXT ( 'NONE', 'WORKASPACE' ) );
#8644=CARTESIAN_POINT ( 'NONE',  ( -13.04265871945630728, 19.29919692355796457, -7.785367473261247007 ) ) ;
#8657=CARTESIAN_POINT ( 'NONE',  ( 12.15290226144649566, 17.45440320673788293, -8.961931909917964845 ) ) ;
#8779=DIRECTION ( 'NONE',  ( 1.000000000000000000, -0.000000000000000000, -0.000000000000000000 ) ) ;
#8818=CARTESIAN_POINT ( 'NONE',  ( 10.05028520371290490, 14.77158978979456272, -10.42891015365750995 ) ) ;
#8851=SURFACE_STYLE_USAGE ( .BOTH. , #51439 ) ;
#8881=CARTESIAN_POINT ( 'NONE',  ( 0.000000000000000000, 1.005902684993156715, 0.000000000000000000 ) ) ;
#8922=CARTESIAN_POINT ( 'NONE',  ( 11.48424297320331888, 12.75586303188949522, 10.00391324386538550 ) ) ;
#8927=FACE_OUTER_BOUND ( 'NONE', #57363, .T. ) ;
#8937=FACE_OUTER_BOUND ( 'NONE', #58035, .T. ) ;
#8943=DIRECTION ( 'NONE',  ( 0.000000000000000000, -0.000000000000000000, 1.000000000000000000 ) ) ;
#9065=SURFACE_STYLE_USAGE ( .BOTH. , #73805 ) ;
#9077=COLOUR_RGB ( '', 0.09019608, 0.27058824, 0.51372549) ;
#9121=CARTESIAN_POINT ( 'NONE',  ( 15.64030048137865947, 6.456385560668104873, 7.561819230143442816 ) ) ;
#9123=CARTESIAN_POINT ( 'NONE',  ( 13.75587262240292930, 20.47468597617315567, -6.665350514229143819 ) ) ;
#9163=CARTESIAN_POINT ( 'NONE',  ( -12.78782033920715833, 21.25124815179102811, -5.673828052979907000 ) ) ;
#9188=FACE_OUTER_BOUND ( 'NONE', #34576, .T. ) ;
#9197=ORIENTED_EDGE ( 'NONE', *, *, #42849, .T. ) ;
#9216=EDGE_LOOP ( 'NONE', ( #84480, #32244 ) ) ;
#9284=ADVANCED_FACE ( 'NONE', ( #68163 ), #7828, .F. ) ;
#9288=EDGE_LOOP ( 'NONE', ( #60258, #100269 ) ) ;
#9289=STYLED_ITEM ( 'NONE', ( #94566 ), #61420 ) ;
#9294=CARTESIAN_POINT ( 'NONE',  ( 14.88745091283334077, 23.11123547206230811, 0.5085106042973103202 ) ) ;
#9305=FILL_AREA_STYLE ('',( #83209 ) ) ;
#9308=CARTESIAN_POINT ( 'NONE',  ( 0.000000000000000000, 35.00000000000000000, 0.000000000000000000 ) ) ;
#9349=DIRECTION ( 'NONE',  ( 0.000000000000000000, 0.000000000000000000, -1.000000000000000000 ) ) ;
#9353=DIRECTION ( 'NONE',  ( 0.000000000000000000, 0.000000000000000000, -1.000000000000000000 ) ) ;
#9387=CYLINDRICAL_SURFACE ( 'NONE', #19077, 7.000000000000000000 ) ;
#9417=CARTESIAN_POINT ( 'NONE',  ( 14.29190075645217028, 19.61368180395370331, 4.501023549821925762 ) ) ;
#9433=SURFACE_STYLE_USAGE ( .BOTH. , #100059 ) ;
#9444=AXIS2_PLACEMENT_3D ( 'NONE', #101680, #2970, #93594 ) ;
#9522=PRESENTATION_STYLE_ASSIGNMENT (( #42434 ) ) ;
#9523=CIRCLE ( 'NONE', #59453, 4.000000000000000000 ) ;
#9536=MECHANICAL_DESIGN_GEOMETRIC_PRESENTATION_REPRESENTATION('',(#85313),#55945);
#9545=CARTESIAN_POINT ( 'NONE',  ( 14.89734172081147179, 1.349300515449291193, -1.760806480387048012 ) ) ;
#9584=DIRECTION ( 'NONE',  ( 1.000000000000000000, -0.000000000000000000, -0.000000000000000000 ) ) ;
#9591=CARTESIAN_POINT ( 'NONE',  ( 15.92744347757530221, 3.245128719855334243, 1.809264762061174148 ) ) ;
#9595=CARTESIAN_POINT ( 'NONE',  ( 15.19414944962543501, 3.422781246271796807, 3.910013010458846860 ) ) ;
#9599=CARTESIAN_POINT ( 'NONE',  ( -19.50000000000000000, 12.99999999999999289, -6.999999999999999112 ) ) ;
#9650=CARTESIAN_POINT ( 'NONE',  ( 13.55851780043528443, 24.71083649413047212, -1.216380116763536856 ) ) ;
#9674=TOROIDAL_SURFACE ( 'NONE', #28680, 6.999999999999999112, 0.5000000000000000000 ) ;
#9697=CARTESIAN_POINT ( 'NONE',  ( -13.32385011686026566, 24.28998873518373358, -2.970456920810112145 ) ) ;
#9712=CARTESIAN_POINT ( 'NONE',  ( 14.29190075645646907, 21.26710225494832329, -5.626279437268317807 ) ) ;
#9792=CIRCLE ( 'NONE', #70090, 11.18527996897366528 ) ;
#9862=CARTESIAN_POINT ( 'NONE',  ( 16.02749411895483078, 4.188372957633037963, -2.551519145317325155 ) ) ;
#9928=ORIENTED_EDGE ( 'NONE', *, *, #5617, .T. ) ;
#9988=CARTESIAN_POINT ( 'NONE',  ( -14.98982670280977203, 2.030473042281319529, -0.4147640935789676520 ) ) ;
#10029=ORIENTED_EDGE ( 'NONE', *, *, #59904, .T. ) ;
#10077=EDGE_CURVE ( 'NONE', #78587, #68971, #9523, .T. ) ;
#10090=CARTESIAN_POINT ( 'NONE',  ( 15.39795322966678981, 3.054092008340477449, -2.852131183220913080 ) ) ;
#10137=CARTESIAN_POINT ( 'NONE',  ( 16.01537386455376932, 3.832633078742941457, 1.292357405299655815 ) ) ;
#10177=( BOUNDED_SURFACE ( )  B_SPLINE_SURFACE ( 3, 2, ( 
 ( #3356, #70211, #103633 ),
 ( #95547, #62145, #21174 ),
 ( #45939, #102037, #78818 ),
 ( #85334, #29785, #4950 ),
 ( #21691, #54524, #46466 ),
 ( #93964, #19587, #11419 ),
 ( #77240, #20114, #7050 ),
 ( #80402, #64769, #72326 ),
 ( #87994, #97126, #46981 ),
 ( #23811, #63189, #79879 ),
 ( #57185, #48031, #96612 ),
 ( #80939, #15148, #22748 ),
 ( #105230, #7569, #32426 ),
 ( #56656, #39967, #56110 ),
 ( #64256, #40486, #73365 ),
 ( #89581, #72838, #49089 ),
 ( #71261, #105749, #106264 ),
 ( #15674, #104155, #88523 ),
 ( #14597, #63728, #23266 ),
 ( #65296, #5985, #98187 ),
 ( #16207, #6515, #39449 ),
 ( #31885, #30301, #48564 ),
 ( #55585, #38396, #14072 ),
 ( #89045, #24342, #22214 ),
 ( #47510, #97644, #81455 ),
 ( #90101, #31375, #96082 ),
 ( #81991, #55064, #38914 ),
 ( #71781, #104690, #30842 ),
 ( #27002, #59883, #8644 ),
 ( #18913, #91706, #73904 ),
 ( #34561, #42077, #50169 ),
 ( #42607, #9163, #49634 ),
 ( #66351, #67435, #25404 ),
 ( #84141, #74960, #10238 ),
 ( #17823, #99236, #26472 ),
 ( #43152, #2131, #76035 ),
 ( #50674, #25953, #99784 ),
 ( #35085, #67955, #58813 ),
 ( #9697, #51758, #1599 ),
 ( #83072, #100838, #41548 ),
 ( #92756, #100310, #82540 ),
 ( #33478, #34027, #83589 ),
 ( #74434, #1052, #513 ),
 ( #8109, #58264, #59343 ),
 ( #66900, #75505, #91188 ),
 ( #41023, #17295, #49063 ),
 ( #51215, #32955, #65825 ),
 ( #92207, #98704, #24859 ),
 ( #18364, #57709, #90636 ),
 ( #16744, #102447, #36694 ),
 ( #84672, #85755, #77108 ),
 ( #61475, #86288, #19454 ),
 ( #37211, #93298, #78683 ),
 ( #52827, #94368, #94906 ),
 ( #12886, #43673, #62529 ),
 ( #11828, #21555, #85199 ),
 ( #53369, #76561, #44758 ),
 ( #60420, #52289, #69557 ),
 ( #68499, #4817, #101908 ),
 ( #45284, #21046, #28592 ),
 ( #2672, #4283, #20531 ),
 ( #78164, #45807, #12360 ),
 ( #29657, #3224, #69034 ),
 ( #70080, #10756, #35624 ),
 ( #101390, #19982, #102982 ),
 ( #77646, #27541, #29143 ),
 ( #53881, #62013, #11284 ),
 ( #60939, #103505, #86813 ),
 ( #95415, #37753, #44217 ),
 ( #36166, #93829, #3762 ),
 ( #70615, #28066, #40356 ),
 ( #15010, #14467, #105105 ),
 ( #80809, #46338, #6923 ),
 ( #30168, #87337, #31245 ),
 ( #63599, #31758, #13414 ),
 ( #39845, #104558, #79753 ),
 ( #64134, #48439, #22081 ),
 ( #95956, #54936, #89454 ),
 ( #15546, #97003, #105619 ),
 ( #87864, #54391, #23142 ),
 ( #88393, #72201, #38785 ),
 ( #23675, #55982, #5859 ),
 ( #72717, #71652, #13947 ),
 ( #47382, #56524, #88917 ),
 ( #65164, #96486, #55461 ),
 ( #22629, #79226, #73234 ) ),
 .UNSPECIFIED., .F., .F., .T. ) 
 B_SPLINE_SURFACE_WITH_KNOTS ( ( 4, 2, 2, 2, 2, 2, 2, 2, 2, 2, 2, 2, 2, 2, 2, 2, 2, 2, 2, 2, 2, 2, 2, 2, 2, 2, 2, 2, 2, 2, 2, 2, 2, 2, 2, 2, 2, 2, 2, 2, 2, 2, 4 ),
 ( 3, 3 ),
 ( 0.02634172422113034359, 0.02840705912624018337, 0.03047239403135001967, 0.03253772893645985598, 0.03357039638901477413, 0.03460306384156969228, 0.03666839874667952859, 0.03873373365178936489, 0.04079906855689920120, 0.04183173600945411935, 0.04286440346200903750, 0.04389707091456395566, 0.04492973836711887381, 0.04699507327222871012, 0.04906040817733854642, 0.05112574308244838273, 0.05215841053500330088, 0.05319107798755821903, 0.05525641289266805534, 0.05628908034522297349, 0.05732174779777789164, 0.05938708270288772795, 0.06145241760799756425, 0.06351775251310740056, 0.06455041996566232565, 0.06558308741821723686, 0.06661575487077214808, 0.06764842232332707317, 0.06971375722843690947, 0.07074642468099182069, 0.07177909213354674578, 0.07384442703865658209, 0.07487709449121149330, 0.07590976194376641839, 0.07797509684887625470, 0.08004043175398609100, 0.08210576665909592731, 0.08417110156420576361, 0.08623643646931559992, 0.08830177137442543622, 0.08933443882698036131, 0.09036710627953527253, 0.09243244118464510883 ),
 ( 0.000000000000000000, 1.000000000000000000 ),
 .UNSPECIFIED. ) 
 GEOMETRIC_REPRESENTATION_ITEM ( )  RATIONAL_B_SPLINE_SURFACE ( (
 ( 1.000000000000000000, 0.7574005004452331047, 1.000000000000000000),
 ( 1.000000000000000000, 0.7678086279399819469, 1.000000000000000000),
 ( 1.000000000000000000, 0.7789244113962565663, 1.000000000000000000),
 ( 1.000000000000000000, 0.8016316046185457678, 1.000000000000000000),
 ( 1.000000000000000000, 0.8132948587418985520, 1.000000000000000000),
 ( 1.000000000000000000, 0.8357926363597657504, 1.000000000000000000),
 ( 1.000000000000000000, 0.8466816614498698934, 1.000000000000000000),
 ( 1.000000000000000000, 0.8621003063894946417, 1.000000000000000000),
 ( 1.000000000000000000, 0.8670881561880485755, 1.000000000000000000),
 ( 1.000000000000000000, 0.8766998973978601395, 1.000000000000000000),
 ( 1.000000000000000000, 0.8813097246197982848, 1.000000000000000000),
 ( 1.000000000000000000, 0.8943093724793236277, 1.000000000000000000),
 ( 1.000000000000000000, 0.9019441283705564860, 1.000000000000000000),
 ( 1.000000000000000000, 0.9147276970316240430, 1.000000000000000000),
 ( 1.000000000000000000, 0.9198874818270340592, 1.000000000000000000),
 ( 1.000000000000000000, 0.9267810911149524378, 1.000000000000000000),
 ( 1.000000000000000000, 0.9285972973398308739, 1.000000000000000000),
 ( 1.000000000000000000, 0.9286317451279045843, 1.000000000000000000),
 ( 1.000000000000000000, 0.9281858723822534740, 1.000000000000000000),
 ( 1.000000000000000000, 0.9264403244317799269, 1.000000000000000000),
 ( 1.000000000000000000, 0.9251417076504168113, 1.000000000000000000),
 ( 1.000000000000000000, 0.9217459610402344294, 1.000000000000000000),
 ( 1.000000000000000000, 0.9196487206541981152, 1.000000000000000000),
 ( 1.000000000000000000, 0.9146973172701069466, 1.000000000000000000),
 ( 1.000000000000000000, 0.9118257467883083001, 1.000000000000000000),
 ( 1.000000000000000000, 0.9023115364206620859, 1.000000000000000000),
 ( 1.000000000000000000, 0.8947616380145678727, 1.000000000000000000),
 ( 1.000000000000000000, 0.8778037105062616030, 1.000000000000000000),
 ( 1.000000000000000000, 0.8683411594436707404, 1.000000000000000000),
 ( 1.000000000000000000, 0.8486622380153294731, 1.000000000000000000),
 ( 1.000000000000000000, 0.8383870565666979857, 1.000000000000000000),
 ( 1.000000000000000000, 0.8228778961941588532, 1.000000000000000000),
 ( 1.000000000000000000, 0.8176744109529193727, 1.000000000000000000),
 ( 1.000000000000000000, 0.8074431182712563659, 1.000000000000000000),
 ( 1.000000000000000000, 0.8024440009126241335, 1.000000000000000000),
 ( 1.000000000000000000, 0.7879812762414096783, 1.000000000000000000),
 ( 1.000000000000000000, 0.7790450003668998313, 1.000000000000000000),
 ( 1.000000000000000000, 0.7675477608643064276, 1.000000000000000000),
 ( 1.000000000000000000, 0.7640348910737623234, 1.000000000000000000),
 ( 1.000000000000000000, 0.7578134264054862124, 1.000000000000000000),
 ( 1.000000000000000000, 0.7551270526901607827, 1.000000000000000000),
 ( 1.000000000000000000, 0.7486526966700658425, 1.000000000000000000),
 ( 1.000000000000000000, 0.7463801361677054880, 1.000000000000000000),
 ( 1.000000000000000000, 0.7463127164022264060, 1.000000000000000000),
 ( 1.000000000000000000, 0.7486000928341679517, 1.000000000000000000),
 ( 1.000000000000000000, 0.7571961929099836341, 1.000000000000000000),
 ( 1.000000000000000000, 0.7634567568201346965, 1.000000000000000000),
 ( 1.000000000000000000, 0.7750654466030536538, 1.000000000000000000),
 ( 1.000000000000000000, 0.7793053813432258004, 1.000000000000000000),
 ( 1.000000000000000000, 0.7882146539232089966, 1.000000000000000000),
 ( 1.000000000000000000, 0.7929022008513715303, 1.000000000000000000),
 ( 1.000000000000000000, 0.8025966256814718314, 1.000000000000000000),
 ( 1.000000000000000000, 0.8076036615378768824, 1.000000000000000000),
 ( 1.000000000000000000, 0.8178083114314877999, 1.000000000000000000),
 ( 1.000000000000000000, 0.8230260163010280072, 1.000000000000000000),
 ( 1.000000000000000000, 0.8386284071981864319, 1.000000000000000000),
 ( 1.000000000000000000, 0.8489266526250032197, 1.000000000000000000),
 ( 1.000000000000000000, 0.8636680828574543334, 1.000000000000000000),
 ( 1.000000000000000000, 0.8684659181649216908, 1.000000000000000000),
 ( 1.000000000000000000, 0.8777487523221890742, 1.000000000000000000),
 ( 1.000000000000000000, 0.8822506950759456679, 1.000000000000000000),
 ( 1.000000000000000000, 0.8950015522441460147, 1.000000000000000000),
 ( 1.000000000000000000, 0.9025191533021075241, 1.000000000000000000),
 ( 1.000000000000000000, 0.9119467452851578448, 1.000000000000000000),
 ( 1.000000000000000000, 0.9147804332722992982, 1.000000000000000000),
 ( 1.000000000000000000, 0.9197485997668242153, 1.000000000000000000),
 ( 1.000000000000000000, 0.9218702435470463863, 1.000000000000000000),
 ( 1.000000000000000000, 0.9269502648627369057, 1.000000000000000000),
 ( 1.000000000000000000, 0.9286883261994179906, 1.000000000000000000),
 ( 1.000000000000000000, 0.9285486022662473582, 1.000000000000000000),
 ( 1.000000000000000000, 0.9266646312235611305, 1.000000000000000000),
 ( 1.000000000000000000, 0.9196578271540671867, 1.000000000000000000),
 ( 1.000000000000000000, 0.9144563017674409711, 1.000000000000000000),
 ( 1.000000000000000000, 0.9016091177945602109, 1.000000000000000000),
 ( 1.000000000000000000, 0.8939535693208001677, 1.000000000000000000),
 ( 1.000000000000000000, 0.8766021895685242038, 1.000000000000000000),
 ( 1.000000000000000000, 0.8668555216837416921, 1.000000000000000000),
 ( 1.000000000000000000, 0.8462716989656902111, 1.000000000000000000),
 ( 1.000000000000000000, 0.8353730651404011054, 1.000000000000000000),
 ( 1.000000000000000000, 0.8184904932442989001, 1.000000000000000000),
 ( 1.000000000000000000, 0.8127516586172595092, 1.000000000000000000),
 ( 1.000000000000000000, 0.8012917549111018278, 1.000000000000000000),
 ( 1.000000000000000000, 0.7955843342310977562, 1.000000000000000000),
 ( 1.000000000000000000, 0.7786720583377687577, 1.000000000000000000),
 ( 1.000000000000000000, 0.7676722966783382507, 1.000000000000000000),
 ( 1.000000000000000000, 0.7574005004457203816, 1.000000000000000000) ) ) 
 REPRESENTATION_ITEM ( '' )  SURFACE ( )  );
#10192=CARTESIAN_POINT ( 'NONE',  ( 14.95236164054155559, 4.204970931318847249, 5.179833178257711168 ) ) ;
#10194=CARTESIAN_POINT ( 'NONE',  ( 13.42487756469949467, 22.38025266455044715, 3.525519932714368032 ) ) ;
#10216=AXIS2_PLACEMENT_3D ( 'NONE', #103129, #45432, #78307 ) ;
#10238=CARTESIAN_POINT ( 'NONE',  ( -14.42049321383198723, 21.45136809881161000, -5.352595841921786501 ) ) ;
#10251=FILL_AREA_STYLE ('',( #60954 ) ) ;
#10278=ORIENTED_EDGE ( 'NONE', *, *, #3616, .F. ) ;
#10283=DIRECTION ( 'NONE',  ( -1.000000000000000000, 0.000000000000000000, 0.000000000000000000 ) ) ;
#10290=CARTESIAN_POINT ( 'NONE',  ( 7.000182694785905824, 17.00031971603035430, -0.2646331733798831243 ) ) ;
#10291=EDGE_LOOP ( 'NONE', ( #13772, #57943, #22523 ) ) ;
#10361=CIRCLE ( 'NONE', #48236, 12.16579798332631945 ) ;
#10378=DIRECTION ( 'NONE',  ( 1.000000000000000000, 0.000000000000000000, 0.000000000000000000 ) ) ;
#10430=CARTESIAN_POINT ( 'NONE',  ( 14.29190075645222358, 19.61368180395867356, -4.501023549814667568 ) ) ;
#10465=SURFACE_STYLE_USAGE ( .BOTH. , #19151 ) ;
#10515=CARTESIAN_POINT ( 'NONE',  ( -14.46174234134181624, 2.926873011486890164, -3.961839331262607899 ) ) ;
#10530=SURFACE_STYLE_USAGE ( .BOTH. , #101145 ) ;
#10534=CARTESIAN_POINT ( 'NONE',  ( -1.836601268058450879E-15, 1.005902684993158047, -14.99698745252234566 ) ) ;
#10541=CARTESIAN_POINT ( 'NONE',  ( -14.29190075645216851, 12.99999999999999289, 0.000000000000000000 ) ) ;
#10654=CARTESIAN_POINT ( 'NONE',  ( 0.000000000000000000, 0.9999999999999970024, 0.000000000000000000 ) ) ;
#10658=CARTESIAN_POINT ( 'NONE',  ( 15.05785784214677037, 3.824195276769946972, 4.604276673498408634 ) ) ;
#10716=CARTESIAN_POINT ( 'NONE',  ( 13.60307364985986744, 22.67980367822178067, -2.541457539100715923 ) ) ;
#10728=AXIS2_PLACEMENT_3D ( 'NONE', #14983, #57033, #47878 ) ;
#10756=CARTESIAN_POINT ( 'NONE',  ( -11.00368196113950781, 16.88294327153011309, 9.222626775518351749 ) ) ;
#10809=CARTESIAN_POINT ( 'NONE',  ( 5.835236874069059887, 14.05646090491896594, 3.867049007331976540 ) ) ;
#10832=CARTESIAN_POINT ( 'NONE',  ( -5.834906339164276368, 14.05456999085811631, 3.867544450381312338 ) ) ;
#10835=CARTESIAN_POINT ( 'NONE',  ( -16.14595037822608248, 20.23371447308014481, 4.922994507609256054 ) ) ;
#10967=( NAMED_UNIT ( * ) PLANE_ANGLE_UNIT ( ) SI_UNIT ( $, .RADIAN. ) );
#10990=DIRECTION ( 'NONE',  ( 0.000000000000000000, 0.000000000000000000, 1.000000000000000000 ) ) ;
#11021=DIRECTION ( 'NONE',  ( 1.427673741351707591E-16, -0.5626279437277410533, 0.8267102254942136907 ) ) ;
#11038=FACE_OUTER_BOUND ( 'NONE', #97615, .T. ) ;
#11041=CARTESIAN_POINT ( 'NONE',  ( -16.13469797932748051, 21.10829079391486474, -3.392296823503756276 ) ) ;
#11054=CARTESIAN_POINT ( 'NONE',  ( 28.12328997684540610, 24.73290587908618932, -14.06164498842270838 ) ) ;
#11076=CARTESIAN_POINT ( 'NONE',  ( -14.11595029532502643, 2.410436752314748521, -5.024000119269296682 ) ) ;
#11082=EDGE_CURVE ( 'NONE', #57762, #21618, #105764, .T. ) ;
#11088=EDGE_CURVE ( 'NONE', #32538, #48149, #16570, .T. ) ;
#11099=CARTESIAN_POINT ( 'NONE',  ( 0.000000000000000000, 35.00000000000000000, 0.000000000000000000 ) ) ;
#11107=( BOUNDED_SURFACE ( )  B_SPLINE_SURFACE ( 3, 2, ( 
 ( #18104, #18648, #59085 ),
 ( #26749, #10515, #92495 ),
 ( #34302, #75787, #42890 ),
 ( #83875, #59626, #1339 ),
 ( #2423, #42354, #67178 ),
 ( #43957, #54013, #2952 ),
 ( #75241, #9988, #51505 ),
 ( #43429, #35367, #68235 ),
 ( #101129, #19201, #27289 ),
 ( #60172, #35911, #86957 ),
 ( #62156, #95049, #13024 ),
 ( #105758, #23282, #56120 ),
 ( #55076, #79888, #39460 ),
 ( #31901, #7060, #72339 ),
 ( #54536, #5487, #15157 ),
 ( #39978, #87480, #64780 ) ),
 .UNSPECIFIED., .F., .F., .F. ) 
 B_SPLINE_SURFACE_WITH_KNOTS ( ( 4, 2, 2, 2, 2, 2, 2, 4 ),
 ( 3, 3 ),
 ( 0.01025942932839742083, 0.01330785678259500601, 0.01483207050969379860, 0.01635628423679259119, 0.01788049796389138205, 0.01940471169099017290, 0.02092892541808896723, 0.02245313914518775808 ),
 ( 0.3005395333822533654, 1.000000000000000000 ),
 .UNSPECIFIED. ) 
 GEOMETRIC_REPRESENTATION_ITEM ( )  RATIONAL_B_SPLINE_SURFACE ( (
 ( 0.8980036390037944294, 0.8303112408401904787, 1.000000000000000000),
 ( 0.9116818979159437841, 0.8530674133114374280, 1.000000000000000000),
 ( 0.9228127777807579868, 0.8715855758632119477, 1.000000000000000000),
 ( 0.9345546761373868527, 0.8911202743843785745, 1.000000000000000000),
 ( 0.9375544117806571265, 0.8961108585007369065, 1.000000000000000000),
 ( 0.9415935919673855681, 0.9028307401437135615, 1.000000000000000000),
 ( 0.9426280110961577918, 0.9045516770153640973, 1.000000000000000000),
 ( 0.9426141662316074310, 0.9045286436653173778, 1.000000000000000000),
 ( 0.9415455155258669606, 0.9027507565871785156, 1.000000000000000000),
 ( 0.9374309181787365830, 0.8959054053270217866, 1.000000000000000000),
 ( 0.9344062863247678541, 0.8908734020162928369, 1.000000000000000000),
 ( 0.9266839229609493689, 0.8780259019271841048, 1.000000000000000000),
 ( 0.9219922915685003773, 0.8702205537594245310, 1.000000000000000000),
 ( 0.9110602365930542401, 0.8520331711338884340, 1.000000000000000000),
 ( 0.9047689875046434071, 0.8415665795716911202, 1.000000000000000000),
 ( 0.8980036390032253291, 0.8303112408392433474, 1.000000000000000000) ) ) 
 REPRESENTATION_ITEM ( '' )  SURFACE ( )  );
#11174=CARTESIAN_POINT ( 'NONE',  ( 6.924369423635565290, 9.133630944394992568, -1.059067681833820940 ) ) ;
#11180=FILL_AREA_STYLE ('',( #52181 ) ) ;
#11185=ORIENTED_EDGE ( 'NONE', *, *, #101178, .T. ) ;
#11245=CARTESIAN_POINT ( 'NONE',  ( 11.77969503333905799, 19.16028191506968525, 7.890828749183966373 ) ) ;
#11284=CARTESIAN_POINT ( 'NONE',  ( -11.59363613587280817, 15.60194627659213751, 9.659792498495315627 ) ) ;
#11306=ORIENTED_EDGE ( 'NONE', *, *, #37328, .F. ) ;
#11342=( LENGTH_UNIT ( ) NAMED_UNIT ( * ) SI_UNIT ( .MILLI., .METRE. ) );
#11419=CARTESIAN_POINT ( 'NONE',  ( -14.22864388059377916, 6.541366219244691749, -7.652784845931969393 ) ) ;
#11444=SURFACE_STYLE_FILL_AREA ( #77266 ) ;
#11474=AXIS2_PLACEMENT_3D ( 'NONE', #46127, #79015, #79538 ) ;
#11475=CARTESIAN_POINT ( 'NONE',  ( -16.07917213302809856, 5.118112109469922899, -4.258304778695157999 ) ) ;
#11519=CARTESIAN_POINT ( 'NONE',  ( 14.87170168469208953, 23.06219547135946968, 1.058210525649228906 ) ) ;
#11605=CIRCLE ( 'NONE', #71903, 0.5000000000000004441 ) ;
#11665=DIRECTION ( 'NONE',  ( -0.000000000000000000, 1.000000000000000000, -0.000000000000000000 ) ) ;
#11666=STYLED_ITEM ( 'NONE', ( #76420 ), #67270 ) ;
#11709=CARTESIAN_POINT ( 'NONE',  ( 5.744562646538026840, 12.72967408581656201, 3.999999999999999112 ) ) ;
#11718=CARTESIAN_POINT ( 'NONE',  ( 16.03930365250129952, 4.449877915870326106, 3.144092084176011159 ) ) ;
#11744=( GEOMETRIC_REPRESENTATION_CONTEXT ( 3 ) GLOBAL_UNCERTAINTY_ASSIGNED_CONTEXT ( ( #96986 ) ) GLOBAL_UNIT_ASSIGNED_CONTEXT ( ( #12661, #45065, #29436 ) ) REPRESENTATION_CONTEXT ( 'NONE', 'WORKASPACE' ) );
#11755=AXIS2_PLACEMENT_3D ( 'NONE', #47618, #80519, #46574 ) ;
#11784=CARTESIAN_POINT ( 'NONE',  ( 13.16322211195412528, 19.50307498396639971, 7.601507676661267254 ) ) ;
#11793=DIRECTION ( 'NONE',  ( -1.000000000000000000, 0.000000000000000000, 0.000000000000000000 ) ) ;
#11828=CARTESIAN_POINT ( 'NONE',  ( -12.02757221648704444, 21.76040073964190213, 7.011289084098431879 ) ) ;
#11857=FACE_OUTER_BOUND ( 'NONE', #2396, .T. ) ;
#11934=CARTESIAN_POINT ( 'NONE',  ( 16.14595037822613932, 20.23371447307979665, -4.922994507609789849 ) ) ;
#11965=CIRCLE ( 'NONE', #94693, 7.000000000000000000 ) ;
#11975=FACE_OUTER_BOUND ( 'NONE', #20438, .T. ) ;
#11978=COLOUR_RGB ( '', 0.08235294, 0.09019608, 0.10196078) ;
#12013=MECHANICAL_DESIGN_GEOMETRIC_PRESENTATION_REPRESENTATION('',(#80921),#56817);
#12019=FILL_AREA_STYLE_COLOUR ( '', #638 ) ;
#12044=DIRECTION ( 'NONE',  ( 0.000000000000000000, 8.673617379884033500E-16, 1.000000000000000000 ) ) ;
#12055=CARTESIAN_POINT ( 'NONE',  ( -12.59046650546478929, 9.287358138947649167, -9.291413486181960835 ) ) ;
#12062=CARTESIAN_POINT ( 'NONE',  ( 14.86018380392216542, 23.02630934695024578, 1.319261379110572285 ) ) ;
#12076=ORIENTED_EDGE ( 'NONE', *, *, #3073, .T. ) ;
#12125=SURFACE_STYLE_FILL_AREA ( #61232 ) ;
#12155=CARTESIAN_POINT ( 'NONE',  ( 1.369801731157060329E-15, 34.00000000000000711, 11.18527996897366528 ) ) ;
#12185=MECHANICAL_DESIGN_GEOMETRIC_PRESENTATION_REPRESENTATION('',(#13866),#17371);
#12223=VERTEX_POINT ( 'NONE', #31579 ) ;
#12246=ORIENTED_EDGE ( 'NONE', *, *, #103892, .T. ) ;
#12292=EDGE_LOOP ( 'NONE', ( #81766, #101694, #74252, #72190 ) ) ;
#12309=VERTEX_POINT ( 'NONE', #105440 ) ;
#12320=CARTESIAN_POINT ( 'NONE',  ( 11.50368691626706052, 15.08202484978332336, 9.785078861151950136 ) ) ;
#12360=CARTESIAN_POINT ( 'NONE',  ( -12.34988716859649394, 17.93113568933560131, 8.716900997220561109 ) ) ;
#12411=CARTESIAN_POINT ( 'NONE',  ( 6.085184064390054992, 15.01719713745825580, -3.463681541593110147 ) ) ;
#12486=SURFACE_STYLE_FILL_AREA ( #53497 ) ;
#12497=EDGE_CURVE ( 'NONE', #95018, #102396, #104920, .T. ) ;
#12558=B_SPLINE_CURVE_WITH_KNOTS ( 'NONE', 3,
 ( #85090, #93180, #66778, #99119, #100727, #34450, #26889, #92640, #51644, #84564, #76448, #50563, #11174, #83480, #35505, #67320, #33366, #101278, #27429, #58141, #91069, #17176, #1486, #33909, #99667, #42492, #26366, #59230, #92103, #18246, #84022, #5236, #52706, #53773, #11709, #37641 ),
 .UNSPECIFIED., .F., .F.,
 ( 4, 2, 2, 2, 2, 2, 2, 2, 2, 2, 2, 2, 2, 2, 2, 2, 2, 4 ),
 ( 1.734723475976807094E-18, 0.0007996222028895917872, 0.001599244405779181840, 0.003198488811558361511, 0.003998111014447950154, 0.004797733217337540532, 0.005597355420227129175, 0.006396977623116717818, 0.006796788724561513874, 0.007196599826006308195, 0.007996222028895896838, 0.008795844231785485481, 0.009595466434675074124, 0.01039508863756466277, 0.01119471084045425141, 0.01159452194189904313, 0.01199433304334383658, 0.01279395524623341482 ),
 .UNSPECIFIED. ) ;
#12581=CARTESIAN_POINT ( 'NONE',  ( -14.01679991993937868, 20.87195963505847374, -6.206891275040918643 ) ) ;
#12587=CARTESIAN_POINT ( 'NONE',  ( 15.72449985194334943, 22.05660461081444268, 3.876398783277453131 ) ) ;
#12598=PRESENTATION_STYLE_ASSIGNMENT (( #103748 ) ) ;
#12635=CARTESIAN_POINT ( 'NONE',  ( -14.59912249378909443, 22.21173916952167815, -3.991112248694528297 ) ) ;
#12640=ADVANCED_FACE ( 'NONE', ( #97208, #22833 ), #56194, .T. ) ;
#12656=( GEOMETRIC_REPRESENTATION_CONTEXT ( 3 ) GLOBAL_UNCERTAINTY_ASSIGNED_CONTEXT ( ( #27651 ) ) GLOBAL_UNIT_ASSIGNED_CONTEXT ( ( #95144, #78938, #100162 ) ) REPRESENTATION_CONTEXT ( 'NONE', 'WORKASPACE' ) );
#12661=( LENGTH_UNIT ( ) NAMED_UNIT ( * ) SI_UNIT ( .MILLI., .METRE. ) );
#12677=( BOUNDED_SURFACE ( )  B_SPLINE_SURFACE ( 3, 2, ( 
 ( #52917, #12967, #77733 ),
 ( #102533, #4363, #36250 ),
 ( #70165, #29738, #62611 ),
 ( #85841, #94458, #78769 ),
 ( #38353, #86894, #69119 ),
 ( #28150, #3844, #61026 ),
 ( #70698, #37834, #95497 ),
 ( #71213, #36775, #20069 ),
 ( #53455, #86375, #54475 ),
 ( #87424, #45367, #78250 ),
 ( #103069, #13498, #79307 ),
 ( #60505, #93390, #19536 ),
 ( #52373, #97597, #105182 ),
 ( #30794, #32380, #47984 ),
 ( #30250, #23223, #7002 ),
 ( #16160, #63679, #31327 ),
 ( #105699, #22702, #89537 ),
 ( #8066, #72278, #80891 ),
 ( #24294, #65252, #79832 ),
 ( #63138, #55539, #49047 ),
 ( #64209, #81944, #31841 ),
 ( #22164, #72794, #55013 ),
 ( #96038, #38864, #14027 ),
 ( #40978, #104642, #39922 ),
 ( #7522, #57143, #56612 ),
 ( #73866, #48520, #15097 ),
 ( #64723, #87945, #71730 ),
 ( #46933, #73320, #97079 ),
 ( #81411, #89002, #23764 ),
 ( #15628, #96567, #98142 ),
 ( #88476, #5937, #56062 ),
 ( #14551, #47460, #40440 ),
 ( #106216, #80353, #90056 ),
 ( #6468, #39400, #83550 ),
 ( #9123, #66311, #92171 ),
 ( #58217, #67909, #91142 ),
 ( #66852, #17252, #84629 ),
 ( #74915, #99741, #67390 ),
 ( #32909, #75463, #43632 ),
 ( #99192, #50123, #8600 ),
 ( #50632, #25911, #26956 ),
 ( #92710, #100796, #75994 ),
 ( #59836, #10716, #43106 ),
 ( #58767, #41502, #18870 ),
 ( #16700, #98664, #24816 ),
 ( #91665, #74390, #9650 ),
 ( #17779, #83032, #42560 ),
 ( #51714, #25354, #59299 ),
 ( #106761, #42033, #1556 ),
 ( #65786, #34521, #2092 ),
 ( #57668, #999, #33980 ),
 ( #100272, #90591, #26434 ),
 ( #18321, #82499, #51171 ),
 ( #49591, #10194, #84094 ),
 ( #35045, #469, #33437 ),
 ( #70578, #52785, #60375 ),
 ( #85156, #29105, #61432 ),
 ( #13370, #19945, #12843 ),
 ( #37174, #93250, #78638 ),
 ( #21005, #28551, #70035 ),
 ( #86247, #77061, #4773 ),
 ( #11784, #77603, #53329 ),
 ( #19413, #52247, #45762 ),
 ( #94326, #11245, #95377 ),
 ( #20491, #62486, #78124 ),
 ( #3177, #44174, #53845 ),
 ( #36123, #101346, #2632 ),
 ( #76521, #61973, #101867 ),
 ( #68992, #28027, #60896 ),
 ( #102939, #4240, #93784 ),
 ( #54349, #94864, #86776 ),
 ( #12320, #102401, #103465 ),
 ( #21513, #29614, #37715 ),
 ( #87291, #35578, #68451 ),
 ( #45245, #85707, #27500 ),
 ( #44714, #3721, #36651 ),
 ( #69516, #46818, #89419 ),
 ( #6338, #47863, #48401 ),
 ( #72680, #71614, #38231 ),
 ( #96967, #72158, #73195 ),
 ( #97477, #65127, #22585 ),
 ( #7407, #57021, #15511 ),
 ( #105066, #87825, #98024 ),
 ( #63015, #71095, #103985 ),
 ( #89935, #79715, #81291 ),
 ( #39280, #80770, #40320 ),
 ( #32247, #14967, #38743 ),
 ( #104516, #24177, #88356 ),
 ( #30127, #106098, #23102 ),
 ( #46297, #79186, #30668 ),
 ( #31722, #6885, #5311 ),
 ( #95913, #64607, #22037 ) ),
 .UNSPECIFIED., .F., .F., .F. ) 
 B_SPLINE_SURFACE_WITH_KNOTS ( ( 4, 2, 2, 2, 2, 2, 2, 2, 2, 2, 2, 2, 2, 2, 2, 2, 2, 2, 2, 2, 2, 2, 2, 2, 2, 2, 2, 2, 2, 2, 2, 2, 2, 2, 2, 2, 2, 2, 2, 2, 2, 2, 2, 2, 2, 4 ),
 ( 3, 3 ),
 ( 0.06669982031955556945, 0.06876509657217773352, 0.06979773469848882250, 0.07083037282479989760, 0.07289564907742207556, 0.07392828720373315066, 0.07496092533004423963, 0.07702620158266640371, 0.07805883970897749269, 0.07909147783528858167, 0.08115675408791074574, 0.08322203034053290982, 0.08425466846684398492, 0.08528730659315507390, 0.08735258284577723797, 0.08838522097208832695, 0.08941785909839941593, 0.09148313535102158001, 0.09251577347733266898, 0.09354841160364374408, 0.09561368785626592204, 0.09664632598257699714, 0.09767896410888808612, 0.09974424036151025019, 0.1007768784878213253, 0.1018095166141324143, 0.1038747928667545783, 0.1059400691193767563, 0.1069727072456878314, 0.1080053453719989204, 0.1100706216246210845, 0.1111032597509321734, 0.1121358978772432624, 0.1142011741298654265, 0.1152338122561765155, 0.1162664503824875906, 0.1172990885087986657, 0.1183317266351097546, 0.1203970028877319187, 0.1224622791403540967, 0.1245275553929762608, 0.1255601935192873497, 0.1265928316455984248, 0.1286581078982206028, 0.1307233841508427807, 0.1327886604034649309 ),
 ( 0.000000000000000000, 1.000000000000000000 ),
 .UNSPECIFIED. ) 
 GEOMETRIC_REPRESENTATION_ITEM ( )  RATIONAL_B_SPLINE_SURFACE ( (
 ( 1.000000000000000000, 0.7574005004452292189, 1.000000000000000000),
 ( 1.000000000000000000, 0.7677881811269363643, 1.000000000000000000),
 ( 1.000000000000000000, 0.7789318350104040833, 1.000000000000000000),
 ( 1.000000000000000000, 0.7960806233368639129, 1.000000000000000000),
 ( 1.000000000000000000, 0.8018814668295082271, 1.000000000000000000),
 ( 1.000000000000000000, 0.8133644828828667794, 1.000000000000000000),
 ( 1.000000000000000000, 0.8190665470845299723, 1.000000000000000000),
 ( 1.000000000000000000, 0.8359369182568276990, 1.000000000000000000),
 ( 1.000000000000000000, 0.8468678900967679946, 1.000000000000000000),
 ( 1.000000000000000000, 0.8623942012808557545, 1.000000000000000000),
 ( 1.000000000000000000, 0.8674321864558991457, 1.000000000000000000),
 ( 1.000000000000000000, 0.8770051489341853523, 1.000000000000000000),
 ( 1.000000000000000000, 0.8815607036504458094, 1.000000000000000000),
 ( 1.000000000000000000, 0.8944702760352207793, 1.000000000000000000),
 ( 1.000000000000000000, 0.9020741755135933682, 1.000000000000000000),
 ( 1.000000000000000000, 0.9116398635700204700, 1.000000000000000000),
 ( 1.000000000000000000, 0.9145203804056111219, 1.000000000000000000),
 ( 1.000000000000000000, 0.9195812072905432677, 1.000000000000000000),
 ( 1.000000000000000000, 0.9216946987500304056, 1.000000000000000000),
 ( 1.000000000000000000, 0.9268367359168875330, 1.000000000000000000),
 ( 1.000000000000000000, 0.9286336546224613908, 1.000000000000000000),
 ( 1.000000000000000000, 0.9286071640124593518, 1.000000000000000000),
 ( 1.000000000000000000, 0.9267923817204344328, 1.000000000000000000),
 ( 1.000000000000000000, 0.9216310222028860633, 1.000000000000000000),
 ( 1.000000000000000000, 0.9194923251911391038, 1.000000000000000000),
 ( 1.000000000000000000, 0.9144746405666180911, 1.000000000000000000),
 ( 1.000000000000000000, 0.9116205049900496515, 1.000000000000000000),
 ( 1.000000000000000000, 0.9021468917526797027, 1.000000000000000000),
 ( 1.000000000000000000, 0.8946191197500281689, 1.000000000000000000),
 ( 1.000000000000000000, 0.8818899456451816388, 1.000000000000000000),
 ( 1.000000000000000000, 0.8773890157683175151, 1.000000000000000000),
 ( 1.000000000000000000, 0.8680974434632235948, 1.000000000000000000),
 ( 1.000000000000000000, 0.8632987000236833630, 1.000000000000000000),
 ( 1.000000000000000000, 0.8485654811955887222, 1.000000000000000000),
 ( 1.000000000000000000, 0.8382874571751192105, 1.000000000000000000),
 ( 1.000000000000000000, 0.8227376552933685083, 1.000000000000000000),
 ( 1.000000000000000000, 0.8175323482194468694, 1.000000000000000000),
 ( 1.000000000000000000, 0.8073811642434209901, 1.000000000000000000),
 ( 1.000000000000000000, 0.8024119013038333303, 1.000000000000000000),
 ( 1.000000000000000000, 0.7880089399916923032, 1.000000000000000000),
 ( 1.000000000000000000, 0.7790711632268805253, 1.000000000000000000),
 ( 1.000000000000000000, 0.7675359669597019430, 1.000000000000000000),
 ( 1.000000000000000000, 0.7639873508355347065, 1.000000000000000000),
 ( 1.000000000000000000, 0.7577827882268577397, 1.000000000000000000),
 ( 1.000000000000000000, 0.7551371035826408562, 1.000000000000000000),
 ( 1.000000000000000000, 0.7486932950123758035, 1.000000000000000000),
 ( 1.000000000000000000, 0.7463960882512324924, 1.000000000000000000),
 ( 1.000000000000000000, 0.7463222396104609579, 1.000000000000000000),
 ( 1.000000000000000000, 0.7468675288289394754, 1.000000000000000000),
 ( 1.000000000000000000, 0.7490620983608700101, 1.000000000000000000),
 ( 1.000000000000000000, 0.7507019908674972264, 1.000000000000000000),
 ( 1.000000000000000000, 0.7570958978920665494, 1.000000000000000000),
 ( 1.000000000000000000, 0.7633320146645002913, 1.000000000000000000),
 ( 1.000000000000000000, 0.7788212728674728247, 1.000000000000000000),
 ( 1.000000000000000000, 0.7878352555929534207, 1.000000000000000000),
 ( 1.000000000000000000, 0.8023450074323924541, 1.000000000000000000),
 ( 1.000000000000000000, 0.8073489187299826009, 1.000000000000000000),
 ( 1.000000000000000000, 0.8175636883870323057, 1.000000000000000000),
 ( 1.000000000000000000, 0.8227765755982912044, 1.000000000000000000),
 ( 1.000000000000000000, 0.8383040332954234675, 1.000000000000000000),
 ( 1.000000000000000000, 0.8485844023486135423, 1.000000000000000000),
 ( 1.000000000000000000, 0.8633419897287184508, 1.000000000000000000),
 ( 1.000000000000000000, 0.8681522541980656316, 1.000000000000000000),
 ( 1.000000000000000000, 0.8774719602938952923, 1.000000000000000000),
 ( 1.000000000000000000, 0.8819611993470838351, 1.000000000000000000),
 ( 1.000000000000000000, 0.8946520234114340164, 1.000000000000000000),
 ( 1.000000000000000000, 0.9021503839376829870, 1.000000000000000000),
 ( 1.000000000000000000, 0.9115857724357809833, 1.000000000000000000),
 ( 1.000000000000000000, 0.9144281988544517015, 1.000000000000000000),
 ( 1.000000000000000000, 0.9194277157626919994, 1.000000000000000000),
 ( 1.000000000000000000, 0.9215935472969858377, 1.000000000000000000),
 ( 1.000000000000000000, 0.9250730986170641046, 1.000000000000000000),
 ( 1.000000000000000000, 0.9263961809546490400, 1.000000000000000000),
 ( 1.000000000000000000, 0.9281725017696547120, 1.000000000000000000),
 ( 1.000000000000000000, 0.9286249391977352552, 1.000000000000000000),
 ( 1.000000000000000000, 0.9286114671366180184, 1.000000000000000000),
 ( 1.000000000000000000, 0.9268058022047847011, 1.000000000000000000),
 ( 1.000000000000000000, 0.9199284077393417025, 1.000000000000000000),
 ( 1.000000000000000000, 0.9147782303380489477, 1.000000000000000000),
 ( 1.000000000000000000, 0.9019685211012331560, 1.000000000000000000),
 ( 1.000000000000000000, 0.8943002565130824255, 1.000000000000000000),
 ( 1.000000000000000000, 0.8812085285205289997, 1.000000000000000000),
 ( 1.000000000000000000, 0.8765859265514783782, 1.000000000000000000),
 ( 1.000000000000000000, 0.8669906351561719182, 1.000000000000000000),
 ( 1.000000000000000000, 0.8620032267436350537, 1.000000000000000000),
 ( 1.000000000000000000, 0.8465577714266654397, 1.000000000000000000),
 ( 1.000000000000000000, 0.8356129422299747311, 1.000000000000000000),
 ( 1.000000000000000000, 0.8129121367137768228, 1.000000000000000000),
 ( 1.000000000000000000, 0.8014017695925140794, 1.000000000000000000),
 ( 1.000000000000000000, 0.7788404441292630098, 1.000000000000000000),
 ( 1.000000000000000000, 0.7677783875764762067, 1.000000000000000000),
 ( 1.000000000000000000, 0.7574005004452295520, 1.000000000000000000) ) ) 
 REPRESENTATION_ITEM ( '' )  SURFACE ( )  );
#12700=FACE_OUTER_BOUND ( 'NONE', #66154, .T. ) ;
#12703=CARTESIAN_POINT ( 'NONE',  ( -10.89640271560199913, 9.008026361043889096, 10.01173798417218741 ) ) ;
#12784=CARTESIAN_POINT ( 'NONE',  ( 16.01236629286577084, 3.722328191965672772, -0.3359674915983867916 ) ) ;
#12794=( GEOMETRIC_REPRESENTATION_CONTEXT ( 3 ) GLOBAL_UNCERTAINTY_ASSIGNED_CONTEXT ( ( #52636 ) ) GLOBAL_UNIT_ASSIGNED_CONTEXT ( ( #6914, #82404, #73227 ) ) REPRESENTATION_CONTEXT ( 'NONE', 'WORKASPACE' ) );
#12801=CARTESIAN_POINT ( 'NONE',  ( -14.84266821126070468, 4.606643506668206989, -5.685020543978184904 ) ) ;
#12843=CARTESIAN_POINT ( 'NONE',  ( 12.42143139619339998, 22.57321393022593981, 6.089946764847198324 ) ) ;
#12886=CARTESIAN_POINT ( 'NONE',  ( -12.32115138270090249, 22.37014720597713335, 6.335230956775115274 ) ) ;
#12941=ORIENTED_EDGE ( 'NONE', *, *, #7066, .F. ) ;
#12967=CARTESIAN_POINT ( 'NONE',  ( 14.35785620000817886, 3.948300967435878661, -4.282865182293611461 ) ) ;
#12985=DIRECTION ( 'NONE',  ( 1.000000000000000000, 0.000000000000000000, 0.000000000000000000 ) ) ;
#12988=MECHANICAL_DESIGN_GEOMETRIC_PRESENTATION_REPRESENTATION('',(#35450),#100832);
#12991=AXIS2_PLACEMENT_3D ( 'NONE', #37128, #62441, #69993 ) ;
#13024=CARTESIAN_POINT ( 'NONE',  ( -14.83949740352256796, 1.410031051014996262, 2.190466161101272125 ) ) ;
#13025=EDGE_LOOP ( 'NONE', ( #77328, #102266, #67734, #101989 ) ) ;
#13073=CARTESIAN_POINT ( 'NONE',  ( 15.05785784214677392, 3.824195276769925655, -4.604276673498363337 ) ) ;
#13097=CARTESIAN_POINT ( 'NONE',  ( 0.000000000000000000, 34.00000000000000000, 0.000000000000000000 ) ) ;
#13114=CARTESIAN_POINT ( 'NONE',  ( 14.37769637048558380, 21.52932494092931037, -5.240976541679501111 ) ) ;
#13127=CARTESIAN_POINT ( 'NONE',  ( 14.99550388410314028, 1.250601500879723993, 0.4346214790721553145 ) ) ;
#13186=CARTESIAN_POINT ( 'NONE',  ( 13.43938057902250804, 24.49812678790979703, 2.259581829312952372 ) ) ;
#13235=CARTESIAN_POINT ( 'NONE',  ( -10.05892818186027426, 14.73916874890172757, -10.42188144405744588 ) ) ;
#13236=AXIS2_PLACEMENT_3D ( 'NONE', #84985, #101166, #85525 ) ;
#13240=EDGE_LOOP ( 'NONE', ( #37355, #47183 ) ) ;
#13258=CIRCLE ( 'NONE', #11474, 7.500000000000000000 ) ;
#13310=CARTESIAN_POINT ( 'NONE',  ( 15.68120647348477625, 6.021684053265039971, -7.051923121165705410 ) ) ;
#13313=AXIS2_PLACEMENT_3D ( 'NONE', #89676, #48130, #6088 ) ;
#13328=CARTESIAN_POINT ( 'NONE',  ( -14.44768974034866815, 5.957293599828318520, -7.129930386717086677 ) ) ;
#13370=CARTESIAN_POINT ( 'NONE',  ( 14.20818530214469355, 21.14724737011036382, 5.805003007643574797 ) ) ;
#13414=CARTESIAN_POINT ( 'NONE',  ( -12.61127845791341073, 9.233498968002802343, 9.278883048239569220 ) ) ;
#13452=ORIENTED_EDGE ( 'NONE', *, *, #52220, .F. ) ;
#13468=CIRCLE ( 'NONE', #27318, 6.999999999999999112 ) ;
#13474=ORIENTED_EDGE ( 'NONE', *, *, #4807, .T. ) ;
#13487=UNCERTAINTY_MEASURE_WITH_UNIT (LENGTH_MEASURE( 1.000000000000000082E-05 ), #1886, 'distance_accuracy_value', 'NONE');
#13498=CARTESIAN_POINT ( 'NONE',  ( 12.33236296408734844, 7.452231929829893353, -8.337237077754760861 ) ) ;
#13540=DIRECTION ( 'NONE',  ( -1.000000000000000000, -0.000000000000000000, -0.000000000000000000 ) ) ;
#13542=AXIS2_PLACEMENT_3D ( 'NONE', #13572, #55606, #14623 ) ;
#13546=FACE_OUTER_BOUND ( 'NONE', #44296, .T. ) ;
#13547=( NAMED_UNIT ( * ) PLANE_ANGLE_UNIT ( ) SI_UNIT ( $, .RADIAN. ) );
#13572=CARTESIAN_POINT ( 'NONE',  ( 0.000000000000000000, 35.00000000000000000, 0.000000000000000000 ) ) ;
#13590=EDGE_CURVE ( 'NONE', #27686, #97818, #69845, .T. ) ;
#13650=CARTESIAN_POINT ( 'NONE',  ( 14.59912249379336657, 22.21173916953564387, -3.991112248664791640 ) ) ;
#13655=( LENGTH_UNIT ( ) NAMED_UNIT ( * ) SI_UNIT ( .MILLI., .METRE. ) );
#13656=ADVANCED_FACE ( 'NONE', ( #36808 ), #54517, .T. ) ;
#13701=CARTESIAN_POINT ( 'NONE',  ( -16.11127471224471464, 21.68306317501279779, 1.725009018224902047 ) ) ;
#13721=CARTESIAN_POINT ( 'NONE',  ( 11.54949964087943037, 7.317938515390196130, 9.354107198949744628 ) ) ;
#13733=CARTESIAN_POINT ( 'NONE',  ( -13.99268144847940576, 6.886032338477331649, 7.933613737989179349 ) ) ;
#13764=CARTESIAN_POINT ( 'NONE',  ( -13.29119999941515218, 24.23229826355910177, 3.185837010029002769 ) ) ;
#13772=ORIENTED_EDGE ( 'NONE', *, *, #28690, .T. ) ;
#13866=STYLED_ITEM ( 'NONE', ( #76310 ), #79178 ) ;
#13887=DIRECTION ( 'NONE',  ( 0.000000000000000000, 0.000000000000000000, 1.000000000000000000 ) ) ;
#13927=DIRECTION ( 'NONE',  ( 0.06744659395759022846, -0.6445107564563566926, -0.7616146281260456341 ) ) ;
#13947=CARTESIAN_POINT ( 'NONE',  ( -15.18386540887443914, 5.234509037293391565, 6.306189099687723676 ) ) ;
#13980=ORIENTED_EDGE ( 'NONE', *, *, #26895, .T. ) ;
#14022=CARTESIAN_POINT ( 'NONE',  ( -5.890693798151878546, 14.30979422482011820, -3.781785903083254574 ) ) ;
#14027=CARTESIAN_POINT ( 'NONE',  ( 10.06671572987654706, 15.03217639615420076, -10.38938273639670840 ) ) ;
#14072=CARTESIAN_POINT ( 'NONE',  ( -11.65716286615917952, 15.89043748982164139, -9.577315898548507178 ) ) ;
#14111=SURFACE_STYLE_USAGE ( .BOTH. , #77279 ) ;
#14172=CARTESIAN_POINT ( 'NONE',  ( -15.43758579534935294, 2.782614627094442739, 1.951547078892869491 ) ) ;
#14186=CARTESIAN_POINT ( 'NONE',  ( 15.26104615578792689, 3.717029890768877021, -4.293899008410894780 ) ) ;
#14226=CARTESIAN_POINT ( 'NONE',  ( -15.64030048137919593, 21.26710225494723616, 5.626279437267545092 ) ) ;
#14247=CARTESIAN_POINT ( 'NONE',  ( 10.29006311568609000, 16.62392477665889956, 10.00613480464933858 ) ) ;
#14291=CARTESIAN_POINT ( 'NONE',  ( -10.08052270137817352, 15.05801543190454694, -10.37155938391993537 ) ) ;
#14361=CARTESIAN_POINT ( 'NONE',  ( -11.46409645960823021, 12.99999999999756994, 10.00000000000000178 ) ) ;
#14363=CARTESIAN_POINT ( 'NONE',  ( 15.85122647056153333, 4.114663126756317624, -4.288211754877312210 ) ) ;
#14367=CARTESIAN_POINT ( 'NONE',  ( 15.35975064870966911, 2.980508189489460946, -2.732879807888741741 ) ) ;
#14412=CARTESIAN_POINT ( 'NONE',  ( -24.33159596665262470, 34.19642918197134662, -12.16579798332630880 ) ) ;
#14428=CARTESIAN_POINT ( 'NONE',  ( -16.01428880459204862, 3.811183212007244414, 1.301242280795995354 ) ) ;
#14467=CARTESIAN_POINT ( 'NONE',  ( -10.93976548513864167, 11.14550375312795438, 9.847392385548467075 ) ) ;
#14523=ORIENTED_EDGE ( 'NONE', *, *, #97591, .F. ) ;
#14526=AXIS2_PLACEMENT_3D ( 'NONE', #100331, #34045, #35107 ) ;
#14528=ORIENTED_EDGE ( 'NONE', *, *, #86666, .T. ) ;
#14551=CARTESIAN_POINT ( 'NONE',  ( 13.04586309976887470, 19.29735459000327324, -7.772842735983566342 ) ) ;
#14597=CARTESIAN_POINT ( 'NONE',  ( -10.04210299847170518, 14.33706770242568851, -10.47444268205537199 ) ) ;
#14623=DIRECTION ( 'NONE',  ( 0.000000000000000000, 0.000000000000000000, -1.000000000000000000 ) ) ;
#14638=CARTESIAN_POINT ( 'NONE',  ( -16.14595037822608958, 7.274337365584599091, -6.616591826375521457 ) ) ;
#14651=SURFACE_SIDE_STYLE ('',( #55634 ) ) ;
#14662=CARTESIAN_POINT ( 'NONE',  ( -12.61670886434728267, 18.48906243878285238, 8.368148073796660924 ) ) ;
#14704=CARTESIAN_POINT ( 'NONE',  ( -15.20015366321276495, 3.406002745437296753, 3.875710626047840446 ) ) ;
#14782=EDGE_CURVE ( 'NONE', #21618, #49400, #83752, .T. ) ;
#14783=CARTESIAN_POINT ( 'NONE',  ( 11.69764001847466339, 21.03308801239159109, -7.673093909533472257 ) ) ;
#14858=CARTESIAN_POINT ( 'NONE',  ( -5.744562646538028616, 12.72950497522988300, 4.000000000000000000 ) ) ;
#14952=FACE_OUTER_BOUND ( 'NONE', #46392, .T. ) ;
#14967=CARTESIAN_POINT ( 'NONE',  ( 13.03375404248404834, 6.122153719266105298, 7.298667805333264980 ) ) ;
#14983=CARTESIAN_POINT ( 'NONE',  ( 0.000000000000000000, 0.000000000000000000, 0.000000000000000000 ) ) ;
#14989=MECHANICAL_DESIGN_GEOMETRIC_PRESENTATION_REPRESENTATION('',(#8127),#35754);
#15010=CARTESIAN_POINT ( 'NONE',  ( -10.36378764587132117, 10.91134418945301832, 10.43617239968854982 ) ) ;
#15060=DIRECTION ( 'NONE',  ( -1.000000000000000000, -0.000000000000000000, -0.000000000000000000 ) ) ;
#15097=CARTESIAN_POINT ( 'NONE',  ( 10.36233036400907004, 16.98659626113961352, -9.892282517339653580 ) ) ;
#15117=CARTESIAN_POINT ( 'NONE',  ( -14.87367913736586900, 23.06835470864390558, 1.002906751349593506 ) ) ;
#15138=CARTESIAN_POINT ( 'NONE',  ( 14.24890542153238471, 2.189729425896414838, -4.659254829976903878 ) ) ;
#15148=CARTESIAN_POINT ( 'NONE',  ( -11.66708038261545965, 8.918174348190984091, -9.153312531148994680 ) ) ;
#15157=CARTESIAN_POINT ( 'NONE',  ( -14.24976063294461781, 2.188309765144745178, 4.656908667384352718 ) ) ;
#15167=CARTESIAN_POINT ( 'NONE',  ( 16.13647630347072948, 6.334953579828321857, -5.738861489052264453 ) ) ;
#15198=SURFACE_STYLE_USAGE ( .BOTH. , #14651 ) ;
#15209=( BOUNDED_SURFACE ( )  B_SPLINE_SURFACE ( 3, 2, ( 
 ( #45186, #14363, #80170 ),
 ( #5760, #62424, #104451 ),
 ( #96388, #87227, #71029 ),
 ( #46233, #21449, #87759 ),
 ( #53263, #13310, #78061 ),
 ( #46754, #29040, #30068 ) ),
 .UNSPECIFIED., .F., .F., .F. ) 
 B_SPLINE_SURFACE_WITH_KNOTS ( ( 4, 2, 4 ),
 ( 3, 3 ),
 ( -8.868773770931426270E-17, 0.001801542390204190734, 0.003603084780408470373 ),
 ( 0.000000000000000000, 1.000000000000000000 ),
 .UNSPECIFIED. ) 
 GEOMETRIC_REPRESENTATION_ITEM ( )  RATIONAL_B_SPLINE_SURFACE ( (
 ( 1.000000000000000000, 0.9115707425106689410, 1.000000000000000000),
 ( 1.000000000000000000, 0.9032011672212912901, 1.000000000000000000),
 ( 1.000000000000000000, 0.8933560653589430745, 1.000000000000000000),
 ( 1.000000000000000000, 0.8671388017652420510, 1.000000000000000000),
 ( 1.000000000000000000, 0.8506934603551941088, 1.000000000000000000),
 ( 1.000000000000000000, 0.8291561975888570579, 1.000000000000000000) ) ) 
 REPRESENTATION_ITEM ( '' )  SURFACE ( )  );
#15210=CARTESIAN_POINT ( 'NONE',  ( -11.50426943841285876, 15.12044061251818938, 9.781685010125752200 ) ) ;
#15211=CARTESIAN_POINT ( 'NONE',  ( -15.00099999999999767, 12.99999999999999289, 0.000000000000000000 ) ) ;
#15248=CARTESIAN_POINT ( 'NONE',  ( -15.91318055706418200, 3.411564560433507420, -2.528039842340506382 ) ) ;
#15321=CARTESIAN_POINT ( 'NONE',  ( 10.56215772281497323, 17.85407101821802556, -9.582426342768091132 ) ) ;
#15395=CARTESIAN_POINT ( 'NONE',  ( -6.705175466950450414, 9.539476085123771654, 2.022930269817423188 ) ) ;
#15426=CARTESIAN_POINT ( 'NONE',  ( 13.07948690922876089, 8.363364708107999590, 8.866367791206201332 ) ) ;
#15486=COLOUR_RGB ( '', 0.72549020, 0.75294118, 0.79215686) ;
#15489=ORIENTED_EDGE ( 'NONE', *, *, #37600, .F. ) ;
#15495=FILL_AREA_STYLE_COLOUR ( '', #15486 ) ;
#15502=ORIENTED_EDGE ( 'NONE', *, *, #19619, .T. ) ;
#15511=CARTESIAN_POINT ( 'NONE',  ( 11.44979815925891842, 7.555154868943327884, 9.462210209118575577 ) ) ;
#15512=DIRECTION ( 'NONE',  ( 0.000000000000000000, -1.000000000000000000, 0.000000000000000000 ) ) ;
#15514=CARTESIAN_POINT ( 'NONE',  ( -14.29190075645675861, 21.26710225494873185, 5.626279437267716510 ) ) ;
#15534=VERTEX_POINT ( 'NONE', #46490 ) ;
#15546=CARTESIAN_POINT ( 'NONE',  ( -12.55742542063729417, 5.178327859976680436, 8.085065843704475341 ) ) ;
#15628=CARTESIAN_POINT ( 'NONE',  ( 12.69532080757137926, 18.64199302928275159, -8.260889120040829425 ) ) ;
#15647=CARTESIAN_POINT ( 'NONE',  ( -14.29190075645675861, 21.26710225494873185, 5.626279437267716510 ) ) ;
#15668=SURFACE_SIDE_STYLE ('',( #48025 ) ) ;
#15672=FILL_AREA_STYLE ('',( #80400 ) ) ;
#15674=CARTESIAN_POINT ( 'NONE',  ( -10.03715289824008750, 13.99183644020731343, -10.50945001292772929 ) ) ;
#15694=CARTESIAN_POINT ( 'NONE',  ( 16.14595037822608603, 7.274337365584590209, -6.616591826375515240 ) ) ;
#15703=CARTESIAN_POINT ( 'NONE',  ( -15.47206823513576524, 2.694788529767829122, 1.611870258443510728 ) ) ;
#15717=CARTESIAN_POINT ( 'NONE',  ( -14.29190075645222180, 6.456385560667815326, -7.561819230143193238 ) ) ;
#15736=ORIENTED_EDGE ( 'NONE', *, *, #98301, .T. ) ;
#15779=CARTESIAN_POINT ( 'NONE',  ( -15.91668924485766112, 3.370617522767656027, 2.350968163848803361 ) ) ;
#15852=CARTESIAN_POINT ( 'NONE',  ( 11.09125750223364548, 19.52129652750905109, -8.745713487163543576 ) ) ;
#15999=EDGE_CURVE ( 'NONE', #72252, #74862, #49498, .T. ) ;
#16072=FILL_AREA_STYLE ('',( #98578 ) ) ;
#16160=CARTESIAN_POINT ( 'NONE',  ( 12.04303557248932677, 10.55999509045389928, -9.701624603060800212 ) ) ;
#16207=CARTESIAN_POINT ( 'NONE',  ( -10.10574779088694441, 15.34502448090799653, -10.31986842472087673 ) ) ;
#16222=( NAMED_UNIT ( * ) SI_UNIT ( $, .STERADIAN. ) SOLID_ANGLE_UNIT ( ) );
#16272=CIRCLE ( 'NONE', #61097, 2.000000000000000000 ) ;
#16290=CARTESIAN_POINT ( 'NONE',  ( -10.17232223684046311, 15.97894553443599719, 10.19325617881414914 ) ) ;
#16303=VERTEX_POINT ( 'NONE', #11934 ) ;
#16305=CARTESIAN_POINT ( 'NONE',  ( -15.93923796801708015, 3.103382665673234619, 0.7338764875060157511 ) ) ;
#16369=CARTESIAN_POINT ( 'NONE',  ( 16.01236936003240885, 3.722446712626720888, -0.6596918664728864679 ) ) ;
#16378=CARTESIAN_POINT ( 'NONE',  ( 14.11595029532510104, 2.410436752314617959, -5.024000119269091513 ) ) ;
#16549=CARTESIAN_POINT ( 'NONE',  ( 16.10373777989397226, 21.82388053252877569, 0.8730104595026707548 ) ) ;
#16570=CIRCLE ( 'NONE', #76844, 2.000000000000000000 ) ;
#16698=( LENGTH_UNIT ( ) NAMED_UNIT ( * ) SI_UNIT ( .MILLI., .METRE. ) );
#16700=CARTESIAN_POINT ( 'NONE',  ( 15.42500621734827781, 22.80173751655717496, -2.001677017651171564 ) ) ;
#16744=CARTESIAN_POINT ( 'NONE',  ( -12.93345011515627796, 23.56910474203129269, 4.607970287769207474 ) ) ;
#16757=CARTESIAN_POINT ( 'NONE',  ( 11.50456601593190342, 15.12187630717486009, -9.781292348127028191 ) ) ;
#16759=( GEOMETRIC_REPRESENTATION_CONTEXT ( 3 ) GLOBAL_UNCERTAINTY_ASSIGNED_CONTEXT ( ( #36501 ) ) GLOBAL_UNIT_ASSIGNED_CONTEXT ( ( #82971, #409, #58154 ) ) REPRESENTATION_CONTEXT ( 'NONE', 'WORKASPACE' ) );
#16778=AXIS2_PLACEMENT_3D ( 'NONE', #102680, #28841, #66460 ) ;
#16818=CARTESIAN_POINT ( 'NONE',  ( -11.41770977658351427, 13.86023221547256412, 9.965253901235293199 ) ) ;
#16932=CARTESIAN_POINT ( 'NONE',  ( 13.39830318362800909, 24.42447744924177400, -2.536416954090644271 ) ) ;
#17040=CARTESIAN_POINT ( 'NONE',  ( 14.15481990207392649, 21.07020540569414635, 5.915594321928214327 ) ) ;
#17051=B_SPLINE_CURVE_WITH_KNOTS ( 'NONE', 3,
 ( #33501, #42634, #2702, #100337, #66376, #43177 ),
 .UNSPECIFIED., .F., .F.,
 ( 4, 2, 4 ),
 ( 0.000000000000000000, 0.001916782365093508281, 0.003833564730187016562 ),
 .UNSPECIFIED. ) ;
#17088=FACE_OUTER_BOUND ( 'NONE', #78016, .T. ) ;
#17130=FILL_AREA_STYLE ('',( #91025 ) ) ;
#17138=ORIENTED_EDGE ( 'NONE', *, *, #82945, .F. ) ;
#17176=CARTESIAN_POINT ( 'NONE',  ( 6.770548583014334376, 9.415629875647791636, 1.794845940801068851 ) ) ;
#17205=EDGE_CURVE ( 'NONE', #98241, #82573, #64344, .T. ) ;
#17218=ADVANCED_FACE ( 'NONE', ( #76415, #99087 ), #67809, .T. ) ;
#17250=SURFACE_STYLE_FILL_AREA ( #26432 ) ;
#17252=CARTESIAN_POINT ( 'NONE',  ( 12.87288491891443165, 21.40780029432582765, -5.438759071948315871 ) ) ;
#17264=MECHANICAL_DESIGN_GEOMETRIC_PRESENTATION_REPRESENTATION('',(#5174),#8614);
#17275=ORIENTED_EDGE ( 'NONE', *, *, #76613, .F. ) ;
#17290=TOROIDAL_SURFACE ( 'NONE', #27640, 8.000000000000000000, 1.000000000000000000 ) ;
#17295=CARTESIAN_POINT ( 'NONE',  ( -13.68089852145233820, 22.80932735910137055, 2.024255124915971482 ) ) ;
#17322=CARTESIAN_POINT ( 'NONE',  ( -15.19395690307318425, 3.423339800917871933, 3.910915912819011186 ) ) ;
#17371=( GEOMETRIC_REPRESENTATION_CONTEXT ( 3 ) GLOBAL_UNCERTAINTY_ASSIGNED_CONTEXT ( ( #75846 ) ) GLOBAL_UNIT_ASSIGNED_CONTEXT ( ( #26225, #33760, #93039 ) ) REPRESENTATION_CONTEXT ( 'NONE', 'WORKASPACE' ) );
#17459=CARTESIAN_POINT ( 'NONE',  ( 16.02741078272304875, 4.186345391437675367, 2.546409592411958744 ) ) ;
#17482=FACE_OUTER_BOUND ( 'NONE', #93522, .T. ) ;
#17545=VERTEX_POINT ( 'NONE', #74684 ) ;
#17672=COLOUR_RGB ( '', 0.40784314, 0.44705882, 0.49803922) ;
#17714=CARTESIAN_POINT ( 'NONE',  ( 16.04721880643842979, 4.604982429971628655, 3.436919038180027641 ) ) ;
#17718=CARTESIAN_POINT ( 'NONE',  ( 15.30754850745360862, 3.114812942699181075, -3.172027124395669695 ) ) ;
#17762=VECTOR ( 'NONE', #24564, 1000.000000000000000 ) ;
#17771=STYLED_ITEM ( 'NONE', ( #12598 ), #95272 ) ;
#17779=CARTESIAN_POINT ( 'NONE',  ( 15.57921808388646312, 22.99888987748559899, -0.5943451063223359476 ) ) ;
#17820=( NAMED_UNIT ( * ) SI_UNIT ( $, .STERADIAN. ) SOLID_ANGLE_UNIT ( ) );
#17823=CARTESIAN_POINT ( 'NONE',  ( -12.69070879414525699, 23.10505005157635949, -5.367139868969495353 ) ) ;
#17911=CARTESIAN_POINT ( 'NONE',  ( -13.92465259748497530, 2.727993544930908509, 5.548800750351575495 ) ) ;
#17964=CARTESIAN_POINT ( 'NONE',  ( -20.00000000000000000, 12.99999999999999289, 0.000000000000000000 ) ) ;
#17986=CARTESIAN_POINT ( 'NONE',  ( 16.01290373797198541, 3.743961321039747769, 0.6473776101028398955 ) ) ;
#18011=FILL_AREA_STYLE ('',( #75152 ) ) ;
#18051=CARTESIAN_POINT ( 'NONE',  ( -20.00000000000000000, 12.99999999999999289, -7.500000000000000000 ) ) ;
#18104=CARTESIAN_POINT ( 'NONE',  ( -15.22818746202957207, 3.929489829918556332, -4.609438620807924103 ) ) ;
#18125=FILL_AREA_STYLE ('',( #100077 ) ) ;
#18131=ADVANCED_FACE ( 'NONE', ( #7970 ), #40364, .T. ) ;
#18184=( NAMED_UNIT ( * ) PLANE_ANGLE_UNIT ( ) SI_UNIT ( $, .RADIAN. ) );
#18205=VERTEX_POINT ( 'NONE', #64123 ) ;
#18211=B_SPLINE_CURVE_WITH_KNOTS ( 'NONE', 3,
 ( #33380, #8008, #945, #17718, #99684, #26904, #41447, #82975, #50067, #50579, #66255, #74858, #8542, #9595, #34987, #83496 ),
 .UNSPECIFIED., .F., .F.,
 ( 4, 2, 2, 2, 2, 2, 2, 4 ),
 ( 2.909219710836648185E-18, 0.001212534658634416241, 0.002425069317268828580, 0.004850138634537652822, 0.006062673293172064944, 0.007275207951806477932, 0.008487742610440890054, 0.009700277269075302175 ),
 .UNSPECIFIED. ) ;
#18219=CARTESIAN_POINT ( 'NONE',  ( 19.50000000000000000, 12.99999999999999289, 0.000000000000000000 ) ) ;
#18246=CARTESIAN_POINT ( 'NONE',  ( 5.919343243681500333, 11.56755076042193764, 3.736960138817876143 ) ) ;
#18253=CIRCLE ( 'NONE', #26826, 7.500000000000000000 ) ;
#18258=SURFACE_STYLE_FILL_AREA ( #36591 ) ;
#18319=PRESENTATION_STYLE_ASSIGNMENT (( #67388 ) ) ;
#18321=CARTESIAN_POINT ( 'NONE',  ( 15.27839008720943781, 22.61312091684385095, 2.812667176176046446 ) ) ;
#18364=CARTESIAN_POINT ( 'NONE',  ( -13.08051135748678107, 23.84419156307226118, 4.072937932820233087 ) ) ;
#18398=VERTEX_POINT ( 'NONE', #93161 ) ;
#18440=( NAMED_UNIT ( * ) PLANE_ANGLE_UNIT ( ) SI_UNIT ( $, .RADIAN. ) );
#18488=COLOUR_RGB ( '', 0.72549020, 0.75294118, 0.79215686) ;
#18543=ORIENTED_EDGE ( 'NONE', *, *, #71778, .F. ) ;
#18648=CARTESIAN_POINT ( 'NONE',  ( -14.27029591641818662, 3.391655494167292950, -4.551126452497153529 ) ) ;
#18735=FILL_AREA_STYLE ('',( #3042 ) ) ;
#18756=CARTESIAN_POINT ( 'NONE',  ( 14.46174234134069359, 2.926873011494404597, 3.961839331259466856 ) ) ;
#18810=FACE_OUTER_BOUND ( 'NONE', #60437, .T. ) ;
#18864=EDGE_LOOP ( 'NONE', ( #2040, #102228, #106497, #2757 ) ) ;
#18870=CARTESIAN_POINT ( 'NONE',  ( 13.42061381376756835, 24.46452927392946464, -2.387491988728646763 ) ) ;
#18911=DIRECTION ( 'NONE',  ( 0.000000000000000000, 0.000000000000000000, 1.000000000000000000 ) ) ;
#18913=CARTESIAN_POINT ( 'NONE',  ( -11.82957429177135289, 21.33083118278957713, -7.415650228056600568 ) ) ;
#18998=CARTESIAN_POINT ( 'NONE',  ( -16.11142072793864699, 21.68022463236556163, 1.737955725777517779 ) ) ;
#19037=CARTESIAN_POINT ( 'NONE',  ( 1.429841143546225365E-15, 35.00000000000000000, 11.18527996897366528 ) ) ;
#19077=AXIS2_PLACEMENT_3D ( 'NONE', #68736, #50385, #10990 ) ;
#19093=ORIENTED_EDGE ( 'NONE', *, *, #44441, .T. ) ;
#19107=( NAMED_UNIT ( * ) PLANE_ANGLE_UNIT ( ) SI_UNIT ( $, .RADIAN. ) );
#19115=CARTESIAN_POINT ( 'NONE',  ( 15.05785784214676326, 3.824195276769950969, 4.604276673498415740 ) ) ;
#19128=COLOUR_RGB ( '', 0.09019608, 0.27058824, 0.51372549) ;
#19141=VERTEX_POINT ( 'NONE', #28636 ) ;
#19151=SURFACE_SIDE_STYLE ('',( #745 ) ) ;
#19201=CARTESIAN_POINT ( 'NONE',  ( -14.97109678640281594, 2.057467188490503585, 0.8486206380284277984 ) ) ;
#19222=FILL_AREA_STYLE_COLOUR ( '', #56011 ) ;
#19225=CARTESIAN_POINT ( 'NONE',  ( 24.33159596665262470, 34.19642918197134662, 12.16579798332630880 ) ) ;
#19261=AXIS2_PLACEMENT_3D ( 'NONE', #85661, #4731, #85113 ) ;
#19269=UNCERTAINTY_MEASURE_WITH_UNIT (LENGTH_MEASURE( 1.000000000000000082E-05 ), #67332, 'distance_accuracy_value', 'NONE');
#19276=CARTESIAN_POINT ( 'NONE',  ( -14.95236164054199257, 4.204970931333630091, 5.179833178273279159 ) ) ;
#19306=FACE_BOUND ( 'NONE', #71634, .T. ) ;
#19312=CARTESIAN_POINT ( 'NONE',  ( 14.89969599197393002, 1.346844969883137511, 1.740400043388351081 ) ) ;
#19347=SURFACE_STYLE_USAGE ( .BOTH. , #93181 ) ;
#19350=EDGE_CURVE ( 'NONE', #92807, #39874, #38174, .T. ) ;
#19358=SURFACE_SIDE_STYLE ('',( #18258 ) ) ;
#19373=DIRECTION ( 'NONE',  ( 1.224646799147351482E-16, 0.000000000000000000, -1.000000000000000000 ) ) ;
#19401=EDGE_CURVE ( 'NONE', #51545, #40845, #59822, .T. ) ;
#19407=( GEOMETRIC_REPRESENTATION_CONTEXT ( 3 ) GLOBAL_UNCERTAINTY_ASSIGNED_CONTEXT ( ( #59158 ) ) GLOBAL_UNIT_ASSIGNED_CONTEXT ( ( #69373, #77456, #4100 ) ) REPRESENTATION_CONTEXT ( 'NONE', 'WORKASPACE' ) );
#19413=CARTESIAN_POINT ( 'NONE',  ( 13.04450623576480872, 19.29496049036926308, 7.774814228663267102 ) ) ;
#19454=CARTESIAN_POINT ( 'NONE',  ( -14.51986452503335734, 21.59086984591841940, 5.125738280916170453 ) ) ;
#19512=DIRECTION ( 'NONE',  ( 1.000000000000000000, 0.000000000000000000, 0.000000000000000000 ) ) ;
#19528=( NAMED_UNIT ( * ) SI_UNIT ( $, .STERADIAN. ) SOLID_ANGLE_UNIT ( ) );
#19531=CARTESIAN_POINT ( 'NONE',  ( -5.763785242774021711, 13.53591622817248563, 3.972758706198395551 ) ) ;
#19536=CARTESIAN_POINT ( 'NONE',  ( 11.55846695675572455, 7.296715529366291975, -9.344306654786388222 ) ) ;
#19545=AXIS2_PLACEMENT_3D ( 'NONE', #5378, #69060, #79252 ) ;
#19587=CARTESIAN_POINT ( 'NONE',  ( -13.02995514262170396, 6.128988252786461643, -7.304746880288981892 ) ) ;
#19608=CYLINDRICAL_SURFACE ( 'NONE', #60018, 10.00000000000000178 ) ;
#19619=EDGE_CURVE ( 'NONE', #27686, #5290, #94985, .T. ) ;
#19623=FILL_AREA_STYLE_COLOUR ( '', #51310 ) ;
#19682=CARTESIAN_POINT ( 'NONE',  ( 16.10370002540634360, 21.82456013744149814, 0.8668566225193951036 ) ) ;
#19697=ORIENTED_EDGE ( 'NONE', *, *, #24682, .T. ) ;
#19758=FILL_AREA_STYLE_COLOUR ( '', #4836 ) ;
#19808=ORIENTED_EDGE ( 'NONE', *, *, #89592, .T. ) ;
#19916=TOROIDAL_SURFACE ( 'NONE', #9444, 13.99700487351915612, 1.000000000000000000 ) ;
#19942=EDGE_LOOP ( 'NONE', ( #7513, #84045, #55652, #83560, #56139, #98132 ) ) ;
#19945=CARTESIAN_POINT ( 'NONE',  ( 12.87241103463997050, 21.40694261541543497, 5.440169305117485976 ) ) ;
#19982=CARTESIAN_POINT ( 'NONE',  ( -10.93523035535289978, 16.60435489604227044, 9.334902641144335433 ) ) ;
#20022=VERTEX_POINT ( 'NONE', #81001 ) ;
#20069=CARTESIAN_POINT ( 'NONE',  ( 12.54481040020086802, 5.202751164716101329, -8.103389815076774028 ) ) ;
#20114=CARTESIAN_POINT ( 'NONE',  ( -12.80252612773492693, 6.537496074479076213, -7.668719352993321969 ) ) ;
#20217=CARTESIAN_POINT ( 'NONE',  ( 15.66336674558382569, 21.48481246047165172, -5.205033774743918151 ) ) ;
#20251=MECHANICAL_DESIGN_GEOMETRIC_PRESENTATION_REPRESENTATION('',(#66702),#56358);
#20272=CARTESIAN_POINT ( 'NONE',  ( -19.50000000000000000, 12.99999999999999467, 7.500000000000000000 ) ) ;
#20331=UNCERTAINTY_MEASURE_WITH_UNIT (LENGTH_MEASURE( 1.000000000000000082E-05 ), #54050, 'distance_accuracy_value', 'NONE');
#20344=CARTESIAN_POINT ( 'NONE',  ( -11.77939662183895386, 6.782627062745584468, -9.100507241011085213 ) ) ;
#20376=CARTESIAN_POINT ( 'NONE',  ( -6.705020855549795655, 9.539818418972618730, -2.023228926981749609 ) ) ;
#20387=CIRCLE ( 'NONE', #80586, 13.99700487351915612 ) ;
#20400=CARTESIAN_POINT ( 'NONE',  ( 11.66726770654783252, 11.72242249675092474, -9.937599956974251469 ) ) ;
#20410=PRESENTATION_STYLE_ASSIGNMENT (( #69963 ) ) ;
#20438=EDGE_LOOP ( 'NONE', ( #101159, #29953, #74118, #106170 ) ) ;
#20440=CARTESIAN_POINT ( 'NONE',  ( -18.00000000000000355, 12.99999999999999289, 9.500000000000000000 ) ) ;
#20488=ORIENTED_EDGE ( 'NONE', *, *, #82996, .T. ) ;
#20491=CARTESIAN_POINT ( 'NONE',  ( 12.69346561929714490, 18.63831398217661928, 8.263378152524056830 ) ) ;
#20499=ADVANCED_FACE ( 'NONE', ( #12700 ), #92719, .T. ) ;
#20531=CARTESIAN_POINT ( 'NONE',  ( -12.68594940236797797, 18.62354890192223422, 8.273500667382888807 ) ) ;
#20545=( NAMED_UNIT ( * ) PLANE_ANGLE_UNIT ( ) SI_UNIT ( $, .RADIAN. ) );
#20578=AXIS2_PLACEMENT_3D ( 'NONE', #40598, #23928, #58378 ) ;
#20614=CARTESIAN_POINT ( 'NONE',  ( -16.10535093526667438, 21.79478144880857826, 1.090471457014209777 ) ) ;
#20663=AXIS2_PLACEMENT_3D ( 'NONE', #55428, #52716, #92114 ) ;
#20736=VECTOR ( 'NONE', #35147, 1000.000000000000000 ) ;
#20743=EDGE_LOOP ( 'NONE', ( #9197, #72086 ) ) ;
#20749=CARTESIAN_POINT ( 'NONE',  ( -11.89526586238883432, 16.74536500488340351, -9.279214822536506091 ) ) ;
#20756=CARTESIAN_POINT ( 'NONE',  ( 14.60001457338170461, 22.21450448812595013, 3.985393713008906325 ) ) ;
#20807=CARTESIAN_POINT ( 'NONE',  ( -14.45674127754199390, 21.77180424838195094, -4.838420908141329413 ) ) ;
#20817=DIRECTION ( 'NONE',  ( -1.224646799147351482E-16, 0.000000000000000000, -1.000000000000000000 ) ) ;
#20870=SURFACE_SIDE_STYLE ('',( #69897 ) ) ;
#20902=CARTESIAN_POINT ( 'NONE',  ( 0.000000000000000000, -3.035766082959412415E-15, 0.000000000000000000 ) ) ;
#20904=CARTESIAN_POINT ( 'NONE',  ( -5.887945094627411002, 11.68790215641263686, -3.787642776067695394 ) ) ;
#20929=CARTESIAN_POINT ( 'NONE',  ( 14.29190075645216851, 6.456385560668102208, -7.561819230143448145 ) ) ;
#20946=TOROIDAL_SURFACE ( 'NONE', #51832, 6.999999999999999112, 0.5000000000000000000 ) ;
#20953=CARTESIAN_POINT ( 'NONE',  ( 16.01293590580093351, 3.745177866445061010, -0.6593600975748525883 ) ) ;
#21005=CARTESIAN_POINT ( 'NONE',  ( 13.75548730145301057, 20.47407606505949218, 6.665969588725104700 ) ) ;
#21046=CARTESIAN_POINT ( 'NONE',  ( -11.77389790720900464, 19.14645581668979446, 7.901544587056179125 ) ) ;
#21056=CARTESIAN_POINT ( 'NONE',  ( -14.29190075644809887, 19.61368180395988148, 4.501023549812855684 ) ) ;
#21103=B_SPLINE_CURVE_WITH_KNOTS ( 'NONE', 3,
 ( #51837, #84751, #19531, #10832, #43752, #105176, #23219, #21636, #104637, #46929, #5424, #37830, #70161, #5933, #63674, #38348, #80886, #30790, #87941, #79303, #70693, #95492, #62093, #86890, #31322, #103583, #96563, #94986, #22697, #38860, #14022, #22158, #55534, #103065, #71208, #62606 ),
 .UNSPECIFIED., .F., .F.,
 ( 4, 2, 2, 2, 2, 2, 2, 2, 2, 2, 2, 2, 2, 2, 2, 2, 2, 4 ),
 ( 0.000000000000000000, 0.0007996222028895878841, 0.001599244405779175768, 0.003198488811558350669, 0.003998111014447940613, 0.004797733217337530123, 0.005597355420227121368, 0.006396977623116711746, 0.006796788724561506935, 0.007196599826006302991, 0.007996222028895893369, 0.008795844231785483747, 0.009595466434675074124, 0.01039508863756465756, 0.01119471084045424274, 0.01159452194189903619, 0.01199433304334382965, 0.01279395524623341482 ),
 .UNSPECIFIED. ) ;
#21174=CARTESIAN_POINT ( 'NONE',  ( -15.78841396623141513, 4.459144360354060588, -5.230423732636918288 ) ) ;
#21222=ORIENTED_EDGE ( 'NONE', *, *, #79354, .T. ) ;
#21232=AXIS2_PLACEMENT_3D ( 'NONE', #86046, #43442, #61227 ) ;
#21254=CARTESIAN_POINT ( 'NONE',  ( 0.000000000000000000, 1.005902684993156715, -14.99698745252234566 ) ) ;
#21267=CARTESIAN_POINT ( 'NONE',  ( 14.37785056366748826, 21.52979621147868272, 5.240284069529759670 ) ) ;
#21276=CARTESIAN_POINT ( 'NONE',  ( 14.11595029532508505, 2.410436752314643716, 5.024000119269132369 ) ) ;
#21312=CARTESIAN_POINT ( 'NONE',  ( -16.10528882106922310, 21.79591095385115906, 1.082486061764422081 ) ) ;
#21324=DIRECTION ( 'NONE',  ( 2.855347482703417278E-17, -0.7561819230137100112, -0.6543614439339221489 ) ) ;
#21334=CARTESIAN_POINT ( 'NONE',  ( 13.39322541715468162, 24.41533748129609549, 2.568124331425434725 ) ) ;
#21372=CARTESIAN_POINT ( 'NONE',  ( -16.10173312979620164, 5.477053992178055886, 4.739458514423359858 ) ) ;
#21376=CARTESIAN_POINT ( 'NONE',  ( -13.02156499116019894, 23.73570805843572273, -4.328872242394949943 ) ) ;
#21449=CARTESIAN_POINT ( 'NONE',  ( 15.72218280906591303, 5.595371698622046530, -6.516822309424127546 ) ) ;
#21513=CARTESIAN_POINT ( 'NONE',  ( 11.46758739460970133, 14.79966376039287823, 9.840969504964308001 ) ) ;
#21555=CARTESIAN_POINT ( 'NONE',  ( -12.52826048495583144, 20.76158922763902126, 6.344216544754339715 ) ) ;
#21568=EDGE_CURVE ( 'NONE', #49969, #12309, #45390, .T. ) ;
#21618=VERTEX_POINT ( 'NONE', #15514 ) ;
#21636=CARTESIAN_POINT ( 'NONE',  ( -6.481088301903609405, 16.00512455538761358, 2.652222390170979160 ) ) ;
#21640=SURFACE_STYLE_FILL_AREA ( #46421 ) ;
#21676=VERTEX_POINT ( 'NONE', #69789 ) ;
#21691=CARTESIAN_POINT ( 'NONE',  ( -13.03515395759786877, 4.280348557850227387, -7.334716606105208925 ) ) ;
#21740=CARTESIAN_POINT ( 'NONE',  ( 14.11595029532508860, 2.410436752314647713, 5.024000119269133258 ) ) ;
#21743=DIRECTION ( 'NONE',  ( 0.000000000000000000, 0.000000000000000000, -1.000000000000000000 ) ) ;
#21782=CARTESIAN_POINT ( 'NONE',  ( -12.67403057162867341, 18.60284021993737724, -8.290260067447448478 ) ) ;
#21790=CARTESIAN_POINT ( 'NONE',  ( 14.77017712487585932, 22.74518112339139364, -2.603937284864370039 ) ) ;
#21794=SURFACE_STYLE_FILL_AREA ( #44998 ) ;
#21861=CARTESIAN_POINT ( 'NONE',  ( 12.85196282309222227, 23.41805309023355974, 4.899702151067347522 ) ) ;
#21905=CARTESIAN_POINT ( 'NONE',  ( -13.40082383129016819, 24.42921809578557202, 2.579497271388879298 ) ) ;
#21926=TOROIDAL_SURFACE ( 'NONE', #104566, 9.500000000000000000, 2.000000000000000000 ) ;
#21931=MECHANICAL_DESIGN_GEOMETRIC_PRESENTATION_REPRESENTATION('',(#77011),#28963);
#21933=CARTESIAN_POINT ( 'NONE',  ( -7.000182694785904047, 8.999680283969629713, 0.2646331733798830133 ) ) ;
#21979=CARTESIAN_POINT ( 'NONE',  ( 15.43758579535049691, 2.782614627089976533, -1.951547078872143626 ) ) ;
#21988=MECHANICAL_DESIGN_GEOMETRIC_PRESENTATION_REPRESENTATION('',(#32302),#42590);
#21994=EDGE_CURVE ( 'NONE', #43519, #19141, #793, .T. ) ;
#22033=CARTESIAN_POINT ( 'NONE',  ( -16.04706041842033315, 4.602438919581462784, -3.432847546122274274 ) ) ;
#22037=CARTESIAN_POINT ( 'NONE',  ( 14.11595029532509216, 2.410436752314641051, 5.024000119269121711 ) ) ;
#22073=EDGE_CURVE ( 'NONE', #16303, #87833, #40215, .T. ) ;
#22081=CARTESIAN_POINT ( 'NONE',  ( -13.40447963469854820, 7.804086714771164779, 8.560322119383409145 ) ) ;
#22100=AXIS2_PLACEMENT_3D ( 'NONE', #30182, #54410, #53900 ) ;
#22107=CIRCLE ( 'NONE', #11755, 8.750000000000023093 ) ;
#22158=CARTESIAN_POINT ( 'NONE',  ( -5.839745530781596194, 14.05731516213037402, -3.859993546116442076 ) ) ;
#22164=CARTESIAN_POINT ( 'NONE',  ( 11.40901652478997796, 14.23906480821464449, -9.939951793343480446 ) ) ;
#22184=CARTESIAN_POINT ( 'NONE',  ( -14.62404193421258647, 22.28898781335485779, 3.917683339309744994 ) ) ;
#22205=FILL_AREA_STYLE_COLOUR ( '', #40498 ) ;
#22214=CARTESIAN_POINT ( 'NONE',  ( -11.79855021826020511, 16.42585737932439471, -9.399101548535638173 ) ) ;
#22222=ORIENTED_EDGE ( 'NONE', *, *, #79354, .F. ) ;
#22310=DIRECTION ( 'NONE',  ( -0.000000000000000000, -1.000000000000000000, -0.000000000000000000 ) ) ;
#22318=CARTESIAN_POINT ( 'NONE',  ( -15.38120149534759484, 2.925591750584245698, 2.537117285879322726 ) ) ;
#22329=ORIENTED_EDGE ( 'NONE', *, *, #3451, .T. ) ;
#22375=CARTESIAN_POINT ( 'NONE',  ( -16.13463197906294155, 21.11076038462449844, 3.387067249032789551 ) ) ;
#22418=EDGE_CURVE ( 'NONE', #17545, #43945, #52500, .T. ) ;
#22441=CARTESIAN_POINT ( 'NONE',  ( -10.27837503968532396, 16.60654002188488221, 10.02334268984631827 ) ) ;
#22446=AXIS2_PLACEMENT_3D ( 'NONE', #105031, #58054, #8445 ) ;
#22469=CARTESIAN_POINT ( 'NONE',  ( 16.05785784214672773, 4.775831776474238843, 3.710403933782425057 ) ) ;
#22520=CARTESIAN_POINT ( 'NONE',  ( 15.51015326906917124, 2.604283801340223192, 0.3849796309686537299 ) ) ;
#22523=ORIENTED_EDGE ( 'NONE', *, *, #55341, .T. ) ;
#22569=SURFACE_SIDE_STYLE ('',( #57005 ) ) ;
#22585=CARTESIAN_POINT ( 'NONE',  ( 11.10339240064335975, 8.425011028989088047, 9.820949472247303191 ) ) ;
#22591=CYLINDRICAL_SURFACE ( 'NONE', #20663, 4.000000000000000000 ) ;
#22629=CARTESIAN_POINT ( 'NONE',  ( -14.11595029531626011, 2.410436752329291110, 5.024000119293333455 ) ) ;
#22697=CARTESIAN_POINT ( 'NONE',  ( -6.012758288945200924, 14.79064451834496552, -3.586184577130258067 ) ) ;
#22702=CARTESIAN_POINT ( 'NONE',  ( 11.09396121529365509, 10.59760035510856468, -9.714813416437120708 ) ) ;
#22721=CARTESIAN_POINT ( 'NONE',  ( -14.77980331624359955, 22.77528010646188505, -2.502200611405557051 ) ) ;
#22722=DIRECTION ( 'NONE',  ( -0.000000000000000000, -1.000000000000000000, -0.000000000000000000 ) ) ;
#22747=CARTESIAN_POINT ( 'NONE',  ( 0.000000000000000000, 0.9999999999999970024, 0.000000000000000000 ) ) ;
#22748=CARTESIAN_POINT ( 'NONE',  ( -12.60033841120074527, 9.255502400745754699, -9.287856882556875249 ) ) ;
#22833=FACE_BOUND ( 'NONE', #5958, .T. ) ;
#22839=AXIS2_PLACEMENT_3D ( 'NONE', #64760, #80395, #89036 ) ;
#22850=STYLED_ITEM ( 'NONE', ( #61826 ), #20499 ) ;
#22918=CARTESIAN_POINT ( 'NONE',  ( 13.01482060791784967, 23.72313099889873556, 4.353235333136677987 ) ) ;
#22930=CARTESIAN_POINT ( 'NONE',  ( -12.28357616224760918, 9.933929378342256200, 9.536270961999530726 ) ) ;
#23041=CARTESIAN_POINT ( 'NONE',  ( 1.836601268058450879E-15, 1.005902684993156715, 14.99698745252234566 ) ) ;
#23102=CARTESIAN_POINT ( 'NONE',  ( 13.27968648137678542, 3.841854981409799752, 6.905317930445485253 ) ) ;
#23114=STYLED_ITEM ( 'NONE', ( #42260 ), #61288 ) ;
#23142=CARTESIAN_POINT ( 'NONE',  ( -14.65137838515496860, 5.949403477195277290, 7.096397616382773776 ) ) ;
#23219=CARTESIAN_POINT ( 'NONE',  ( -6.242019780568027976, 15.46330733086430875, 3.192545347364962094 ) ) ;
#23223=CARTESIAN_POINT ( 'NONE',  ( 11.45439866395856221, 9.461585312351356691, -9.377169115924592901 ) ) ;
#23266=CARTESIAN_POINT ( 'NONE',  ( -11.42336277867628880, 14.22106288968689469, -9.929318634850201164 ) ) ;
#23270=DIRECTION ( 'NONE',  ( -1.000000000000000000, 0.000000000000000000, 0.000000000000000000 ) ) ;
#23282=CARTESIAN_POINT ( 'NONE',  ( -14.71845092680128353, 2.464670597987486111, 2.845879451984156372 ) ) ;
#23287=( BOUNDED_SURFACE ( )  B_SPLINE_SURFACE ( 3, 2, ( 
 ( #2630, #9121, #42031 ),
 ( #41500, #33435, #27498 ),
 ( #83548, #42558, #60373 ),
 ( #66309, #74913, #84092 ),
 ( #10192, #33978, #34519 ),
 ( #25909, #58765, #91663 ) ),
 .UNSPECIFIED., .F., .F., .T. ) 
 B_SPLINE_SURFACE_WITH_KNOTS ( ( 4, 2, 4 ),
 ( 3, 3 ),
 ( 0.000000000000000000, 0.001801542390204249932, 0.003603084780408499863 ),
 ( 0.000000000000000000, 1.000000000000000000 ),
 .UNSPECIFIED. ) 
 GEOMETRIC_REPRESENTATION_ITEM ( )  RATIONAL_B_SPLINE_SURFACE ( (
 ( 1.000000000000000000, 0.8291561975888502856, 1.000000000000000000),
 ( 1.000000000000000000, 0.8506934603555468266, 1.000000000000000000),
 ( 1.000000000000000000, 0.8671388017648747892, 1.000000000000000000),
 ( 1.000000000000000000, 0.8933560653593087819, 1.000000000000000000),
 ( 1.000000000000000000, 0.9032011672210142894, 1.000000000000000000),
 ( 1.000000000000000000, 0.9115707425106691630, 1.000000000000000000) ) ) 
 REPRESENTATION_ITEM ( '' )  SURFACE ( )  );
#23296=( BOUNDED_SURFACE ( )  B_SPLINE_SURFACE ( 3, 2, ( 
 ( #59726, #92601, #21276 ),
 ( #67804, #18756, #86538 ),
 ( #4522, #1988, #101240 ),
 ( #27393, #51063, #35471 ),
 ( #93142, #37466, #19312 ),
 ( #92068, #50530, #87055 ),
 ( #42999, #1445, #13127 ),
 ( #46053, #34408, #26856 ),
 ( #5061, #58656, #91558 ),
 ( #100686, #83442, #9545 ),
 ( #42454, #34935, #26329 ),
 ( #10090, #46572, #79467 ),
 ( #96725, #88627, #54641 ),
 ( #6636, #81047, #63306 ),
 ( #14186, #32002, #39026 ),
 ( #80517, #71370, #105340 ) ),
 .UNSPECIFIED., .F., .F., .F. ) 
 B_SPLINE_SURFACE_WITH_KNOTS ( ( 4, 2, 2, 2, 2, 2, 2, 4 ),
 ( 3, 3 ),
 ( 0.01025942932839742430, 0.01330785678258415185, 0.01483207050967751475, 0.01635628423677087939, 0.01788049796386424403, 0.01940471169095760867, 0.02092892541805096984, 0.02245313914514433448 ),
 ( 0.3005395333819582682, 1.000000000000000000 ),
 .UNSPECIFIED. ) 
 GEOMETRIC_REPRESENTATION_ITEM ( )  RATIONAL_B_SPLINE_SURFACE ( (
 ( 0.8980036390038548255, 0.8303112408401241984, 1.000000000000000000),
 ( 0.9116818979159833081, 0.8530674133113587132, 1.000000000000000000),
 ( 0.9228127777806771626, 0.8715855758629514893, 1.000000000000000000),
 ( 0.9345546761373628719, 0.8911202743842321361, 1.000000000000000000),
 ( 0.9375544117806124955, 0.8961108585005606031, 1.000000000000000000),
 ( 0.9415935919673705801, 0.9028307401435932134, 1.000000000000000000),
 ( 0.9426280110962133030, 0.9045516770153625430, 1.000000000000000000),
 ( 0.9426141662316163128, 0.9045286436652386630, 1.000000000000000000),
 ( 0.9415455155260004094, 0.9027507565873051920, 1.000000000000000000),
 ( 0.9374309181788871292, 0.8959054053271698903, 1.000000000000000000),
 ( 0.9344062863249886774, 0.8908734020165530731, 1.000000000000000000),
 ( 0.9266839229612940931, 0.8780259019276379640, 1.000000000000000000),
 ( 0.9219922915688816278, 0.8702205537599312368, 1.000000000000000000),
 ( 0.9110602365935736024, 0.8520331711346073034, 1.000000000000000000),
 ( 0.9047689875052107311, 0.8415665795724794895, 1.000000000000000000),
 ( 0.8980036390038557137, 0.8303112408401255307, 1.000000000000000000) ) ) 
 REPRESENTATION_ITEM ( '' )  SURFACE ( )  );
#23308=CARTESIAN_POINT ( 'NONE',  ( -16.13590653351237236, 6.313628335805701930, -5.716602451449800171 ) ) ;
#23371=CARTESIAN_POINT ( 'NONE',  ( -15.13200660511302864, 3.596720279098536643, -4.250825932781741479 ) ) ;
#23373=CARTESIAN_POINT ( 'NONE',  ( 16.14595037822608603, 20.23371447307436810, 4.922994507617730164 ) ) ;
#23419=VERTEX_POINT ( 'NONE', #63139 ) ;
#23451=CARTESIAN_POINT ( 'NONE',  ( 10.19089998482013648, 16.03205744524296605, -10.16805419969074009 ) ) ;
#23472=ADVANCED_FACE ( 'NONE', ( #59704 ), #9674, .T. ) ;
#23555=CARTESIAN_POINT ( 'NONE',  ( 11.44639037572927620, 14.62121991795728349, 9.874825666010542236 ) ) ;
#23556=TOROIDAL_SURFACE ( 'NONE', #6263, 7.999999999999998224, 2.000000000000000000 ) ;
#23607=CARTESIAN_POINT ( 'NONE',  ( 16.13488272710862859, 21.13099985709055062, -3.419103882760960111 ) ) ;
#23666=SURFACE_SIDE_STYLE ('',( #72193 ) ) ;
#23675=CARTESIAN_POINT ( 'NONE',  ( -13.27937243830230152, 3.845154223814204020, 6.891420024422192370 ) ) ;
#23764=CARTESIAN_POINT ( 'NONE',  ( 10.83745700209015261, 18.77853125270598156, -9.157543372961134409 ) ) ;
#23782=CARTESIAN_POINT ( 'NONE',  ( -14.78158836401471099, 22.78085926477313450, 2.483703530589361552 ) ) ;
#23799=CARTESIAN_POINT ( 'NONE',  ( 14.97540207516710176, 1.269614109201394614, 0.8865648853246460570 ) ) ;
#23811=CARTESIAN_POINT ( 'NONE',  ( -11.56629382471032663, 7.278338580405791625, -9.335672732236384164 ) ) ;
#23833=CYLINDRICAL_SURFACE ( 'NONE', #41581, 10.00000000000000178 ) ;
#23841=CARTESIAN_POINT ( 'NONE',  ( -15.12883790376237414, 3.606441264082763887, 4.265930408091180404 ) ) ;
#23877=CARTESIAN_POINT ( 'NONE',  ( -11.42862062371675691, 13.43085172858349274, 9.993030149489131375 ) ) ;
#23913=CARTESIAN_POINT ( 'NONE',  ( -15.50133110405651315, 2.625676835716459045, -0.7746791666654442299 ) ) ;
#23928=DIRECTION ( 'NONE',  ( 0.000000000000000000, 1.000000000000000000, -1.224646799147353207E-16 ) ) ;
#23974=ADVANCED_FACE ( 'NONE', ( #44447 ), #96208, .T. ) ;
#23978=B_SPLINE_CURVE_WITH_KNOTS ( 'NONE', 3,
 ( #104338, #13733, #39637, #39103, #71982, #89238, #31032, #22930, #104892, #30486, #46641, #97308 ),
 .UNSPECIFIED., .F., .F.,
 ( 4, 2, 2, 2, 2, 4 ),
 ( 0.05939584100412212408, 0.06135403683694420907, 0.06233313475335525849, 0.06331223266976629405, 0.06527042850258839291, 0.06722862433541047789 ),
 .UNSPECIFIED. ) ;
#23983=CARTESIAN_POINT ( 'NONE',  ( 16.02333492353055533, 4.076663811953147309, 2.240748598616852938 ) ) ;
#23990=CARTESIAN_POINT ( 'NONE',  ( 10.52363060357091307, 10.25739784061314630, -10.32240453393743707 ) ) ;
#23999=DIRECTION ( 'NONE',  ( -1.000000000000000000, -0.000000000000000000, -0.000000000000000000 ) ) ;
#24091=CARTESIAN_POINT ( 'NONE',  ( 11.54022871740204081, 12.38863196018314383, 9.987975719479239345 ) ) ;
#24104=SURFACE_STYLE_FILL_AREA ( #18125 ) ;
#24107=( GEOMETRIC_REPRESENTATION_CONTEXT ( 3 ) GLOBAL_UNCERTAINTY_ASSIGNED_CONTEXT ( ( #5413 ) ) GLOBAL_UNIT_ASSIGNED_CONTEXT ( ( #8374, #88778, #80664 ) ) REPRESENTATION_CONTEXT ( 'NONE', 'WORKASPACE' ) );
#24148=CARTESIAN_POINT ( 'NONE',  ( 16.11155731264993918, 21.67754735133535249, -1.749455090942883206 ) ) ;
#24177=CARTESIAN_POINT ( 'NONE',  ( 13.47222701196340466, 5.364671514323175572, 6.505800345027190623 ) ) ;
#24219=STYLED_ITEM ( 'NONE', ( #68183 ), #81053 ) ;
#24244=B_SPLINE_CURVE_WITH_KNOTS ( 'NONE', 3,
 ( #79123, #88813, #80176, #23041 ),
 .UNSPECIFIED., .F., .F.,
 ( 4, 4 ),
 ( 0.02698643027831515440, 0.9670246242088337274 ),
 .UNSPECIFIED. ) ;
#24251=EDGE_CURVE ( 'NONE', #54847, #68971, #70182, .T. ) ;
#24258=CARTESIAN_POINT ( 'NONE',  ( 20.00000000000000000, 12.99999999999999467, -7.500000000000000000 ) ) ;
#24294=CARTESIAN_POINT ( 'NONE',  ( 11.69764828795528011, 11.66347120412247662, -9.914309509057556369 ) ) ;
#24331=CARTESIAN_POINT ( 'NONE',  ( 14.24907788157470634, 2.189443139869392763, 4.658781708031014546 ) ) ;
#24342=CARTESIAN_POINT ( 'NONE',  ( -10.93723481929648678, 16.61273572670358689, -9.331603509320386181 ) ) ;
#24356=CARTESIAN_POINT ( 'NONE',  ( 11.40992495151485464, 13.86395319139118243, -9.971698466393837279 ) ) ;
#24373=( GEOMETRIC_REPRESENTATION_CONTEXT ( 3 ) GLOBAL_UNCERTAINTY_ASSIGNED_CONTEXT ( ( #69632 ) ) GLOBAL_UNIT_ASSIGNED_CONTEXT ( ( #56677, #83092, #16222 ) ) REPRESENTATION_CONTEXT ( 'NONE', 'WORKASPACE' ) );
#24396=ORIENTED_EDGE ( 'NONE', *, *, #19350, .T. ) ;
#24419=EDGE_CURVE ( 'NONE', #74862, #15534, #4701, .T. ) ;
#24433=CARTESIAN_POINT ( 'NONE',  ( -12.29126969517217205, 22.30877634104236762, 6.406973025524664855 ) ) ;
#24449=CARTESIAN_POINT ( 'NONE',  ( -15.93262767509097877, 3.183098147201662176, -1.443311391221110407 ) ) ;
#24511=CARTESIAN_POINT ( 'NONE',  ( 16.04706041842035802, 4.602438919581936183, 3.432847546123024340 ) ) ;
#24564=DIRECTION ( 'NONE',  ( 1.000000000000000000, -0.000000000000000000, -0.000000000000000000 ) ) ;
#24576=VERTEX_POINT ( 'NONE', #94212 ) ;
#24616=CARTESIAN_POINT ( 'NONE',  ( 13.27069161507911588, 19.68838461291719355, 7.441922568579489194 ) ) ;
#24647=EDGE_CURVE ( 'NONE', #75752, #71001, #55279, .T. ) ;
#24666=CARTESIAN_POINT ( 'NONE',  ( 16.14595037822606827, 20.73037563563847385, -4.193214079404498307 ) ) ;
#24681=CIRCLE ( 'NONE', #21232, 1.999999999999999778 ) ;
#24682=EDGE_CURVE ( 'NONE', #21618, #29736, #49488, .T. ) ;
#24752=VERTEX_POINT ( 'NONE', #99899 ) ;
#24757=FILL_AREA_STYLE ('',( #41443 ) ) ;
#24816=CARTESIAN_POINT ( 'NONE',  ( 13.46094959822379700, 24.53673296982877261, -2.096148705070425500 ) ) ;
#24859=CARTESIAN_POINT ( 'NONE',  ( -15.05945180436592779, 22.32467781490405656, 3.623638290633223846 ) ) ;
#24888=CARTESIAN_POINT ( 'NONE',  ( -15.30754850745070250, 3.114812942706816745, 3.172027124417305721 ) ) ;
#24890=ORIENTED_EDGE ( 'NONE', *, *, #52281, .F. ) ;
#24927=CARTESIAN_POINT ( 'NONE',  ( -11.77297503979913174, 16.33093105868367800, 9.431242781962609456 ) ) ;
#24947=CARTESIAN_POINT ( 'NONE',  ( -13.01572312192210035, 4.315727270466244825, 7.367595652848586418 ) ) ;
#25027=CARTESIAN_POINT ( 'NONE',  ( 16.01537606005197389, 3.832707337348138843, 1.292662844563333246 ) ) ;
#25035=CARTESIAN_POINT ( 'NONE',  ( 13.02391187303469344, 23.74004891468554490, -4.319434719146233448 ) ) ;
#25052=CARTESIAN_POINT ( 'NONE',  ( 0.000000000000000000, 34.00000000000000000, 0.000000000000000000 ) ) ;
#25082=AXIS2_PLACEMENT_3D ( 'NONE', #31377, #23270, #72840 ) ;
#25240=DIRECTION ( 'NONE',  ( 0.000000000000000000, 0.000000000000000000, 1.000000000000000000 ) ) ;
#25282=ORIENTED_EDGE ( 'NONE', *, *, #36323, .T. ) ;
#25291=LINE ( 'NONE', #83485, #884 ) ;
#25354=CARTESIAN_POINT ( 'NONE',  ( 13.79682684651001878, 23.00040460847749202, 0.2373010561590335743 ) ) ;
#25381=EDGE_CURVE ( 'NONE', #39874, #25504, #46323, .T. ) ;
#25404=CARTESIAN_POINT ( 'NONE',  ( -14.20583055102296477, 21.14383427519521419, -5.809807938884436140 ) ) ;
#25417=CARTESIAN_POINT ( 'NONE',  ( 11.76826524265346841, 16.33356993944290991, -9.436846598424574850 ) ) ;
#25501=CIRCLE ( 'NONE', #78801, 2.000000000000000000 ) ;
#25504=VERTEX_POINT ( 'NONE', #15694 ) ;
#25581=AXIS2_PLACEMENT_3D ( 'NONE', #12155, #77965, #62329 ) ;
#25586=CARTESIAN_POINT ( 'NONE',  ( 10.07445889136302419, 12.82167443387120720, -10.57244230701620857 ) ) ;
#25587=CIRCLE ( 'NONE', #82437, 8.750000000000033751 ) ;
#25686=EDGE_CURVE ( 'NONE', #76857, #20022, #6276, .T. ) ;
#25784=STYLED_ITEM ( 'NONE', ( #95036 ), #33976 ) ;
#25909=CARTESIAN_POINT ( 'NONE',  ( 15.05785784214676326, 3.824195276769945639, 4.604276673498420180 ) ) ;
#25911=CARTESIAN_POINT ( 'NONE',  ( 13.42164844308434546, 22.37475377612458161, -3.539341413710700657 ) ) ;
#25951=( LENGTH_UNIT ( ) NAMED_UNIT ( * ) SI_UNIT ( .MILLI., .METRE. ) );
#25953=CARTESIAN_POINT ( 'NONE',  ( -13.42196180547802875, 22.37528182222316886, -3.537684213275340550 ) ) ;
#25955=CIRCLE ( 'NONE', #103435, 8.750000000000023093 ) ;
#25990=ADVANCED_FACE ( 'NONE', ( #33921 ), #32267, .T. ) ;
#26085=DIRECTION ( 'NONE',  ( -0.000000000000000000, -1.000000000000000000, -0.000000000000000000 ) ) ;
#26090=( GEOMETRIC_REPRESENTATION_CONTEXT ( 3 ) GLOBAL_UNCERTAINTY_ASSIGNED_CONTEXT ( ( #13487 ) ) GLOBAL_UNIT_ASSIGNED_CONTEXT ( ( #1886, #84954, #2956 ) ) REPRESENTATION_CONTEXT ( 'NONE', 'WORKASPACE' ) );
#26160=FILL_AREA_STYLE_COLOUR ( '', #33733 ) ;
#26207=ADVANCED_FACE ( 'NONE', ( #18810 ), #30063, .T. ) ;
#26225=( LENGTH_UNIT ( ) NAMED_UNIT ( * ) SI_UNIT ( .MILLI., .METRE. ) );
#26259=CARTESIAN_POINT ( 'NONE',  ( -15.99999999999999645, 2.437231117875781727, -5.694551215225702734 ) ) ;
#26307=( LENGTH_UNIT ( ) NAMED_UNIT ( * ) SI_UNIT ( .MILLI., .METRE. ) );
#26329=CARTESIAN_POINT ( 'NONE',  ( 14.83949740352631252, 1.410031051010677716, -2.190466161075831142 ) ) ;
#26366=CARTESIAN_POINT ( 'NONE',  ( 6.239948093758000525, 10.55525250974069174, 3.176436098724912505 ) ) ;
#26408=CARTESIAN_POINT ( 'NONE',  ( -14.29190075645216851, 12.99999999999999289, 10.00000000000000178 ) ) ;
#26432=FILL_AREA_STYLE ('',( #74388 ) ) ;
#26434=CARTESIAN_POINT ( 'NONE',  ( 13.43131796715543125, 24.48388052888637745, 2.370280691517476779 ) ) ;
#26461=CARTESIAN_POINT ( 'NONE',  ( 14.11595029532510104, 2.410436752314617959, -5.024000119269091513 ) ) ;
#26472=CARTESIAN_POINT ( 'NONE',  ( -14.52296734940917311, 21.59519996265376562, -5.118403002213263164 ) ) ;
#26527=CARTESIAN_POINT ( 'NONE',  ( 6.086031112480590366, 15.01982037264469838, 3.462237351910362193 ) ) ;
#26533=( NAMED_UNIT ( * ) PLANE_ANGLE_UNIT ( ) SI_UNIT ( $, .RADIAN. ) );
#26542=CIRCLE ( 'NONE', #67618, 10.00000000000000178 ) ;
#26596=DIRECTION ( 'NONE',  ( 0.000000000000000000, 0.000000000000000000, -1.000000000000000000 ) ) ;
#26679=DIRECTION ( 'NONE',  ( 0.000000000000000000, 0.000000000000000000, -1.000000000000000000 ) ) ;
#26691=AXIS2_PLACEMENT_3D ( 'NONE', #52909, #68578, #85831 ) ;
#26749=CARTESIAN_POINT ( 'NONE',  ( -15.29454505947251164, 3.501281615896531640, -3.973654925239204605 ) ) ;
#26752=CARTESIAN_POINT ( 'NONE',  ( -15.66336674554169406, 21.48481245971760956, -5.205033774386319756 ) ) ;
#26758=B_SPLINE_CURVE_WITH_KNOTS ( 'NONE', 3,
 ( #66449, #99327, #32520, #33052, #81536, #50263 ),
 .UNSPECIFIED., .F., .F.,
 ( 4, 2, 4 ),
 ( 1.226634733346699349E-18, 0.002016319290324606727, 0.004032638580649211719 ),
 .UNSPECIFIED. ) ;
#26770=( LENGTH_UNIT ( ) NAMED_UNIT ( * ) SI_UNIT ( .MILLI., .METRE. ) );
#26806=UNCERTAINTY_MEASURE_WITH_UNIT (LENGTH_MEASURE( 1.000000000000000082E-05 ), #28727, 'distance_accuracy_value', 'NONE');
#26826=AXIS2_PLACEMENT_3D ( 'NONE', #85716, #67400, #51721 ) ;
#26856=CARTESIAN_POINT ( 'NONE',  ( 14.99524476912893434, 1.250852691627993396, -0.4434096852967474578 ) ) ;
#26889=CARTESIAN_POINT ( 'NONE',  ( 6.242019780568028864, 10.53669266913567348, -3.192545347364960762 ) ) ;
#26895=EDGE_CURVE ( 'NONE', #48149, #103416, #77212, .T. ) ;
#26904=CARTESIAN_POINT ( 'NONE',  ( 15.47206823513687368, 2.694788529765176133, -1.611870258425112334 ) ) ;
#26956=CARTESIAN_POINT ( 'NONE',  ( 13.08520229868874729, 23.85374324172591898, -4.084787787685606020 ) ) ;
#27000=( NAMED_UNIT ( * ) PLANE_ANGLE_UNIT ( ) SI_UNIT ( $, .RADIAN. ) );
#27002=CARTESIAN_POINT ( 'NONE',  ( -11.42275469891026241, 20.37773691717305269, -8.181910656862440234 ) ) ;
#27042=ORIENTED_EDGE ( 'NONE', *, *, #89592, .F. ) ;
#27113=AXIS2_PLACEMENT_3D ( 'NONE', #42484, #92097, #66227 ) ;
#27139=CARTESIAN_POINT ( 'NONE',  ( -14.44768974034976061, 5.957293599826361863, 7.129930386714873336 ) ) ;
#27145=PRESENTATION_STYLE_ASSIGNMENT (( #35224 ) ) ;
#27156=CARTESIAN_POINT ( 'NONE',  ( 16.10302234481879680, 5.501632350609837019, -4.770674012950182785 ) ) ;
#27188=TOROIDAL_SURFACE ( 'NONE', #47840, 6.999999999999999112, 0.5000000000000000000 ) ;
#27191=SURFACE_STYLE_USAGE ( .BOTH. , #35271 ) ;
#27212=ORIENTED_EDGE ( 'NONE', *, *, #5860, .F. ) ;
#27215=STYLED_ITEM ( 'NONE', ( #71547 ), #59293 ) ;
#27227=( BOUNDED_SURFACE ( )  B_SPLINE_SURFACE ( 3, 2, ( 
 ( #87045, #5050, #46562 ),
 ( #13114, #20217, #69267 ),
 ( #29880, #53594, #54624 ),
 ( #13650, #86525, #102140 ),
 ( #104257, #45522, #77344 ),
 ( #21790, #79456, #85437 ),
 ( #70844, #62760, #77877 ),
 ( #3455, #94055, #3989 ),
 ( #28294, #36917, #93536 ),
 ( #5567, #85990, #87565 ),
 ( #61169, #38494, #37983 ),
 ( #11519, #71357, #19682 ),
 ( #12062, #46040, #52521 ),
 ( #4511, #44449, #103736 ),
 ( #44992, #102679, #28840 ),
 ( #78395, #61718, #37449 ),
 ( #20756, #12587, #70318 ),
 ( #103213, #29358, #95133 ),
 ( #21267, #39013, #90206 ),
 ( #106366, #55683, #23373 ) ),
 .UNSPECIFIED., .F., .F., .F. ) 
 B_SPLINE_SURFACE_WITH_KNOTS ( ( 4, 2, 2, 2, 2, 2, 2, 2, 2, 4 ),
 ( 3, 3 ),
 ( -1.480586486746204855E-15, 0.001208125624079908192, 0.002416251248161296970, 0.003624376872242685531, 0.004832502496324074526, 0.005436565308364768589, 0.006040628120405463521, 0.007248753744486852515, 0.008456879368568242378, 0.009665004992649630505 ),
 ( 0.000000000000000000, 1.000000000000000000 ),
 .UNSPECIFIED. ) 
 GEOMETRIC_REPRESENTATION_ITEM ( )  RATIONAL_B_SPLINE_SURFACE ( (
 ( 1.000000000000000000, 0.8291561975891529324, 1.000000000000000000),
 ( 1.000000000000000000, 0.8411444448780550642, 1.000000000000000000),
 ( 1.000000000000000000, 0.8513107778598306696, 1.000000000000000000),
 ( 1.000000000000000000, 0.8686991428046330066, 1.000000000000000000),
 ( 1.000000000000000000, 0.8759367825450403711, 1.000000000000000000),
 ( 1.000000000000000000, 0.8878384569990958042, 1.000000000000000000),
 ( 1.000000000000000000, 0.8925163270236815549, 1.000000000000000000),
 ( 1.000000000000000000, 0.8988019894163230550, 1.000000000000000000),
 ( 1.000000000000000000, 0.9004488336117625336, 1.000000000000000000),
 ( 1.000000000000000000, 0.9004787869545872736, 1.000000000000000000),
 ( 1.000000000000000000, 0.9000741598243027219, 1.000000000000000000),
 ( 1.000000000000000000, 0.8984769429442116540, 1.000000000000000000),
 ( 1.000000000000000000, 0.8972871579692190958, 1.000000000000000000),
 ( 1.000000000000000000, 0.8926126616867483543, 1.000000000000000000),
 ( 1.000000000000000000, 0.8880148073973201939, 1.000000000000000000),
 ( 1.000000000000000000, 0.8760712452964969366, 1.000000000000000000),
 ( 1.000000000000000000, 0.8688049777774786708, 1.000000000000000000),
 ( 1.000000000000000000, 0.8513604698956054317, 1.000000000000000000),
 ( 1.000000000000000000, 0.8411660073558567818, 1.000000000000000000),
 ( 1.000000000000000000, 0.8291561975888496194, 1.000000000000000000) ) ) 
 REPRESENTATION_ITEM ( '' )  SURFACE ( )  );
#27246=EDGE_CURVE ( 'NONE', #83606, #77985, #28999, .T. ) ;
#27272=MECHANICAL_DESIGN_GEOMETRIC_PRESENTATION_REPRESENTATION('',(#28986),#6567);
#27289=CARTESIAN_POINT ( 'NONE',  ( -14.97535898699339185, 1.269652431127602732, 0.8876819510843543259 ) ) ;
#27318=AXIS2_PLACEMENT_3D ( 'NONE', #70954, #29990, #52631 ) ;
#27350=UNCERTAINTY_MEASURE_WITH_UNIT (LENGTH_MEASURE( 1.000000000000000082E-05 ), #52303, 'distance_accuracy_value', 'NONE');
#27393=CARTESIAN_POINT ( 'NONE',  ( 15.45341029906007080, 2.829415941283409008, 2.060260514166198931 ) ) ;
#27429=CARTESIAN_POINT ( 'NONE',  ( 6.969759372139044729, 9.053100120927640049, 0.6630323575263609159 ) ) ;
#27430=FILL_AREA_STYLE ('',( #101279 ) ) ;
#27433=EDGE_CURVE ( 'NONE', #98070, #15534, #46258, .T. ) ;
#27498=CARTESIAN_POINT ( 'NONE',  ( 16.14595037866761729, 6.775806037746459509, 6.185188124841393353 ) ) ;
#27500=CARTESIAN_POINT ( 'NONE',  ( 10.03715787451029584, 14.00015749138419174, 10.50872311893226296 ) ) ;
#27541=CARTESIAN_POINT ( 'NONE',  ( -10.81517053142260210, 16.02938924181589897, 9.536203003419373658 ) ) ;
#27595=CARTESIAN_POINT ( 'NONE',  ( 6.481635180341071667, 16.00630266284368730, 2.650895967029502476 ) ) ;
#27599=SURFACE_STYLE_USAGE ( .BOTH. , #69618 ) ;
#27622=CARTESIAN_POINT ( 'NONE',  ( -16.13488272710901583, 21.13099985707890127, -3.419103882786595605 ) ) ;
#27640=AXIS2_PLACEMENT_3D ( 'NONE', #22747, #30841, #70737 ) ;
#27651=UNCERTAINTY_MEASURE_WITH_UNIT (LENGTH_MEASURE( 1.000000000000000082E-05 ), #95144, 'distance_accuracy_value', 'NONE');
#27663=CARTESIAN_POINT ( 'NONE',  ( 20.00000000000000000, 12.99999999999999289, 0.000000000000000000 ) ) ;
#27685=AXIS2_PLACEMENT_3D ( 'NONE', #34103, #91778, #74509 ) ;
#27686=VERTEX_POINT ( 'NONE', #19115 ) ;
#27694=SURFACE_SIDE_STYLE ('',( #11444 ) ) ;
#27758=DIRECTION ( 'NONE',  ( 0.000000000000000000, 1.000000000000000000, 0.000000000000000000 ) ) ;
#27771=VERTEX_POINT ( 'NONE', #5016 ) ;
#27776=FILL_AREA_STYLE ('',( #51459 ) ) ;
#27841=CARTESIAN_POINT ( 'NONE',  ( 24.33159596665262470, 34.19642918197134662, -12.16579798332631768 ) ) ;
#27864=MECHANICAL_DESIGN_GEOMETRIC_PRESENTATION_REPRESENTATION('',(#57119),#24373);
#27885=UNCERTAINTY_MEASURE_WITH_UNIT (LENGTH_MEASURE( 1.000000000000000082E-05 ), #26307, 'distance_accuracy_value', 'NONE');
#27891=CARTESIAN_POINT ( 'NONE',  ( -16.05785784214753065, 4.775831776487158287, 3.710403933803144927 ) ) ;
#27972=CARTESIAN_POINT ( 'NONE',  ( 15.31585736565561895, 3.092902776793541975, 3.111329462080190567 ) ) ;
#27986=CARTESIAN_POINT ( 'NONE',  ( -14.95520043898949325, 4.194724623211063097, -5.164345506890816395 ) ) ;
#28000=EDGE_LOOP ( 'NONE', ( #93657, #105134, #63752, #3155 ) ) ;
#28008=CIRCLE ( 'NONE', #22839, 1.999999999999999556 ) ;
#28027=CARTESIAN_POINT ( 'NONE',  ( 10.94373115620249770, 16.64040335846121721, 9.320882347487696507 ) ) ;
#28066=CARTESIAN_POINT ( 'NONE',  ( -10.71251212345380566, 12.35323841155236479, 9.997968061205504853 ) ) ;
#28092=DIRECTION ( 'NONE',  ( 0.000000000000000000, 0.000000000000000000, -1.000000000000000000 ) ) ;
#28150=CARTESIAN_POINT ( 'NONE',  ( 14.77355847997981364, 5.782273590395790919, -6.926453096434407541 ) ) ;
#28161=ORIENTED_EDGE ( 'NONE', *, *, #4688, .T. ) ;
#28184=CARTESIAN_POINT ( 'NONE',  ( 20.00000000000000000, 12.99999999999999289, 4.000000000000000000 ) ) ;
#28193=COLOUR_RGB ( '', 0.66274510, 0.83137255, 0.94901961) ;
#28250=EDGE_LOOP ( 'NONE', ( #12076, #3690 ) ) ;
#28288=MECHANICAL_DESIGN_GEOMETRIC_PRESENTATION_REPRESENTATION('',(#23114),#31656);
#28294=CARTESIAN_POINT ( 'NONE',  ( 14.89085744133905109, 23.12183015427916999, -0.5456866263682997875 ) ) ;
#28323=SHAPE_DEFINITION_REPRESENTATION ( #76852, #66748 ) ;
#28340=SURFACE_STYLE_USAGE ( .BOTH. , #94662 ) ;
#28356=CARTESIAN_POINT ( 'NONE',  ( 29.87930712590254245, 10.71892156097790583, -14.93965356295128011 ) ) ;
#28364=ADVANCED_FACE ( 'NONE', ( #37638 ), #71680, .T. ) ;
#28436=CARTESIAN_POINT ( 'NONE',  ( -6.481635180341071667, 9.993697337156294935, -2.650895967029505140 ) ) ;
#28501=DIRECTION ( 'NONE',  ( 0.000000000000000000, 0.000000000000000000, -1.000000000000000000 ) ) ;
#28551=CARTESIAN_POINT ( 'NONE',  ( 12.53384725709329750, 20.77238591696947267, 6.330773932024738926 ) ) ;
#28592=CARTESIAN_POINT ( 'NONE',  ( -12.80228504472586692, 18.84866368018861493, 8.115852207351810677 ) ) ;
#28636=CARTESIAN_POINT ( 'NONE',  ( 14.29190075645216851, 12.99999999999999289, 10.00000000000000000 ) ) ;
#28680=AXIS2_PLACEMENT_3D ( 'NONE', #76931, #84504, #60252 ) ;
#28690=EDGE_CURVE ( 'NONE', #63378, #55614, #23978, .T. ) ;
#28701=CARTESIAN_POINT ( 'NONE',  ( -15.00099999999999767, 12.99999999999999289, -10.00000000000000178 ) ) ;
#28705=PRODUCT ( '5. Joint', '5. Joint', '', ( #102175 ) ) ;
#28712=ORIENTED_EDGE ( 'NONE', *, *, #73393, .T. ) ;
#28721=EDGE_LOOP ( 'NONE', ( #34322, #56946, #28748 ) ) ;
#28727=( LENGTH_UNIT ( ) NAMED_UNIT ( * ) SI_UNIT ( .MILLI., .METRE. ) );
#28748=ORIENTED_EDGE ( 'NONE', *, *, #72002, .T. ) ;
#28820=DIRECTION ( 'NONE',  ( 0.000000000000000000, 0.000000000000000000, -1.000000000000000000 ) ) ;
#28831=EDGE_CURVE ( 'NONE', #51169, #23419, #13258, .T. ) ;
#28840=CARTESIAN_POINT ( 'NONE',  ( 16.11696382278844197, 21.57140452653176865, 2.149593460099603170 ) ) ;
#28841=DIRECTION ( 'NONE',  ( -1.000000000000000000, 0.000000000000000000, 0.000000000000000000 ) ) ;
#28846=DIRECTION ( 'NONE',  ( -1.000000000000000000, 0.000000000000000000, 0.000000000000000000 ) ) ;
#28892=CARTESIAN_POINT ( 'NONE',  ( -15.68546860017134748, 21.68927415055489405, -4.769872285932397205 ) ) ;
#28905=FACE_OUTER_BOUND ( 'NONE', #76646, .T. ) ;
#28906=CARTESIAN_POINT ( 'NONE',  ( 29.99397490504468067, 1.005902684993158047, -14.99698745252235099 ) ) ;
#28913=CARTESIAN_POINT ( 'NONE',  ( 13.22204626516810322, 24.10488446132543316, 3.477574009107253339 ) ) ;
#28948=UNCERTAINTY_MEASURE_WITH_UNIT (LENGTH_MEASURE( 1.000000000000000082E-05 ), #80219, 'distance_accuracy_value', 'NONE');
#28954=SURFACE_STYLE_USAGE ( .BOTH. , #20870 ) ;
#28960=CARTESIAN_POINT ( 'NONE',  ( -13.24996097722020139, 3.894558718262700392, -6.960810507241065537 ) ) ;
#28963=( GEOMETRIC_REPRESENTATION_CONTEXT ( 3 ) GLOBAL_UNCERTAINTY_ASSIGNED_CONTEXT ( ( #29445 ) ) GLOBAL_UNIT_ASSIGNED_CONTEXT ( ( #13655, #95138, #4516 ) ) REPRESENTATION_CONTEXT ( 'NONE', 'WORKASPACE' ) );
#28986=STYLED_ITEM ( 'NONE', ( #32467 ), #205 ) ;
#28992=CARTESIAN_POINT ( 'NONE',  ( -5.744562646538028616, 12.99999999999999289, -4.000000000000000000 ) ) ;
#28999=CIRCLE ( 'NONE', #92675, 1.000000000000000888 ) ;
#29036=CARTESIAN_POINT ( 'NONE',  ( 0.000000000000000000, 0.9999999999999970024, 7.000000000000000000 ) ) ;
#29040=CARTESIAN_POINT ( 'NONE',  ( 15.64030048137866835, 6.456385560667919243, -7.561819230143238535 ) ) ;
#29051=FILL_AREA_STYLE_COLOUR ( '', #63056 ) ;
#29105=CARTESIAN_POINT ( 'NONE',  ( 13.02890126842911123, 21.69022161494968159, 4.974805862544680046 ) ) ;
#29120=CIRCLE ( 'NONE', #20578, 0.5000000000000004441 ) ;
#29143=CARTESIAN_POINT ( 'NONE',  ( -11.65430815032340206, 15.87850340580320641, 9.580969490850751669 ) ) ;
#29198=CARTESIAN_POINT ( 'NONE',  ( 6.481161585458342422, 16.00528638454814256, -2.652050489361057029 ) ) ;
#29321=ADVANCED_FACE ( 'NONE', ( #89102 ), #21926, .F. ) ;
#29358=CARTESIAN_POINT ( 'NONE',  ( 15.68557340203072137, 21.69024387810497956, 4.767881275881356906 ) ) ;
#29434=CARTESIAN_POINT ( 'NONE',  ( 10.14382783504288632, 15.68598017974148107, 10.24918285280354624 ) ) ;
#29436=( NAMED_UNIT ( * ) SI_UNIT ( $, .STERADIAN. ) SOLID_ANGLE_UNIT ( ) );
#29445=UNCERTAINTY_MEASURE_WITH_UNIT (LENGTH_MEASURE( 1.000000000000000082E-05 ), #13655, 'distance_accuracy_value', 'NONE');
#29473=CARTESIAN_POINT ( 'NONE',  ( -16.13590653351290527, 6.313628335808340708, 5.716602451450103928 ) ) ;
#29477=CARTESIAN_POINT ( 'NONE',  ( -12.85904595378377735, 23.43151218796164059, -4.877252156032461095 ) ) ;
#29483=ADVANCED_FACE ( 'NONE', ( #67490 ), #92268, .T. ) ;
#29517=DIRECTION ( 'NONE',  ( 0.000000000000000000, 0.000000000000000000, 1.000000000000000000 ) ) ;
#29548=COLOUR_RGB ( '', 0.31764706, 0.68627451, 0.89019608) ;
#29557=CARTESIAN_POINT ( 'NONE',  ( 16.03938085755554255, 4.451364308013095794, -3.146830695484701845 ) ) ;
#29586=CIRCLE ( 'NONE', #101834, 14.99698745252234566 ) ;
#29610=CARTESIAN_POINT ( 'NONE',  ( -18.00000000000000355, 12.99999999999999289, 0.000000000000000000 ) ) ;
#29614=CARTESIAN_POINT ( 'NONE',  ( 10.65767722103599979, 14.87225365928225607, 9.828355766833842821 ) ) ;
#29657=CARTESIAN_POINT ( 'NONE',  ( -10.65078532968085590, 18.17514175625904826, 9.445934609551695615 ) ) ;
#29736=VERTEX_POINT ( 'NONE', #26408 ) ;
#29738=CARTESIAN_POINT ( 'NONE',  ( 14.04769258328531834, 4.430038579581392355, -5.212585019726944324 ) ) ;
#29775=( NAMED_UNIT ( * ) SI_UNIT ( $, .STERADIAN. ) SOLID_ANGLE_UNIT ( ) );
#29785=CARTESIAN_POINT ( 'NONE',  ( -13.67306322407435815, 5.033750017361354523, -6.094185097971928755 ) ) ;
#29801=EDGE_LOOP ( 'NONE', ( #24890, #64411, #95922, #76193 ) ) ;
#29818=CARTESIAN_POINT ( 'NONE',  ( 0.000000000000000000, 0.9999999999999970024, 8.000000000000000000 ) ) ;
#29837=VERTEX_POINT ( 'NONE', #102374 ) ;
#29875=CARTESIAN_POINT ( 'NONE',  ( -13.72062045121628415, 20.42744233313543489, -6.730531604610976437 ) ) ;
#29880=CARTESIAN_POINT ( 'NONE',  ( 14.45674127754722349, 21.77180424839734485, -4.838420908114524188 ) ) ;
#29884=SURFACE_SIDE_STYLE ('',( #21794 ) ) ;
#29924=CARTESIAN_POINT ( 'NONE',  ( -15.79067987436804188, 22.71383723441329394, 1.248691266770723285 ) ) ;
#29947=CARTESIAN_POINT ( 'NONE',  ( 10.18660115262752086, 16.00273039107469941, 10.17531074053961682 ) ) ;
#29953=ORIENTED_EDGE ( 'NONE', *, *, #24251, .T. ) ;
#29990=DIRECTION ( 'NONE',  ( 1.000000000000000000, 0.000000000000000000, 0.000000000000000000 ) ) ;
#29992=CARTESIAN_POINT ( 'NONE',  ( -13.54312819440545113, 24.68321509063727248, 1.318894457162179235 ) ) ;
#30021=CARTESIAN_POINT ( 'NONE',  ( -6.999814028509885766, 9.000325450264105243, -0.2742116757349308265 ) ) ;
#30063=( BOUNDED_SURFACE ( )  B_SPLINE_SURFACE ( 3, 2, ( 
 ( #10658, #44113, #61368 ),
 ( #68933, #43573, #17714 ),
 ( #101807, #77540, #11718 ),
 ( #27972, #44657, #50575 ),
 ( #83492, #84034, #67850 ),
 ( #76460, #9591, #34462 ),
 ( #100212, #59240, #10137 ),
 ( #43051, #104454, #70514 ),
 ( #22520, #103404, #30602 ),
 ( #63492, #103923, #12784 ),
 ( #4180, #55363, #20953 ),
 ( #96390, #46757, #102878 ),
 ( #21979, #62428, #30070 ),
 ( #53784, #88292, #71032 ),
 ( #14367, #47276, #95318 ),
 ( #79122, #87762, #79651 ),
 ( #5248, #62953, #61912 ),
 ( #53267, #6278, #29557 ),
 ( #94804, #37653, #95849 ),
 ( #54834, #46237, #80174 ) ),
 .UNSPECIFIED., .F., .F., .T. ) 
 B_SPLINE_SURFACE_WITH_KNOTS ( ( 4, 2, 2, 2, 2, 2, 2, 2, 2, 4 ),
 ( 3, 3 ),
 ( 0.001112359326668568328, 0.002061628542468994449, 0.003010897758269421003, 0.003960166974069847558, 0.004909436189870273679, 0.005858705405670700667, 0.006807974621471126787, 0.007282609229371340281, 0.007757243837271552908, 0.008706513053071979896 ),
 ( 0.000000000000000000, 1.000000000000000000 ),
 .UNSPECIFIED. ) 
 GEOMETRIC_REPRESENTATION_ITEM ( )  RATIONAL_B_SPLINE_SURFACE ( (
 ( 1.000000000000000000, 0.9115707425106703843, 1.000000000000000000),
 ( 1.000000000000000000, 0.9186010707723997193, 1.000000000000000000),
 ( 1.000000000000000000, 0.9248333139228899213, 1.000000000000000000),
 ( 1.000000000000000000, 0.9351156329914673826, 1.000000000000000000),
 ( 1.000000000000000000, 0.9392288573273753771, 1.000000000000000000),
 ( 1.000000000000000000, 0.9457209207428006748, 1.000000000000000000),
 ( 1.000000000000000000, 0.9480998420262755078, 1.000000000000000000),
 ( 1.000000000000000000, 0.9511999291517022614, 1.000000000000000000),
 ( 1.000000000000000000, 0.9519548416862092521, 1.000000000000000000),
 ( 1.000000000000000000, 0.9519314736513960762, 1.000000000000000000),
 ( 1.000000000000000000, 0.9511539719351175259, 1.000000000000000000),
 ( 1.000000000000000000, 0.9480480161104184456, 1.000000000000000000),
 ( 1.000000000000000000, 0.9457194361327755372, 1.000000000000000000),
 ( 1.000000000000000000, 0.9408176163900222599, 1.000000000000000000),
 ( 1.000000000000000000, 0.9389456878146280605, 1.000000000000000000),
 ( 1.000000000000000000, 0.9347647373046783503, 1.000000000000000000),
 ( 1.000000000000000000, 0.9324473665774060116, 1.000000000000000000),
 ( 1.000000000000000000, 0.9247734139713987833, 1.000000000000000000),
 ( 1.000000000000000000, 0.9186884142194181591, 1.000000000000000000),
 ( 1.000000000000000000, 0.9115707425106747142, 1.000000000000000000) ) ) 
 REPRESENTATION_ITEM ( '' )  SURFACE ( )  );
#30068=CARTESIAN_POINT ( 'NONE',  ( 16.14595037822608958, 7.274337365584599091, -6.616591826375524121 ) ) ;
#30070=CARTESIAN_POINT ( 'NONE',  ( 16.01731991787289999, 3.900165755866083828, -1.616345057638605143 ) ) ;
#30109=CARTESIAN_POINT ( 'NONE',  ( -24.33159596665262470, 34.19642918197134662, 12.16579798332631768 ) ) ;
#30112=FACE_OUTER_BOUND ( 'NONE', #829, .T. ) ;
#30116=ORIENTED_EDGE ( 'NONE', *, *, #2942, .T. ) ;
#30127=CARTESIAN_POINT ( 'NONE',  ( 15.05475665200631497, 5.402209584884851701, 6.523587638318953275 ) ) ;
#30152=ORIENTED_EDGE ( 'NONE', *, *, #73393, .F. ) ;
#30168=CARTESIAN_POINT ( 'NONE',  ( -10.89906287216224534, 8.997476634352441494, 10.00979493832057088 ) ) ;
#30182=CARTESIAN_POINT ( 'NONE',  ( 20.00100000000000122, 12.99999999999999289, 0.000000000000000000 ) ) ;
#30250=CARTESIAN_POINT ( 'NONE',  ( 12.35621370429071675, 9.768256507115607334, -9.479262080219816866 ) ) ;
#30271=CARTESIAN_POINT ( 'NONE',  ( -18.00000000000000355, 12.99999999999999467, -9.500000000000000000 ) ) ;
#30301=CARTESIAN_POINT ( 'NONE',  ( -10.76670854121271326, 15.75155368674281675, -9.619787616750810955 ) ) ;
#30336=CARTESIAN_POINT ( 'NONE',  ( -16.05785784214673484, 4.775831776474318779, -3.710403933782550290 ) ) ;
#30378=EDGE_CURVE ( 'NONE', #21676, #54847, #21103, .T. ) ;
#30381=EDGE_LOOP ( 'NONE', ( #47286, #56498, #78798, #4587 ) ) ;
#30401=CARTESIAN_POINT ( 'NONE',  ( -15.50988061984491395, 2.604948194297879382, 0.4026888889386251447 ) ) ;
#30403=( NAMED_UNIT ( * ) SI_UNIT ( $, .STERADIAN. ) SOLID_ANGLE_UNIT ( ) );
#30406=DIRECTION ( 'NONE',  ( 0.000000000000000000, -0.6543614439331875143, -0.7561819230143458359 ) ) ;
#30455=CARTESIAN_POINT ( 'NONE',  ( -15.79700980112394326, 22.78020937716808803, 0.4986931010682000287 ) ) ;
#30474=CARTESIAN_POINT ( 'NONE',  ( 13.70945920918955174, 3.091663963860816988, 6.042453855890579817 ) ) ;
#30486=CARTESIAN_POINT ( 'NONE',  ( -11.66623074095491752, 11.72717158878924693, 9.938064884429101298 ) ) ;
#30507=EDGE_LOOP ( 'NONE', ( #100600, #100809, #15502, #99719 ) ) ;
#30514=DIRECTION ( 'NONE',  ( -1.000000000000000000, -0.000000000000000000, -0.000000000000000000 ) ) ;
#30523=CARTESIAN_POINT ( 'NONE',  ( -10.04689216137323626, 14.71245185582296244, 10.43754960648917063 ) ) ;
#30578=CARTESIAN_POINT ( 'NONE',  ( 14.14239901661592214, 6.671053996447657397, -7.747582395498725738 ) ) ;
#30600=( LENGTH_UNIT ( ) NAMED_UNIT ( * ) SI_UNIT ( .MILLI., .METRE. ) );
#30602=CARTESIAN_POINT ( 'NONE',  ( 16.01234866801993562, 3.721647123654680200, 0.3211924699178611009 ) ) ;
#30615=ORIENTED_EDGE ( 'NONE', *, *, #7200, .F. ) ;
#30649=FILL_AREA_STYLE ('',( #15495 ) ) ;
#30668=CARTESIAN_POINT ( 'NONE',  ( 13.72259981623363245, 3.069379053792045564, 6.012713411074214420 ) ) ;
#30723=FACE_OUTER_BOUND ( 'NONE', #13025, .T. ) ;
#30790=CARTESIAN_POINT ( 'NONE',  ( -6.981089760825446078, 16.96682926832163574, -0.5312715680615397451 ) ) ;
#30794=CARTESIAN_POINT ( 'NONE',  ( 12.59533268909488868, 9.265824853558118690, -9.291863273163992076 ) ) ;
#30815=CARTESIAN_POINT ( 'NONE',  ( 0.000000000000000000, 34.19642918197134662, 0.000000000000000000 ) ) ;
#30836=ORIENTED_EDGE ( 'NONE', *, *, #34953, .F. ) ;
#30838=CIRCLE ( 'NONE', #13542, 11.18527996897366528 ) ;
#30841=DIRECTION ( 'NONE',  ( 0.000000000000000000, 1.000000000000000000, 0.000000000000000000 ) ) ;
#30842=CARTESIAN_POINT ( 'NONE',  ( -12.80299720903387772, 18.86371276137014874, -8.118784003668798377 ) ) ;
#30844=( GEOMETRIC_REPRESENTATION_CONTEXT ( 3 ) GLOBAL_UNCERTAINTY_ASSIGNED_CONTEXT ( ( #33334 ) ) GLOBAL_UNIT_ASSIGNED_CONTEXT ( ( #92893, #34699, #67574 ) ) REPRESENTATION_CONTEXT ( 'NONE', 'WORKASPACE' ) );
#30894=AXIS2_PLACEMENT_3D ( 'NONE', #69254, #35847, #2889 ) ;
#30901=DIRECTION ( 'NONE',  ( 1.000000000000000000, 0.000000000000000000, 0.000000000000000000 ) ) ;
#30903=CARTESIAN_POINT ( 'NONE',  ( 16.05785784214672773, 4.775831776474238843, 3.710403933782425057 ) ) ;
#30944=CARTESIAN_POINT ( 'NONE',  ( -15.36292483821495125, 2.971926847717763831, -2.727430453969307944 ) ) ;
#30997=CARTESIAN_POINT ( 'NONE',  ( -15.66340762197392777, 21.48519827103249824, 5.204287273233059175 ) ) ;
#31019=CARTESIAN_POINT ( 'NONE',  ( 13.92274006198912950, 2.731168379989813211, 5.554047545514793072 ) ) ;
#31032=CARTESIAN_POINT ( 'NONE',  ( -12.67601371193146420, 9.116793994832203651, 9.219871167800874900 ) ) ;
#31131=( NAMED_UNIT ( * ) SI_UNIT ( $, .STERADIAN. ) SOLID_ANGLE_UNIT ( ) );
#31189=CARTESIAN_POINT ( 'NONE',  ( -3.673202536116901758E-15, 1.005902684993158047, -14.99698745252234566 ) ) ;
#31201=CARTESIAN_POINT ( 'NONE',  ( -16.05785784214673484, 4.775831776474317891, -3.710403933782548513 ) ) ;
#31245=CARTESIAN_POINT ( 'NONE',  ( -12.37099948902435465, 9.735505124397592525, 9.467962123340013747 ) ) ;
#31255=PRESENTATION_STYLE_ASSIGNMENT (( #105114 ) ) ;
#31322=CARTESIAN_POINT ( 'NONE',  ( -6.481071417163346560, 16.00509389820063078, -2.652271756153595561 ) ) ;
#31327=CARTESIAN_POINT ( 'NONE',  ( 10.60657896622984175, 9.978945271511751258, -10.25335130518080007 ) ) ;
#31348=CARTESIAN_POINT ( 'NONE',  ( -14.62302398986549967, 22.28582220554202920, -3.922348837399933341 ) ) ;
#31371=FILL_AREA_STYLE ('',( #105742 ) ) ;
#31375=CARTESIAN_POINT ( 'NONE',  ( -11.23306095913861213, 17.71175306491347712, -8.845014664451463560 ) ) ;
#31377=CARTESIAN_POINT ( 'NONE',  ( 20.00100000000000477, 12.99999999999999289, 0.000000000000000000 ) ) ;
#31400=CARTESIAN_POINT ( 'NONE',  ( -15.00099999999999767, 12.99999999999999289, 0.000000000000000000 ) ) ;
#31435=CARTESIAN_POINT ( 'NONE',  ( 16.13647630347087514, 6.334953579828610515, 5.738861489051994447 ) ) ;
#31463=CARTESIAN_POINT ( 'NONE',  ( -1.722054852581828306E-15, 24.73290587908618932, -14.06164498842270483 ) ) ;
#31471=CARTESIAN_POINT ( 'NONE',  ( -15.13304769501037050, 3.593526408006888939, 4.245863293369651181 ) ) ;
#31489=CARTESIAN_POINT ( 'NONE',  ( -14.11595029532502643, 2.410436752314748521, -5.024000119269296682 ) ) ;
#31521=CARTESIAN_POINT ( 'NONE',  ( -16.14595037822608958, 20.23371447308013771, 4.922994507609250725 ) ) ;
#31569=MECHANICAL_DESIGN_GEOMETRIC_PRESENTATION_REPRESENTATION('',(#17771),#12656);
#31579=CARTESIAN_POINT ( 'NONE',  ( 14.29190075645216851, 12.99999999999999289, -10.00000000000000178 ) ) ;
#31581=ORIENTED_EDGE ( 'NONE', *, *, #75675, .F. ) ;
#31656=( GEOMETRIC_REPRESENTATION_CONTEXT ( 3 ) GLOBAL_UNCERTAINTY_ASSIGNED_CONTEXT ( ( #56679 ) ) GLOBAL_UNIT_ASSIGNED_CONTEXT ( ( #58996, #19107, #51945 ) ) REPRESENTATION_CONTEXT ( 'NONE', 'WORKASPACE' ) );
#31722=CARTESIAN_POINT ( 'NONE',  ( 15.78903373183817394, 4.458378530872352918, 5.229003202815950324 ) ) ;
#31742=( GEOMETRIC_REPRESENTATION_CONTEXT ( 3 ) GLOBAL_UNCERTAINTY_ASSIGNED_CONTEXT ( ( #92957 ) ) GLOBAL_UNIT_ASSIGNED_CONTEXT ( ( #44299, #45891, #61562 ) ) REPRESENTATION_CONTEXT ( 'NONE', 'WORKASPACE' ) );
#31758=CARTESIAN_POINT ( 'NONE',  ( -11.67652068491833006, 8.895001519498853426, 9.142920084771974487 ) ) ;
#31794=EDGE_LOOP ( 'NONE', ( #84913, #1216, #39794, #64674, #94932, #33216, #89032, #43478, #93542 ) ) ;
#31816=VECTOR ( 'NONE', #105820, 1000.000000000000000 ) ;
#31838=EDGE_LOOP ( 'NONE', ( #18543, #91604, #93668, #49872 ) ) ;
#31841=CARTESIAN_POINT ( 'NONE',  ( 10.06039080892654169, 12.97763442506446907, -10.57343087305293317 ) ) ;
#31861=CARTESIAN_POINT ( 'NONE',  ( -14.82216446135968901, 22.90771190644582234, 1.995522466596231226 ) ) ;
#31885=CARTESIAN_POINT ( 'NONE',  ( -10.18585140722862192, 16.00067669882299271, -10.17614714549901578 ) ) ;
#31896=CARTESIAN_POINT ( 'NONE',  ( 19.50000000000000000, 12.99999999999999289, 7.500000000000000000 ) ) ;
#31901=CARTESIAN_POINT ( 'NONE',  ( -15.29749241880924338, 3.521433830184460767, 3.946287723054361152 ) ) ;
#31911=CARTESIAN_POINT ( 'NONE',  ( 1.714138721600513892E-15, 0.9999999999999943379, 13.99700487351915612 ) ) ;
#31927=CARTESIAN_POINT ( 'NONE',  ( -15.68120647348229468, 6.021684053265807357, -7.051923121162609220 ) ) ;
#31961=LINE ( 'NONE', #49711, #31816 ) ;
#32002=CARTESIAN_POINT ( 'NONE',  ( 14.36577178754511763, 3.159923610463285293, -4.257245723725899822 ) ) ;
#32005=CARTESIAN_POINT ( 'NONE',  ( -14.89763918506242213, 1.348991191048001692, -1.758109506422078638 ) ) ;
#32064=CARTESIAN_POINT ( 'NONE',  ( 12.86305608435086256, 23.43906773663930565, -4.864083290606698640 ) ) ;
#32065=EDGE_CURVE ( 'NONE', #43945, #17545, #84324, .T. ) ;
#32120=ORIENTED_EDGE ( 'NONE', *, *, #24647, .F. ) ;
#32135=CARTESIAN_POINT ( 'NONE',  ( -6.321708934325914520, 10.35608347206918545, 3.012444762083620109 ) ) ;
#32145=( GEOMETRIC_REPRESENTATION_CONTEXT ( 3 ) GLOBAL_UNCERTAINTY_ASSIGNED_CONTEXT ( ( #38595 ) ) GLOBAL_UNIT_ASSIGNED_CONTEXT ( ( #3642, #61355, #61896 ) ) REPRESENTATION_CONTEXT ( 'NONE', 'WORKASPACE' ) );
#32149=ORIENTED_EDGE ( 'NONE', *, *, #30378, .T. ) ;
#32179=CARTESIAN_POINT ( 'NONE',  ( 20.00000000000000000, 12.99999999999999289, -6.999999999999999112 ) ) ;
#32224=ORIENTED_EDGE ( 'NONE', *, *, #35503, .T. ) ;
#32231=CARTESIAN_POINT ( 'NONE',  ( -3.444109705163657007E-15, 24.73290587908618932, -14.06164498842270483 ) ) ;
#32244=ORIENTED_EDGE ( 'NONE', *, *, #7200, .T. ) ;
#32247=CARTESIAN_POINT ( 'NONE',  ( 14.23326139838831494, 6.534605160808406588, 7.647391678231034717 ) ) ;
#32267=TOROIDAL_SURFACE ( 'NONE', #56312, 6.999999999999999112, 0.5000000000000000000 ) ;
#32302=STYLED_ITEM ( 'NONE', ( #75567 ), #29483 ) ;
#32310=EDGE_CURVE ( 'NONE', #55614, #21618, #69174, .T. ) ;
#32328=( GEOMETRIC_REPRESENTATION_CONTEXT ( 3 ) GLOBAL_UNCERTAINTY_ASSIGNED_CONTEXT ( ( #58036 ) ) GLOBAL_UNIT_ASSIGNED_CONTEXT ( ( #61330, #59732, #68894 ) ) REPRESENTATION_CONTEXT ( 'NONE', 'WORKASPACE' ) );
#32380=CARTESIAN_POINT ( 'NONE',  ( 11.66272034348327757, 8.929129883720431593, -9.157998212364818258 ) ) ;
#32416=CARTESIAN_POINT ( 'NONE',  ( 14.99580413334056139, 1.250310433696042889, -0.8744943966827515291 ) ) ;
#32426=CARTESIAN_POINT ( 'NONE',  ( -12.36035296938143446, 9.759048222428928554, -9.476106837505529512 ) ) ;
#32446=SURFACE_STYLE_FILL_AREA ( #82561 ) ;
#32467=PRESENTATION_STYLE_ASSIGNMENT (( #14111 ) ) ;
#32494=CARTESIAN_POINT ( 'NONE',  ( -11.46409645960823021, 12.99999999999756994, 10.00000000000000178 ) ) ;
#32512=CARTESIAN_POINT ( 'NONE',  ( -13.40797866535512028, 24.44206711738619475, -2.534967161872643260 ) ) ;
#32520=CARTESIAN_POINT ( 'NONE',  ( 14.58934900096756770, 5.487773041252724582, -6.668063844682254881 ) ) ;
#32529=CARTESIAN_POINT ( 'NONE',  ( -15.43760447746183928, 2.782577468885437000, -1.950845582978123938 ) ) ;
#32538=VERTEX_POINT ( 'NONE', #56594 ) ;
#32602=CARTESIAN_POINT ( 'NONE',  ( 13.44467335266196528, 24.50761115066882212, -2.221713994527983793 ) ) ;
#32627=ORIENTED_EDGE ( 'NONE', *, *, #10077, .T. ) ;
#32641=B_SPLINE_CURVE_WITH_KNOTS ( 'NONE', 3,
 ( #43282, #102041, #92889, #51891, #84807, #1742 ),
 .UNSPECIFIED., .F., .F.,
 ( 4, 2, 4 ),
 ( 0.000000000000000000, 0.002016319290324576803, 0.004032638580649153606 ),
 .UNSPECIFIED. ) ;
#32677=CARTESIAN_POINT ( 'NONE',  ( -6.481161585458341534, 9.994713615451841449, 2.652050489361055696 ) ) ;
#32690=SURFACE_STYLE_FILL_AREA ( #96869 ) ;
#32755=UNCERTAINTY_MEASURE_WITH_UNIT (LENGTH_MEASURE( 1.000000000000000082E-05 ), #55581, 'distance_accuracy_value', 'NONE');
#32799=ADVANCED_FACE ( 'NONE', ( #88340, #14952 ), #70044, .F. ) ;
#32909=CARTESIAN_POINT ( 'NONE',  ( 14.52361579593611296, 21.59610066891373137, -5.116830242441418264 ) ) ;
#32947=CARTESIAN_POINT ( 'NONE',  ( 14.68536286785138323, 1.589102881334510720, 3.051189359066827311 ) ) ;
#32955=CARTESIAN_POINT ( 'NONE',  ( -13.61191251355394449, 22.69522632434492238, 2.525242973133198010 ) ) ;
#33032=AXIS2_PLACEMENT_3D ( 'NONE', #100886, #10283, #91752 ) ;
#33044=CARTESIAN_POINT ( 'NONE',  ( -12.19077546297355141, 22.10107656903681672, 6.639256695208207937 ) ) ;
#33046=DIRECTION ( 'NONE',  ( 0.000000000000000000, 0.000000000000000000, -1.000000000000000000 ) ) ;
#33052=CARTESIAN_POINT ( 'NONE',  ( 14.84266821126404423, 4.606643506680114797, -5.685020543968223095 ) ) ;
#33057=ORIENTED_EDGE ( 'NONE', *, *, #19401, .F. ) ;
#33059=CARTESIAN_POINT ( 'NONE',  ( -16.05785784214732104, 4.775831776487164504, 3.710403933803105847 ) ) ;
#33064=DIRECTION ( 'NONE',  ( 0.000000000000000000, 0.000000000000000000, -1.000000000000000000 ) ) ;
#33081=MECHANICAL_DESIGN_GEOMETRIC_PRESENTATION_REPRESENTATION('',(#60640),#88184);
#33128=CARTESIAN_POINT ( 'NONE',  ( 10.35700060563541669, 16.95883745406678855, -9.900998136418390771 ) ) ;
#33200=CARTESIAN_POINT ( 'NONE',  ( -5.835411572216779419, 11.94238963164415068, 3.866789010015637462 ) ) ;
#33216=ORIENTED_EDGE ( 'NONE', *, *, #79053, .F. ) ;
#33262=ORIENTED_EDGE ( 'NONE', *, *, #92928, .T. ) ;
#33334=UNCERTAINTY_MEASURE_WITH_UNIT (LENGTH_MEASURE( 1.000000000000000082E-05 ), #92893, 'distance_accuracy_value', 'NONE');
#33366=CARTESIAN_POINT ( 'NONE',  ( 6.996281870428059158, 9.006495247806538984, 0.2643931112039918929 ) ) ;
#33380=CARTESIAN_POINT ( 'NONE',  ( 15.05785784214677392, 3.824195276769925655, -4.604276673498363337 ) ) ;
#33435=CARTESIAN_POINT ( 'NONE',  ( 15.68120647347719299, 6.021684053266091574, 7.051923121159668462 ) ) ;
#33437=CARTESIAN_POINT ( 'NONE',  ( 12.94162442892976017, 23.58706790872225767, 4.602324725384438153 ) ) ;
#33478=CARTESIAN_POINT ( 'NONE',  ( -13.55912885999853579, 24.71192378330096773, -1.209952234050663211 ) ) ;
#33495=PRESENTATION_STYLE_ASSIGNMENT (( #49653 ) ) ;
#33501=CARTESIAN_POINT ( 'NONE',  ( -16.05785784214753775, 4.775831776487168945, 3.710403933803116949 ) ) ;
#33613=CARTESIAN_POINT ( 'NONE',  ( -15.05785784214257461, 3.824195276785042896, 4.604276673521232155 ) ) ;
#33620=FACE_OUTER_BOUND ( 'NONE', #31838, .T. ) ;
#33650=CARTESIAN_POINT ( 'NONE',  ( 10.36976902195542749, 10.88984728681280778, -10.43162212896576335 ) ) ;
#33733=COLOUR_RGB ( '', 0.08235294, 0.09019608, 0.10196078) ;
#33760=( NAMED_UNIT ( * ) PLANE_ANGLE_UNIT ( ) SI_UNIT ( $, .RADIAN. ) );
#33767=CARTESIAN_POINT ( 'NONE',  ( 11.42008614078136119, 13.49845512739828202, 9.994469747613118571 ) ) ;
#33862=AXIS2_PLACEMENT_3D ( 'NONE', #25052, #99969, #91368 ) ;
#33909=CARTESIAN_POINT ( 'NONE',  ( 6.560102024233679607, 9.829711121158393183, 2.452861370513718331 ) ) ;
#33921=FACE_OUTER_BOUND ( 'NONE', #37019, .T. ) ;
#33976=ADVANCED_FACE ( 'NONE', ( #86943 ), #10177, .F. ) ;
#33978=CARTESIAN_POINT ( 'NONE',  ( 15.82318872385758546, 4.444012391148053354, 4.874853782833517002 ) ) ;
#33980=CARTESIAN_POINT ( 'NONE',  ( 13.52808898108708568, 24.65652623284792000, 1.487090316686600744 ) ) ;
#34027=CARTESIAN_POINT ( 'NONE',  ( -13.77345804302984789, 22.96215306780717924, -1.017947650526750181 ) ) ;
#34045=DIRECTION ( 'NONE',  ( 1.000000000000000000, -0.000000000000000000, -0.000000000000000000 ) ) ;
#34103=CARTESIAN_POINT ( 'NONE',  ( -14.29190075645224844, 19.61368180394242700, -4.501023549838558679 ) ) ;
#34158=CARTESIAN_POINT ( 'NONE',  ( 0.000000000000000000, 34.19642918197134662, 0.000000000000000000 ) ) ;
#34187=CARTESIAN_POINT ( 'NONE',  ( 16.01235146068399473, 3.721755040408527115, 0.3223148954820237444 ) ) ;
#34213=ORIENTED_EDGE ( 'NONE', *, *, #34620, .F. ) ;
#34263=DIRECTION ( 'NONE',  ( 0.000000000000000000, 0.6543614439331889576, -0.7561819230143446147 ) ) ;
#34280=B_SPLINE_CURVE_WITH_KNOTS ( 'NONE', 3,
 ( #28992, #95803, #36541, #62383, #20904, #102290, #53739, #86668, #95277, #28436, #87185, #20376, #46186, #79078, #70984, #103873, #30021, #21933, #54783, #8363, #81181, #65547, #15395, #97367, #32677, #32135, #41264, #88761, #39166, #89301, #33200, #40200, #14858, #98435 ),
 .UNSPECIFIED., .F., .F.,
 ( 4, 2, 2, 2, 2, 2, 2, 2, 2, 2, 2, 2, 2, 2, 2, 2, 4 ),
 ( 0.01279395524623341482, 0.01359199989167121127, 0.01439004453710900772, 0.01518808918254680243, 0.01598613382798460061, 0.01678417847342239533, 0.01758222311886019351, 0.01838026776429798823, 0.01917831240973578294, 0.01997635705517358112, 0.02077440170061137931, 0.02157244634604917402, 0.02237049099148696873, 0.02316853563692476692, 0.02396658028236256510, 0.02476462492780035982, 0.02556266957323815453 ),
 .UNSPECIFIED. ) ;
#34299=( GEOMETRIC_REPRESENTATION_CONTEXT ( 3 ) GLOBAL_UNCERTAINTY_ASSIGNED_CONTEXT ( ( #44834 ) ) GLOBAL_UNIT_ASSIGNED_CONTEXT ( ( #25951, #27000, #17820 ) ) REPRESENTATION_CONTEXT ( 'NONE', 'WORKASPACE' ) );
#34302=CARTESIAN_POINT ( 'NONE',  ( -15.37029426978759084, 3.165964433752528784, -3.249157221772423831 ) ) ;
#34322=ORIENTED_EDGE ( 'NONE', *, *, #81419, .F. ) ;
#34340=DIRECTION ( 'NONE',  ( 0.000000000000000000, 0.8802307401770171902, 0.4745459346021421165 ) ) ;
#34365=UNCERTAINTY_MEASURE_WITH_UNIT (LENGTH_MEASURE( 1.000000000000000082E-05 ), #86523, 'distance_accuracy_value', 'NONE');
#34408=CARTESIAN_POINT ( 'NONE',  ( 14.98958921077330508, 2.030821136742458233, -0.4231615532927078260 ) ) ;
#34450=CARTESIAN_POINT ( 'NONE',  ( 6.075240630612074533, 10.96939156344817690, -3.485377474036338352 ) ) ;
#34462=CARTESIAN_POINT ( 'NONE',  ( 16.01731991114695575, 3.900112512635703244, 1.615757124600548433 ) ) ;
#34519=CARTESIAN_POINT ( 'NONE',  ( 16.07816244837400177, 5.101897851402082296, 4.232350007277328352 ) ) ;
#34521=CARTESIAN_POINT ( 'NONE',  ( 13.76825510980707001, 22.95345116768091742, 1.005136556262091307 ) ) ;
#34561=CARTESIAN_POINT ( 'NONE',  ( -12.03221859608693833, 21.77027319522744619, -7.001194585145907645 ) ) ;
#34576=EDGE_LOOP ( 'NONE', ( #59236, #56673, #25282 ) ) ;
#34585=DIRECTION ( 'NONE',  ( 0.000000000000000000, 0.000000000000000000, -1.000000000000000000 ) ) ;
#34620=EDGE_CURVE ( 'NONE', #93549, #27771, #96485, .T. ) ;
#34699=( NAMED_UNIT ( * ) PLANE_ANGLE_UNIT ( ) SI_UNIT ( $, .RADIAN. ) );
#34700=CIRCLE ( 'NONE', #79473, 2.000000000000000000 ) ;
#34872=ORIENTED_EDGE ( 'NONE', *, *, #106185, .T. ) ;
#34894=UNCERTAINTY_MEASURE_WITH_UNIT (LENGTH_MEASURE( 1.000000000000000082E-05 ), #91410, 'distance_accuracy_value', 'NONE');
#34935=CARTESIAN_POINT ( 'NONE',  ( 14.84861631010743999, 2.245468665773563632, -2.074511027864127222 ) ) ;
#34939=CARTESIAN_POINT ( 'NONE',  ( 20.00000000000000000, 12.99999999999999289, 0.000000000000000000 ) ) ;
#34953=EDGE_CURVE ( 'NONE', #93240, #82573, #25291, .T. ) ;
#34983=FILL_AREA_STYLE_COLOUR ( '', #71797 ) ;
#34987=CARTESIAN_POINT ( 'NONE',  ( 15.12883458092736788, 3.606451457941568517, 4.265946247307269346 ) ) ;
#35045=CARTESIAN_POINT ( 'NONE',  ( 14.81649318718688235, 22.00128301469023384, 4.391045811938269594 ) ) ;
#35085=CARTESIAN_POINT ( 'NONE',  ( -13.26885379642688889, 24.19022360890687651, -3.253372505828892702 ) ) ;
#35099=SURFACE_SIDE_STYLE ('',( #84152 ) ) ;
#35107=DIRECTION ( 'NONE',  ( 0.000000000000000000, 0.000000000000000000, 1.000000000000000000 ) ) ;
#35147=DIRECTION ( 'NONE',  ( 1.000000000000000000, -0.000000000000000000, -0.000000000000000000 ) ) ;
#35158=FILL_AREA_STYLE_COLOUR ( '', #69693 ) ;
#35224=SURFACE_STYLE_USAGE ( .BOTH. , #42752 ) ;
#35241=ADVANCED_FACE ( 'NONE', ( #28905 ), #19916, .T. ) ;
#35271=SURFACE_SIDE_STYLE ('',( #701 ) ) ;
#35367=CARTESIAN_POINT ( 'NONE',  ( -14.98958921077340456, 2.030821136742817945, 0.4231615533124187256 ) ) ;
#35450=STYLED_ITEM ( 'NONE', ( #92967 ), #9284 ) ;
#35471=CARTESIAN_POINT ( 'NONE',  ( 14.84237598262652646, 1.406801708889429348, 2.172554589314652063 ) ) ;
#35476=DIRECTION ( 'NONE',  ( 1.000000000000000000, 0.000000000000000000, 0.000000000000000000 ) ) ;
#35483=ORIENTED_EDGE ( 'NONE', *, *, #22418, .F. ) ;
#35503=EDGE_CURVE ( 'NONE', #97818, #39874, #48421, .T. ) ;
#35505=CARTESIAN_POINT ( 'NONE',  ( 6.999768563658489207, 9.000405013899001716, -0.2746924679829751414 ) ) ;
#35578=CARTESIAN_POINT ( 'NONE',  ( 10.62194528067082189, 14.25751096852423494, 9.925505253905029690 ) ) ;
#35621=DIRECTION ( 'NONE',  ( -1.000000000000000000, -0.000000000000000000, -0.000000000000000000 ) ) ;
#35624=CARTESIAN_POINT ( 'NONE',  ( -11.87699017361764753, 16.68016500116531020, 9.302345733532593641 ) ) ;
#35754=( GEOMETRIC_REPRESENTATION_CONTEXT ( 3 ) GLOBAL_UNCERTAINTY_ASSIGNED_CONTEXT ( ( #19269 ) ) GLOBAL_UNIT_ASSIGNED_CONTEXT ( ( #67332, #102341, #101290 ) ) REPRESENTATION_CONTEXT ( 'NONE', 'WORKASPACE' ) );
#35847=DIRECTION ( 'NONE',  ( -1.000000000000000000, 0.000000000000000000, 0.000000000000000000 ) ) ;
#35911=CARTESIAN_POINT ( 'NONE',  ( -14.90069340504740758, 2.164550790749281362, 1.672538227389957166 ) ) ;
#35914=CARTESIAN_POINT ( 'NONE',  ( -15.72426027928782588, 22.05433369633805896, -3.882282778265964129 ) ) ;
#35929=( NAMED_UNIT ( * ) PLANE_ANGLE_UNIT ( ) SI_UNIT ( $, .RADIAN. ) );
#35990=SURFACE_STYLE_FILL_AREA ( #18735 ) ;
#36090=COLOUR_RGB ( '', 0.40784314, 0.44705882, 0.49803922) ;
#36123=CARTESIAN_POINT ( 'NONE',  ( 12.15267230755900663, 17.47167679243762350, 8.961506924172995880 ) ) ;
#36166=CARTESIAN_POINT ( 'NONE',  ( -10.06395418932315167, 12.92917864820601892, 10.57395537501041183 ) ) ;
#36175=FACE_OUTER_BOUND ( 'NONE', #40909, .T. ) ;
#36206=ORIENTED_EDGE ( 'NONE', *, *, #84741, .F. ) ;
#36250=CARTESIAN_POINT ( 'NONE',  ( 13.92920313560041023, 2.720439590250280482, -5.536316934251884980 ) ) ;
#36287=( NAMED_UNIT ( * ) PLANE_ANGLE_UNIT ( ) SI_UNIT ( $, .RADIAN. ) );
#36323=EDGE_CURVE ( 'NONE', #19141, #53038, #104395, .T. ) ;
#36332=COLOUR_RGB ( '', 0.08235294, 0.09019608, 0.10196078) ;
#36343=EDGE_LOOP ( 'NONE', ( #102268, #33057, #17138, #67246 ) ) ;
#36393=CARTESIAN_POINT ( 'NONE',  ( -13.07716338512343590, 8.367404540816639980, -8.868549848999556673 ) ) ;
#36399=SURFACE_SIDE_STYLE ('',( #3453 ) ) ;
#36460=( LENGTH_UNIT ( ) NAMED_UNIT ( * ) SI_UNIT ( .MILLI., .METRE. ) );
#36501=UNCERTAINTY_MEASURE_WITH_UNIT (LENGTH_MEASURE( 1.000000000000000082E-05 ), #82971, 'distance_accuracy_value', 'NONE');
#36506=CARTESIAN_POINT ( 'NONE',  ( -14.58597127886929101, 5.499146323188746521, 6.679532531467523349 ) ) ;
#36511=CARTESIAN_POINT ( 'NONE',  ( -13.92190297528754783, 2.732557955353745349, -5.556343985222209625 ) ) ;
#36541=CARTESIAN_POINT ( 'NONE',  ( -5.763898627153208665, 12.46274061085392759, -3.972597389303859750 ) ) ;
#36550=SURFACE_STYLE_USAGE ( .BOTH. , #2530 ) ;
#36591=FILL_AREA_STYLE ('',( #34983 ) ) ;
#36598=( NAMED_UNIT ( * ) SI_UNIT ( $, .STERADIAN. ) SOLID_ANGLE_UNIT ( ) );
#36634=AXIS2_PLACEMENT_3D ( 'NONE', #5754, #5237, #62417 ) ;
#36651=CARTESIAN_POINT ( 'NONE',  ( 10.06130352118416660, 12.96572514657750474, 10.57352155064043231 ) ) ;
#36665=B_SPLINE_CURVE_WITH_KNOTS ( 'NONE', 3,
 ( #69780, #12581, #29875, #54095, #37975, #85982, #21782, #3447, #95648, #102671, #20749, #102131, #77336, #103728, #46035, #45514, #79447, #94602, #94048, #61709, #37441, #62752, #87038, #70836, #12055, #54616, #36393, #87558, #63282, #44440 ),
 .UNSPECIFIED., .F., .F.,
 ( 4, 2, 2, 2, 2, 2, 2, 2, 2, 2, 2, 2, 2, 2, 4 ),
 ( 0.02276231911146334164, 0.02503730341472417895, 0.02617479556635459934, 0.02731228771798501972, 0.02844977986961544011, 0.02958727202124586050, 0.03186225632450671863, 0.03243100240032192882, 0.03299974847613713902, 0.03413724062776756635, 0.03527473277939799368, 0.03641222493102841407, 0.03754971708265884139, 0.03868720923428926872, 0.04096219353755012338 ),
 .UNSPECIFIED. ) ;
#36694=CARTESIAN_POINT ( 'NONE',  ( -14.80696975987319242, 21.98616633791558783, 4.396263791233566920 ) ) ;
#36706=( GEOMETRIC_REPRESENTATION_CONTEXT ( 3 ) GLOBAL_UNCERTAINTY_ASSIGNED_CONTEXT ( ( #39469 ) ) GLOBAL_UNIT_ASSIGNED_CONTEXT ( ( #96381, #45693, #31131 ) ) REPRESENTATION_CONTEXT ( 'NONE', 'WORKASPACE' ) );
#36707=DIRECTION ( 'NONE',  ( 5.378903587909331904E-13, -0.5626279437274303019, 0.8267102254944252993 ) ) ;
#36775=CARTESIAN_POINT ( 'NONE',  ( 13.02702147844135716, 6.134201042431408624, -7.309633161561180259 ) ) ;
#36808=FACE_OUTER_BOUND ( 'NONE', #100858, .T. ) ;
#36917=CARTESIAN_POINT ( 'NONE',  ( 15.79785611713298366, 22.78916061418795636, -0.5147589528736694620 ) ) ;
#36953=B_SPLINE_CURVE_WITH_KNOTS ( 'NONE', 3,
 ( #37439, #31463, #62750, #21254 ),
 .UNSPECIFIED., .F., .F.,
 ( 4, 4 ),
 ( 0.02698643027831515440, 0.9670246242088337274 ),
 .UNSPECIFIED. ) ;
#36967=CARTESIAN_POINT ( 'NONE',  ( -16.14595037837264968, 20.48388002475744685, -4.555408037181266856 ) ) ;
#36988=CARTESIAN_POINT ( 'NONE',  ( 11.78635468501824057, 6.776294004930349502, 9.084523618773719278 ) ) ;
#37019=EDGE_LOOP ( 'NONE', ( #61203, #50798, #39742, #30152 ) ) ;
#37088=MECHANICAL_DESIGN_GEOMETRIC_PRESENTATION_REPRESENTATION('',(#52579),#105934);
#37128=CARTESIAN_POINT ( 'NONE',  ( 0.000000000000000000, 34.00000000000000000, -8.000000000000000000 ) ) ;
#37174=CARTESIAN_POINT ( 'NONE',  ( 14.09641130086054872, 20.98415506194422164, 6.027230611388303849 ) ) ;
#37211=CARTESIAN_POINT ( 'NONE',  ( -12.60023245287857740, 22.92871684446009439, 5.621329045441238570 ) ) ;
#37299=SURFACE_STYLE_USAGE ( .BOTH. , #94991 ) ;
#37313=VERTEX_POINT ( 'NONE', #49554 ) ;
#37328=EDGE_CURVE ( 'NONE', #17545, #51169, #81910, .T. ) ;
#37333=MECHANICAL_DESIGN_GEOMETRIC_PRESENTATION_REPRESENTATION('',(#7945),#32145);
#37355=ORIENTED_EDGE ( 'NONE', *, *, #48252, .T. ) ;
#37405=( NAMED_UNIT ( * ) PLANE_ANGLE_UNIT ( ) SI_UNIT ( $, .RADIAN. ) );
#37410=( NAMED_UNIT ( * ) SI_UNIT ( $, .STERADIAN. ) SOLID_ANGLE_UNIT ( ) );
#37439=CARTESIAN_POINT ( 'NONE',  ( 0.000000000000000000, 34.19642918197134662, -12.16579798332631945 ) ) ;
#37441=CARTESIAN_POINT ( 'NONE',  ( -11.79370259999046411, 11.30362766250548034, -9.861606943826988214 ) ) ;
#37449=CARTESIAN_POINT ( 'NONE',  ( 16.12871211736549881, 21.28428926968472723, 2.982820907299407853 ) ) ;
#37466=CARTESIAN_POINT ( 'NONE',  ( 14.90280835358713318, 2.161282233155129795, 1.653369514896020576 ) ) ;
#37504=CARTESIAN_POINT ( 'NONE',  ( -14.66373388272641520, 22.41296547519206328, 3.537915336770097952 ) ) ;
#37521=ORIENTED_EDGE ( 'NONE', *, *, #101178, .F. ) ;
#37524=CARTESIAN_POINT ( 'NONE',  ( 10.37426823381935570, 10.87037927388256087, 10.42851533226476235 ) ) ;
#37568=B_SPLINE_CURVE_WITH_KNOTS ( 'NONE', 3,
 ( #10835, #93911, #100926, #61024, #18998, #20614, #68587, #68032, #101470, #44844, #93388, #92293, #52916, #27622, #51302, #84223 ),
 .UNSPECIFIED., .F., .F.,
 ( 4, 2, 2, 2, 2, 2, 2, 4 ),
 ( 0.000000000000000000, 0.002625638288314691149, 0.003938457432472034989, 0.004594867004550707776, 0.005251276576629379696, 0.006564095720786724403, 0.007876914864944068242, 0.01050255315325875766 ),
 .UNSPECIFIED. ) ;
#37571=CARTESIAN_POINT ( 'NONE',  ( -11.38602198108772434, 20.27704874433871396, -8.239207418153725371 ) ) ;
#37600=EDGE_CURVE ( 'NONE', #87833, #43519, #49406, .T. ) ;
#37638=FACE_OUTER_BOUND ( 'NONE', #5043, .T. ) ;
#37641=CARTESIAN_POINT ( 'NONE',  ( 5.744562646538028616, 12.99999999999999289, 4.000000000000000000 ) ) ;
#37644=( BOUNDED_SURFACE ( )  B_SPLINE_SURFACE ( 3, 2, ( 
 ( #77393, #77926, #100593 ),
 ( #36967, #26752, #102733 ),
 ( #60696, #28892, #20807 ),
 ( #11041, #35914, #12635 ),
 ( #68786, #101667, #92499 ),
 ( #75791, #59629, #68239 ),
 ( #56265, #46092, #87617 ),
 ( #88668, #63349, #104854 ),
 ( #47659, #95700, #55220 ),
 ( #80555, #96249, #6140 ),
 ( #72476, #30455, #71407 ),
 ( #47132, #38542, #104305 ),
 ( #21312, #29924, #78977 ),
 ( #13701, #39603, #54149 ),
 ( #46612, #89202, #80027 ),
 ( #79509, #70891, #37504 ),
 ( #22375, #39069, #88146 ),
 ( #71950, #87089, #105382 ),
 ( #5619, #30997, #62290 ),
 ( #31521, #14226, #95180 ) ),
 .UNSPECIFIED., .F., .F., .T. ) 
 B_SPLINE_SURFACE_WITH_KNOTS ( ( 4, 2, 2, 2, 2, 2, 2, 2, 2, 4 ),
 ( 3, 3 ),
 ( 3.184952301893417825E-15, 0.001208125624086961360, 0.002416251248170737768, 0.003624376872254514177, 0.004832502496338290585, 0.005436565308380179005, 0.006040628120422067426, 0.007248753744505843401, 0.008456879368589619375, 0.009665004992673396217 ),
 ( 0.000000000000000000, 1.000000000000000000 ),
 .UNSPECIFIED. ) 
 GEOMETRIC_REPRESENTATION_ITEM ( )  RATIONAL_B_SPLINE_SURFACE ( (
 ( 1.000000000000000000, 0.8291561975880743507, 1.000000000000000000),
 ( 1.000000000000000000, 0.8411444448774373361, 1.000000000000000000),
 ( 1.000000000000000000, 0.8513107778592109431, 1.000000000000000000),
 ( 1.000000000000000000, 0.8686991428040923280, 1.000000000000000000),
 ( 1.000000000000000000, 0.8759367825447341716, 1.000000000000000000),
 ( 1.000000000000000000, 0.8878384569986785824, 1.000000000000000000),
 ( 1.000000000000000000, 0.8925163270234079960, 1.000000000000000000),
 ( 1.000000000000000000, 0.8988019894165557577, 1.000000000000000000),
 ( 1.000000000000000000, 0.9004488336118289249, 1.000000000000000000),
 ( 1.000000000000000000, 0.9004787869545520795, 1.000000000000000000),
 ( 1.000000000000000000, 0.9000741598243899855, 1.000000000000000000),
 ( 1.000000000000000000, 0.8984769429442731603, 1.000000000000000000),
 ( 1.000000000000000000, 0.8972871579692907051, 1.000000000000000000),
 ( 1.000000000000000000, 0.8926126616870123653, 1.000000000000000000),
 ( 1.000000000000000000, 0.8880148073974446499, 1.000000000000000000),
 ( 1.000000000000000000, 0.8760712452968238972, 1.000000000000000000),
 ( 1.000000000000000000, 0.8688049777777138161, 1.000000000000000000),
 ( 1.000000000000000000, 0.8513604698959409411, 1.000000000000000000),
 ( 1.000000000000000000, 0.8411660073561874063, 1.000000000000000000),
 ( 1.000000000000000000, 0.8291561975891263980, 1.000000000000000000) ) ) 
 REPRESENTATION_ITEM ( '' )  SURFACE ( )  );
#37653=CARTESIAN_POINT ( 'NONE',  ( 15.86714682456667092, 3.932109987699209164, -3.945841262946509609 ) ) ;
#37710=CARTESIAN_POINT ( 'NONE',  ( -16.03934073995868204, 4.450581328283826466, 3.145353196842342935 ) ) ;
#37715=CARTESIAN_POINT ( 'NONE',  ( 10.07739987653159908, 15.02570658418118121, 10.37755588292369247 ) ) ;
#37753=CARTESIAN_POINT ( 'NONE',  ( -10.60777364585932681, 14.22653809302268080, 9.944243933998073715 ) ) ;
#37767=CYLINDRICAL_SURFACE ( 'NONE', #22100, 4.000000000000000000 ) ;
#37830=CARTESIAN_POINT ( 'NONE',  ( -6.879475648205854554, 16.78609259491953409, 1.316666052250859753 ) ) ;
#37834=CARTESIAN_POINT ( 'NONE',  ( 13.35126306661430995, 5.573441611265049112, -6.725115378757728912 ) ) ;
#37853=DIRECTION ( 'NONE',  ( -1.000000000000000000, -0.000000000000000000, -0.000000000000000000 ) ) ;
#37871=SURFACE_STYLE_USAGE ( .BOTH. , #4939 ) ;
#37877=CARTESIAN_POINT ( 'NONE',  ( 14.46738925856536540, 21.80453881764446322, -4.782842684419118306 ) ) ;
#37938=EDGE_CURVE ( 'NONE', #16303, #87076, #83993, .T. ) ;
#37975=CARTESIAN_POINT ( 'NONE',  ( -13.12019779049608026, 19.43057441571500377, -7.665946815556264227 ) ) ;
#37983=CARTESIAN_POINT ( 'NONE',  ( 16.10155139016696069, 21.86297139503093589, 0.4316986452390899065 ) ) ;
#38053=CARTESIAN_POINT ( 'NONE',  ( 13.25615415199737335, 3.883583888817405239, 6.949209056975313992 ) ) ;
#38058=MECHANICAL_DESIGN_GEOMETRIC_PRESENTATION_REPRESENTATION('',(#51779),#65574);
#38096=CARTESIAN_POINT ( 'NONE',  ( -12.49438147519285813, 22.71955599834702966, -5.903923697086765898 ) ) ;
#38132=AXIS2_PLACEMENT_3D ( 'NONE', #64543, #74204, #8943 ) ;
#38152=CARTESIAN_POINT ( 'NONE',  ( 11.52978300598590700, 12.35134215813147485, -9.999999999999882760 ) ) ;
#38168=ADVANCED_FACE ( 'NONE', ( #73438 ), #41621, .F. ) ;
#38174=CIRCLE ( 'NONE', #19261, 1.999999999999999556 ) ;
#38176=CIRCLE ( 'NONE', #98425, 2.000000000000000000 ) ;
#38231=CARTESIAN_POINT ( 'NONE',  ( 10.51501260721461151, 10.28692437246665214, 10.32948041498278435 ) ) ;
#38348=CARTESIAN_POINT ( 'NONE',  ( -7.000111909206518490, 17.00019584125958616, -0.1284026198027884702 ) ) ;
#38353=CARTESIAN_POINT ( 'NONE',  ( 15.04093380808766867, 5.422855115928403968, -6.531324706886918463 ) ) ;
#38390=SURFACE_STYLE_USAGE ( .BOTH. , #15668 ) ;
#38396=CARTESIAN_POINT ( 'NONE',  ( -10.81758598141882644, 16.04212470968489868, -9.532093978217352159 ) ) ;
#38494=CARTESIAN_POINT ( 'NONE',  ( 15.79700980112376918, 22.78020937716664562, 0.4986931010921795693 ) ) ;
#38541=DIRECTION ( 'NONE',  ( -1.000000000000000000, -0.000000000000000000, -0.000000000000000000 ) ) ;
#38542=CARTESIAN_POINT ( 'NONE',  ( -15.79338834186285290, 22.74219270459669318, 1.000334277921258508 ) ) ;
#38595=UNCERTAINTY_MEASURE_WITH_UNIT (LENGTH_MEASURE( 1.000000000000000082E-05 ), #3642, 'distance_accuracy_value', 'NONE');
#38609=CARTESIAN_POINT ( 'NONE',  ( -12.84988518786640199, 23.41409974762299484, 4.906243843517776426 ) ) ;
#38634=AXIS2_PLACEMENT_3D ( 'NONE', #89966, #72710, #39311 ) ;
#38642=VERTEX_POINT ( 'NONE', #76524 ) ;
#38728=CARTESIAN_POINT ( 'NONE',  ( -29.87930712590254245, 10.71892156097790583, 14.93965356295128011 ) ) ;
#38739=CARTESIAN_POINT ( 'NONE',  ( -16.03926360544215157, 4.449054639247318477, -3.142406330834766948 ) ) ;
#38743=CARTESIAN_POINT ( 'NONE',  ( 12.55213272931464275, 5.188451237610401279, 8.093010545847016957 ) ) ;
#38764=UNCERTAINTY_MEASURE_WITH_UNIT (LENGTH_MEASURE( 1.000000000000000082E-05 ), #93981, 'distance_accuracy_value', 'NONE');
#38785=CARTESIAN_POINT ( 'NONE',  ( -14.78804146188508462, 5.762582778709502307, 6.905855753343613124 ) ) ;
#38797=EDGE_CURVE ( 'NONE', #27771, #93549, #20387, .T. ) ;
#38838=CARTESIAN_POINT ( 'NONE',  ( 6.559876275494352704, 16.16983035391954360, -2.453497130494365575 ) ) ;
#38860=CARTESIAN_POINT ( 'NONE',  ( -5.919343243681499445, 14.43244923957804460, -3.736960138817876143 ) ) ;
#38864=CARTESIAN_POINT ( 'NONE',  ( 10.64742384531193942, 14.88071023319941411, -9.840650288117007705 ) ) ;
#38914=CARTESIAN_POINT ( 'NONE',  ( -12.35636350804288774, 17.94545210593157236, -8.708632758017785136 ) ) ;
#38932=CARTESIAN_POINT ( 'NONE',  ( 16.14595037822608603, 7.274337365584590209, -6.616591826375515240 ) ) ;
#39003=DIRECTION ( 'NONE',  ( 0.000000000000000000, 0.000000000000000000, -1.000000000000000000 ) ) ;
#39011=CARTESIAN_POINT ( 'NONE',  ( -15.90328822607555281, 3.524689239577517341, 2.889827284417966435 ) ) ;
#39013=CARTESIAN_POINT ( 'NONE',  ( 15.66340762197770786, 21.48519827103249469, 5.204287273250217893 ) ) ;
#39016=DIRECTION ( 'NONE',  ( -8.566042448110249984E-17, -0.7561819230143457249, 0.6543614439331877364 ) ) ;
#39019=EDGE_CURVE ( 'NONE', #25504, #24752, #22107, .T. ) ;
#39026=CARTESIAN_POINT ( 'NONE',  ( 14.24976063295490825, 2.188309765130968199, -4.656908667353339304 ) ) ;
#39069=CARTESIAN_POINT ( 'NONE',  ( -15.72449985194402977, 22.05660461081803803, 3.876398783261274961 ) ) ;
#39075=COLOUR_RGB ( '', 0.31764706, 0.68627451, 0.89019608) ;
#39076=B_SPLINE_CURVE_WITH_KNOTS ( 'NONE', 3,
 ( #55124, #80464, #31435, #47038, #79937, #30903 ),
 .UNSPECIFIED., .F., .F.,
 ( 4, 2, 4 ),
 ( 0.000000000000000000, 0.001916782365109770663, 0.003833564730219541326 ),
 .UNSPECIFIED. ) ;
#39091=CARTESIAN_POINT ( 'NONE',  ( 11.90699106250066741, 6.512150199977177145, 8.940599429151134814 ) ) ;
#39103=CARTESIAN_POINT ( 'NONE',  ( -13.24448459474634809, 8.079006937257503296, 8.710096806171129913 ) ) ;
#39166=CARTESIAN_POINT ( 'NONE',  ( -6.013035130119651406, 11.20840185166977498, 3.585725784831610419 ) ) ;
#39176=AXIS2_PLACEMENT_3D ( 'NONE', #649, #8779, #41685 ) ;
#39191=CARTESIAN_POINT ( 'NONE',  ( 13.09294039136050181, 8.329457025090279743, -8.860870387164958117 ) ) ;
#39280=CARTESIAN_POINT ( 'NONE',  ( 13.95195489779432307, 6.945883722228267665, 7.976544621831442861 ) ) ;
#39311=DIRECTION ( 'NONE',  ( 0.000000000000000000, 0.000000000000000000, 1.000000000000000000 ) ) ;
#39323=CARTESIAN_POINT ( 'NONE',  ( 16.05785784214673129, 4.775831776474256607, -3.710403933782447261 ) ) ;
#39332=SURFACE_STYLE_FILL_AREA ( #6396 ) ;
#39400=CARTESIAN_POINT ( 'NONE',  ( 12.35050418871243139, 20.41302141647243573, -6.749052883688374749 ) ) ;
#39449=CARTESIAN_POINT ( 'NONE',  ( -11.50180495297654204, 15.06797554620490232, -9.787940426045702580 ) ) ;
#39460=CARTESIAN_POINT ( 'NONE',  ( -14.59561887822985327, 1.699647480229564245, 3.448601310208504689 ) ) ;
#39469=UNCERTAINTY_MEASURE_WITH_UNIT (LENGTH_MEASURE( 1.000000000000000082E-05 ), #96381, 'distance_accuracy_value', 'NONE');
#39519=AXIS2_PLACEMENT_3D ( 'NONE', #1501, #52188, #67336 ) ;
#39526=MECHANICAL_DESIGN_GEOMETRIC_PRESENTATION_REPRESENTATION('',(#25784),#3396);
#39532=DIRECTION ( 'NONE',  ( 0.000000000000000000, 0.000000000000000000, -1.000000000000000000 ) ) ;
#39548=CARTESIAN_POINT ( 'NONE',  ( -15.46466052604883323, 2.715844537113373924, 1.564829471106392145 ) ) ;
#39603=CARTESIAN_POINT ( 'NONE',  ( -15.77996175643155929, 22.60291536984139071, 1.987376761536549408 ) ) ;
#39637=CARTESIAN_POINT ( 'NONE',  ( -13.68990076057127148, 7.343638245770522488, 8.266402366871409058 ) ) ;
#39650=VERTEX_POINT ( 'NONE', #26461 ) ;
#39657=ORIENTED_EDGE ( 'NONE', *, *, #27246, .F. ) ;
#39681=ORIENTED_EDGE ( 'NONE', *, *, #98301, .F. ) ;
#39742=ORIENTED_EDGE ( 'NONE', *, *, #97591, .T. ) ;
#39774=( NAMED_UNIT ( * ) SI_UNIT ( $, .STERADIAN. ) SOLID_ANGLE_UNIT ( ) );
#39779=CARTESIAN_POINT ( 'NONE',  ( 16.11737681246577480, 21.56249621366840330, -2.179529459261059898 ) ) ;
#39794=ORIENTED_EDGE ( 'NONE', *, *, #104553, .F. ) ;
#39845=CARTESIAN_POINT ( 'NONE',  ( -11.57142077548166093, 7.251212190646564082, 9.335706481127813205 ) ) ;
#39874=VERTEX_POINT ( 'NONE', #39323 ) ;
#39922=CARTESIAN_POINT ( 'NONE',  ( 10.18861149534500932, 16.01981654604731986, -10.17146396841989109 ) ) ;
#39957=CARTESIAN_POINT ( 'NONE',  ( 14.89763918506130835, 1.348991191049166538, 1.758109506431186686 ) ) ;
#39967=CARTESIAN_POINT ( 'NONE',  ( -11.09180518623727529, 10.57614021777674118, -9.722244198893070788 ) ) ;
#39969=FACE_OUTER_BOUND ( 'NONE', #13240, .T. ) ;
#39978=CARTESIAN_POINT ( 'NONE',  ( -15.22818746202677787, 3.929489829936595235, 4.609438620834709788 ) ) ;
#39987=CARTESIAN_POINT ( 'NONE',  ( 16.14595037822607182, 6.785770140112303395, -6.193810554583006223 ) ) ;
#40029=CARTESIAN_POINT ( 'NONE',  ( -13.46456120603693662, 20.01150154851706020, 7.140757873385461529 ) ) ;
#40046=DIRECTION ( 'NONE',  ( 1.000000000000000000, 0.000000000000000000, 0.000000000000000000 ) ) ;
#40060=( NAMED_UNIT ( * ) PLANE_ANGLE_UNIT ( ) SI_UNIT ( $, .RADIAN. ) );
#40076=CARTESIAN_POINT ( 'NONE',  ( -14.29190075645216851, 12.99999999999999289, 0.000000000000000000 ) ) ;
#40200=CARTESIAN_POINT ( 'NONE',  ( -5.763828452502798072, 12.46312952775077676, 3.972702736835262982 ) ) ;
#40215=B_SPLINE_CURVE_WITH_KNOTS ( 'NONE', 3,
 ( #98520, #24666, #23607, #39779, #24148, #65634, #90440, #105036, #56992, #16549, #49434, #56458, #48373, #81266, #8451, #74245 ),
 .UNSPECIFIED., .F., .F.,
 ( 4, 2, 2, 2, 2, 2, 2, 4 ),
 ( 0.000000000000000000, 0.002612557234031565555, 0.003918835851047347031, 0.005225114468063129375, 0.005878253776571019246, 0.006531393085078909984, 0.007837671702094688858, 0.01045022893612624661 ),
 .UNSPECIFIED. ) ;
#40236=CARTESIAN_POINT ( 'NONE',  ( 12.02599986777602048, 10.59850526615580257, 9.713964925274206408 ) ) ;
#40272=ADVANCED_FACE ( 'NONE', ( #11975 ), #68094, .F. ) ;
#40320=CARTESIAN_POINT ( 'NONE',  ( 12.30282354285915680, 5.677685097715426288, 8.440510770982715627 ) ) ;
#40356=CARTESIAN_POINT ( 'NONE',  ( -11.51709745524291684, 12.46548236075430260, 10.00164875338921178 ) ) ;
#40364=TOROIDAL_SURFACE ( 'NONE', #38634, 7.999999999999998224, 2.000000000000000000 ) ;
#40367=( NAMED_UNIT ( * ) PLANE_ANGLE_UNIT ( ) SI_UNIT ( $, .RADIAN. ) );
#40440=CARTESIAN_POINT ( 'NONE',  ( 11.42547868101649655, 20.37551526749874142, -8.168836983366716709 ) ) ;
#40451=ORIENTED_EDGE ( 'NONE', *, *, #65720, .T. ) ;
#40476=EDGE_CURVE ( 'NONE', #47808, #87076, #99193, .T. ) ;
#40486=CARTESIAN_POINT ( 'NONE',  ( -10.93260317179502472, 11.17563650224738403, -9.852957799267798578 ) ) ;
#40490=AXIS2_PLACEMENT_3D ( 'NONE', #57519, #82343, #6855 ) ;
#40498=COLOUR_RGB ( '', 0.31764706, 0.68627451, 0.89019608) ;
#40503=CARTESIAN_POINT ( 'NONE',  ( 12.95110512856954443, 19.14606607232447999, -7.926761694102399503 ) ) ;
#40527=CARTESIAN_POINT ( 'NONE',  ( -14.44581512915354615, 5.963299184995717539, -7.135127315210193721 ) ) ;
#40570=CARTESIAN_POINT ( 'NONE',  ( -13.55583764533404612, 24.70617620989347074, -1.273591148780106153 ) ) ;
#40587=CARTESIAN_POINT ( 'NONE',  ( -16.01236629286567492, 3.722328191965275312, 0.3359674916118658983 ) ) ;
#40598=CARTESIAN_POINT ( 'NONE',  ( 19.50000000000000000, 12.99999999999999289, 6.999999999999999112 ) ) ;
#40602=CARTESIAN_POINT ( 'NONE',  ( -14.24907788157500121, 2.189443139868889165, -4.658781708030211632 ) ) ;
#40658=CARTESIAN_POINT ( 'NONE',  ( 13.70756188771709283, 3.094783711518300784, -6.047234902213228125 ) ) ;
#40718=DIRECTION ( 'NONE',  ( 0.000000000000000000, 1.000000000000000000, 0.000000000000000000 ) ) ;
#40734=ADVANCED_FACE ( 'NONE', ( #55476 ), #37767, .F. ) ;
#40793=ORIENTED_EDGE ( 'NONE', *, *, #3808, .F. ) ;
#40813=DIRECTION ( 'NONE',  ( 0.000000000000000000, 0.000000000000000000, 1.000000000000000000 ) ) ;
#40845=VERTEX_POINT ( 'NONE', #1367 ) ;
#40909=EDGE_LOOP ( 'NONE', ( #63316, #71351 ) ) ;
#40978=CARTESIAN_POINT ( 'NONE',  ( 11.60044415005657825, 15.63502551787816408, -9.650786643963554567 ) ) ;
#41019=MECHANICAL_DESIGN_GEOMETRIC_PRESENTATION_REPRESENTATION('',(#104769),#11744);
#41023=CARTESIAN_POINT ( 'NONE',  ( -13.42978829143733499, 24.48114154733749714, 2.381220245303011573 ) ) ;
#41037=COLOUR_RGB ( '', 0.31764706, 0.68627451, 0.89019608) ;
#41066=ADVANCED_FACE ( 'NONE', ( #93607 ), #101314, .T. ) ;
#41089=CARTESIAN_POINT ( 'NONE',  ( -12.95148853894511731, 19.13138155041741229, 7.909606116934300601 ) ) ;
#41109=CARTESIAN_POINT ( 'NONE',  ( -12.58006369834112625, 22.88893462671237344, 5.677102170468417697 ) ) ;
#41124=CARTESIAN_POINT ( 'NONE',  ( -15.94091178690226407, 3.082798537041112841, 0.3736180973001349548 ) ) ;
#41258=CIRCLE ( 'NONE', #30894, 6.999999999999999112 ) ;
#41264=CARTESIAN_POINT ( 'NONE',  ( -6.239770560962896617, 10.55575045314059501, 3.176762229947383886 ) ) ;
#41298=CARTESIAN_POINT ( 'NONE',  ( 13.59061921561113984, 7.494096743409553341, 8.374275364764086405 ) ) ;
#41369=ORIENTED_EDGE ( 'NONE', *, *, #39019, .T. ) ;
#41443=FILL_AREA_STYLE_COLOUR ( '', #18488 ) ;
#41447=CARTESIAN_POINT ( 'NONE',  ( 15.50996574327959721, 2.604740765349685461, -0.8136923573247164532 ) ) ;
#41500=CARTESIAN_POINT ( 'NONE',  ( 14.44581512912309229, 5.963299184987445933, 7.135127315203210863 ) ) ;
#41502=CARTESIAN_POINT ( 'NONE',  ( 13.67390614417971939, 22.79767714195904915, -2.033812096035475303 ) ) ;
#41548=CARTESIAN_POINT ( 'NONE',  ( -15.37715070606341072, 22.74015324434795460, -2.282816646031935459 ) ) ;
#41581=AXIS2_PLACEMENT_3D ( 'NONE', #74980, #56127, #89067 ) ;
#41621=CYLINDRICAL_SURFACE ( 'NONE', #92533, 4.000000000000000000 ) ;
#41670=TOROIDAL_SURFACE ( 'NONE', #89864, 11.18527996897366528, 1.000000000000000000 ) ;
#41685=DIRECTION ( 'NONE',  ( 0.000000000000000000, 0.000000000000000000, 1.000000000000000000 ) ) ;
#41693=( BOUNDED_SURFACE ( )  B_SPLINE_SURFACE ( 3, 2, ( 
 ( #30336, #80443, #97160 ),
 ( #6552, #7608, #88032 ),
 ( #72361, #65337, #71826 ),
 ( #23308, #79917, #89087 ),
 ( #6025, #31927, #40527 ),
 ( #14638, #89619, #15717 ) ),
 .UNSPECIFIED., .F., .F., .F. ) 
 B_SPLINE_SURFACE_WITH_KNOTS ( ( 4, 2, 4 ),
 ( 3, 3 ),
 ( -1.626303258728256651E-18, 0.001801542390204181844, 0.003603084780408365422 ),
 ( 0.000000000000000000, 1.000000000000000000 ),
 .UNSPECIFIED. ) 
 GEOMETRIC_REPRESENTATION_ITEM ( )  RATIONAL_B_SPLINE_SURFACE ( (
 ( 1.000000000000000000, 0.9115707425106669426, 1.000000000000000000),
 ( 1.000000000000000000, 0.9032011672211383013, 1.000000000000000000),
 ( 1.000000000000000000, 0.8933560653591404721, 1.000000000000000000),
 ( 1.000000000000000000, 0.8671388017650408786, 1.000000000000000000),
 ( 1.000000000000000000, 0.8506934603554324736, 1.000000000000000000),
 ( 1.000000000000000000, 0.8291561975888571689, 1.000000000000000000) ) ) 
 REPRESENTATION_ITEM ( '' )  SURFACE ( )  );
#41715=ORIENTED_EDGE ( 'NONE', *, *, #48345, .T. ) ;
#41722=CARTESIAN_POINT ( 'NONE',  ( 11.29173574096709309, 20.04892995410248702, -8.410943388600204074 ) ) ;
#41828=CARTESIAN_POINT ( 'NONE',  ( 12.59151156833761220, 9.285187046072287842, 9.290575386839268646 ) ) ;
#41891=AXIS2_PLACEMENT_3D ( 'NONE', #31911, #46103, #20817 ) ;
#41898=ORIENTED_EDGE ( 'NONE', *, *, #99066, .T. ) ;
#41916=PRESENTATION_STYLE_ASSIGNMENT (( #80776 ) ) ;
#41922=MECHANICAL_DESIGN_GEOMETRIC_PRESENTATION_REPRESENTATION('',(#526),#97121);
#42031=CARTESIAN_POINT ( 'NONE',  ( 16.14595037822608958, 7.274337365584589321, 6.616591826375514351 ) ) ;
#42033=CARTESIAN_POINT ( 'NONE',  ( 13.79123284555586082, 22.99122672343318285, 0.4943395215415997135 ) ) ;
#42057=ORIENTED_EDGE ( 'NONE', *, *, #63462, .T. ) ;
#42077=CARTESIAN_POINT ( 'NONE',  ( -12.53238701598708182, 20.76954288979780117, -6.334205635054888539 ) ) ;
#42204=CARTESIAN_POINT ( 'NONE',  ( 14.89104587296188242, 23.12241641510997070, 0.2537601492100622913 ) ) ;
#42215=DIRECTION ( 'NONE',  ( 0.000000000000000000, 0.000000000000000000, -1.000000000000000000 ) ) ;
#42260=PRESENTATION_STYLE_ASSIGNMENT (( #27191 ) ) ;
#42334=STYLED_ITEM ( 'NONE', ( #9522 ), #23472 ) ;
#42354=CARTESIAN_POINT ( 'NONE',  ( -14.90280835358831268, 2.161282233151506915, -1.653369514881387836 ) ) ;
#42411=MECHANICAL_DESIGN_GEOMETRIC_PRESENTATION_REPRESENTATION('',(#42334),#101001);
#42434=SURFACE_STYLE_USAGE ( .BOTH. , #68864 ) ;
#42442=ORIENTED_EDGE ( 'NONE', *, *, #25686, .F. ) ;
#42454=CARTESIAN_POINT ( 'NONE',  ( 15.45234973294653003, 2.833591715789641974, -2.076776216656130991 ) ) ;
#42476=MECHANICAL_DESIGN_GEOMETRIC_PRESENTATION_REPRESENTATION('',(#27215),#70056);
#42484=CARTESIAN_POINT ( 'NONE',  ( 0.000000000000000000, -3.035766082959412415E-15, 0.000000000000000000 ) ) ;
#42492=CARTESIAN_POINT ( 'NONE',  ( 6.321595794353348730, 10.35635176133114577, 3.012682989575210524 ) ) ;
#42558=CARTESIAN_POINT ( 'NONE',  ( 15.72218280906592369, 5.595371698624338919, 6.516822309427269033 ) ) ;
#42560=CARTESIAN_POINT ( 'NONE',  ( 13.59240052242509655, 24.77055383530022681, -0.6222571633745787034 ) ) ;
#42561=AXIS2_PLACEMENT_3D ( 'NONE', #30815, #22722, #72296 ) ;
#42590=( GEOMETRIC_REPRESENTATION_CONTEXT ( 3 ) GLOBAL_UNCERTAINTY_ASSIGNED_CONTEXT ( ( #59144 ) ) GLOBAL_UNIT_ASSIGNED_CONTEXT ( ( #11342, #26533, #93885 ) ) REPRESENTATION_CONTEXT ( 'NONE', 'WORKASPACE' ) );
#42592=ORIENTED_EDGE ( 'NONE', *, *, #21994, .T. ) ;
#42607=CARTESIAN_POINT ( 'NONE',  ( -12.32388454875233386, 22.37570981292809691, -6.328626427332589621 ) ) ;
#42634=CARTESIAN_POINT ( 'NONE',  ( -16.07917213302881621, 5.118112109480979832, 4.258304778710242822 ) ) ;
#42639=CARTESIAN_POINT ( 'NONE',  ( -15.43348245327105062, 2.792842261934127990, -2.002630087548765925 ) ) ;
#42662=CARTESIAN_POINT ( 'NONE',  ( 6.013174582917088173, 14.79219749984193477, 3.585507868043892987 ) ) ;
#42668=SURFACE_STYLE_FILL_AREA ( #2192 ) ;
#42752=SURFACE_SIDE_STYLE ('',( #72463 ) ) ;
#42774=CARTESIAN_POINT ( 'NONE',  ( 16.03934073995819531, 4.450581328273877979, -3.145353196822298969 ) ) ;
#42849=EDGE_CURVE ( 'NONE', #105603, #18398, #13468, .T. ) ;
#42890=CARTESIAN_POINT ( 'NONE',  ( -14.61305944212192109, 1.672740767017481422, -3.460733717101187157 ) ) ;
#42999=CARTESIAN_POINT ( 'NONE',  ( 15.51358515996928489, 2.608314655050632425, 0.4154586159794320666 ) ) ;
#43051=CARTESIAN_POINT ( 'NONE',  ( 15.50133110405595183, 2.625676835717284607, 0.7746791666779427876 ) ) ;
#43106=CARTESIAN_POINT ( 'NONE',  ( 13.32459112348717589, 24.29133014533524104, -2.966397270190748614 ) ) ;
#43120=CARTESIAN_POINT ( 'NONE',  ( 0.000000000000000000, 34.00000000000000000, 7.000000000000000000 ) ) ;
#43152=CARTESIAN_POINT ( 'NONE',  ( -12.93917161702704099, 23.58243205744838278, -4.610450678648994050 ) ) ;
#43177=CARTESIAN_POINT ( 'NONE',  ( -16.14595037822608603, 7.274337365578172232, 6.616591826369962348 ) ) ;
#43277=CARTESIAN_POINT ( 'NONE',  ( 14.29190075645216496, 21.26710225494213802, 5.626279437277409201 ) ) ;
#43282=CARTESIAN_POINT ( 'NONE',  ( 15.05785784214676326, 3.824195276769950969, 4.604276673498415740 ) ) ;
#43303=SURFACE_STYLE_USAGE ( .BOTH. , #27694 ) ;
#43369=COLOUR_RGB ( '', 0.40784314, 0.44705882, 0.49803922) ;
#43429=CARTESIAN_POINT ( 'NONE',  ( -15.51348069825386844, 2.608686647714169027, 0.4238655689775820967 ) ) ;
#43430=DIRECTION ( 'NONE',  ( -0.000000000000000000, -1.000000000000000000, -0.000000000000000000 ) ) ;
#43442=DIRECTION ( 'NONE',  ( -2.284277986162734315E-16, -0.7561819230143446147, 0.6543614439331888466 ) ) ;
#43448=( NAMED_UNIT ( * ) PLANE_ANGLE_UNIT ( ) SI_UNIT ( $, .RADIAN. ) );
#43451=CARTESIAN_POINT ( 'NONE',  ( 29.99397490504469133, 1.005902684993158047, 14.99698745252234033 ) ) ;
#43459=DIRECTION ( 'NONE',  ( -1.000000000000000000, 0.000000000000000000, 0.000000000000000000 ) ) ;
#43478=ORIENTED_EDGE ( 'NONE', *, *, #76419, .F. ) ;
#43492=DIRECTION ( 'NONE',  ( 0.000000000000000000, 0.000000000000000000, 1.000000000000000000 ) ) ;
#43519=VERTEX_POINT ( 'NONE', #132 ) ;
#43529=ADVANCED_FACE ( 'NONE', ( #33620 ), #58410, .T. ) ;
#43540=FACE_OUTER_BOUND ( 'NONE', #30381, .T. ) ;
#43572=DIRECTION ( 'NONE',  ( 0.000000000000000000, 0.000000000000000000, 1.000000000000000000 ) ) ;
#43573=CARTESIAN_POINT ( 'NONE',  ( 15.86692673747663918, 3.934633648118698979, 3.950574283723627733 ) ) ;
#43586=ORIENTED_EDGE ( 'NONE', *, *, #3073, .F. ) ;
#43632=CARTESIAN_POINT ( 'NONE',  ( 12.69126316887715689, 23.10611922033335119, -5.365485820795227845 ) ) ;
#43673=CARTESIAN_POINT ( 'NONE',  ( -12.78544757660326603, 21.24685875135632784, 5.680288811016952266 ) ) ;
#43686=SURFACE_STYLE_USAGE ( .BOTH. , #35099 ) ;
#43732=DIRECTION ( 'NONE',  ( 0.000000000000000000, 0.000000000000000000, -1.000000000000000000 ) ) ;
#43752=CARTESIAN_POINT ( 'NONE',  ( -5.887588022526042408, 14.31049540200681669, 3.788193301707003524 ) ) ;
#43766=COLOUR_RGB ( '', 0.72549020, 0.75294118, 0.79215686) ;
#43796=ORIENTED_EDGE ( 'NONE', *, *, #44441, .F. ) ;
#43881=( NAMED_UNIT ( * ) SI_UNIT ( $, .STERADIAN. ) SOLID_ANGLE_UNIT ( ) );
#43890=EDGE_LOOP ( 'NONE', ( #1304, #14528 ) ) ;
#43916=VERTEX_POINT ( 'NONE', #6522 ) ;
#43945=VERTEX_POINT ( 'NONE', #31896 ) ;
#43957=CARTESIAN_POINT ( 'NONE',  ( -15.50569080112025588, 2.636008032210750862, -0.8338155181678262862 ) ) ;
#43984=SURFACE_STYLE_USAGE ( .BOTH. , #94684 ) ;
#44028=CARTESIAN_POINT ( 'NONE',  ( -14.11595029532502643, 2.410436752314748521, -5.024000119269296682 ) ) ;
#44060=DIRECTION ( 'NONE',  ( -1.000000000000000000, 0.000000000000000000, 0.000000000000000000 ) ) ;
#44113=CARTESIAN_POINT ( 'NONE',  ( 15.85122647056153333, 4.114663126756291867, 4.288211754877272242 ) ) ;
#44174=CARTESIAN_POINT ( 'NONE',  ( 11.41053004416664862, 18.22558145230713578, 8.550477479386900725 ) ) ;
#44217=CARTESIAN_POINT ( 'NONE',  ( -11.40730658230364192, 14.19993524424377007, 9.944788788907292343 ) ) ;
#44296=EDGE_LOOP ( 'NONE', ( #7177, #55831, #71794, #7358 ) ) ;
#44299=( LENGTH_UNIT ( ) NAMED_UNIT ( * ) SI_UNIT ( .MILLI., .METRE. ) );
#44323=CIRCLE ( 'NONE', #27113, 8.000000000000000000 ) ;
#44384=SURFACE_STYLE_FILL_AREA ( #85371 ) ;
#44402=MECHANICAL_DESIGN_GEOMETRIC_PRESENTATION_REPRESENTATION('',(#11666),#32328);
#44403=CARTESIAN_POINT ( 'NONE',  ( -16.05785784214673484, 4.775831776474317891, -3.710403933782548513 ) ) ;
#44440=CARTESIAN_POINT ( 'NONE',  ( -14.29190075645216318, 6.456385560668112866, -7.561819230143454362 ) ) ;
#44441=EDGE_CURVE ( 'NONE', #93240, #1532, #12558, .T. ) ;
#44447=FACE_OUTER_BOUND ( 'NONE', #91662, .T. ) ;
#44449=CARTESIAN_POINT ( 'NONE',  ( 15.77996175643055565, 22.60291536983757155, 1.987376761556955307 ) ) ;
#44480=DIRECTION ( 'NONE',  ( 0.000000000000000000, -0.8267102254942136907, -0.5626279437277412754 ) ) ;
#44483=ADVANCED_FACE ( 'NONE', ( #8927 ), #19608, .T. ) ;
#44631=CLOSED_SHELL ( 'NONE', ( #32799, #52016, #18131, #67270, #23472, #101792, #40272, #61288, #8082, #9284, #100226, #51855, #78390, #35241, #38168, #5817, #29483, #66106, #44774, #99544, #80873, #55770, #105491, #54535, #61420, #13656, #17218, #69512, #46357, #47508, #50979, #45183, #29321, #86700, #95272, #44483, #43529, #12640, #40734, #85702, #33976, #79178, #25990, #79642, #7605, #28364, #41066, #20499, #205, #23974, #90878, #81053, #59293, #65971, #26207, #102887 ) ) ;
#44642=SURFACE_SIDE_STYLE ('',( #46223 ) ) ;
#44650=EDGE_CURVE ( 'NONE', #72252, #98070, #30838, .T. ) ;
#44657=CARTESIAN_POINT ( 'NONE',  ( 15.90404091944966325, 3.516460376327609882, 2.884095128131958674 ) ) ;
#44702=ORIENTED_EDGE ( 'NONE', *, *, #11082, .F. ) ;
#44714=CARTESIAN_POINT ( 'NONE',  ( 11.43762656160894764, 13.06896439115584663, 10.01660222353511109 ) ) ;
#44758=CARTESIAN_POINT ( 'NONE',  ( -13.51094462923033745, 20.09129127893359268, 7.071435863031892310 ) ) ;
#44774=ADVANCED_FACE ( 'NONE', ( #9188 ), #74983, .T. ) ;
#44834=UNCERTAINTY_MEASURE_WITH_UNIT (LENGTH_MEASURE( 1.000000000000000082E-05 ), #25951, 'distance_accuracy_value', 'NONE');
#44837=SURFACE_STYLE_FILL_AREA ( #2209 ) ;
#44844=CARTESIAN_POINT ( 'NONE',  ( -16.10103474921845645, 21.87197452378397600, -0.4486278773666070863 ) ) ;
#44915=DIRECTION ( 'NONE',  ( 0.000000000000000000, 0.000000000000000000, 1.000000000000000000 ) ) ;
#44976=CARTESIAN_POINT ( 'NONE',  ( -14.29190075645216851, 12.99999999999999289, 0.000000000000000000 ) ) ;
#44985=EDGE_LOOP ( 'NONE', ( #17275, #35483, #80714, #31581 ) ) ;
#44990=FILL_AREA_STYLE_COLOUR ( '', #68376 ) ;
#44992=CARTESIAN_POINT ( 'NONE',  ( 14.77180908113486346, 22.75028154196231611, 2.587654188261260924 ) ) ;
#44998=FILL_AREA_STYLE ('',( #55171 ) ) ;
#45040=CARTESIAN_POINT ( 'NONE',  ( 0.000000000000000000, -3.035766082959412415E-15, 0.000000000000000000 ) ) ;
#45063=CARTESIAN_POINT ( 'NONE',  ( 11.89035689955473885, 21.46281526437144649, 7.296656512214268808 ) ) ;
#45065=( NAMED_UNIT ( * ) PLANE_ANGLE_UNIT ( ) SI_UNIT ( $, .RADIAN. ) );
#45128=CIRCLE ( 'NONE', #48545, 8.000000000000000000 ) ;
#45174=FILL_AREA_STYLE ('',( #5749 ) ) ;
#45183=ADVANCED_FACE ( 'NONE', ( #59243 ), #73900, .T. ) ;
#45186=CARTESIAN_POINT ( 'NONE',  ( 15.05785784214675616, 3.824195276769981611, -4.604276673498455708 ) ) ;
#45188=DIRECTION ( 'NONE',  ( -0.000000000000000000, -1.000000000000000000, -0.000000000000000000 ) ) ;
#45245=CARTESIAN_POINT ( 'NONE',  ( 11.41582910567000830, 13.93800615581069380, 9.960141238938595265 ) ) ;
#45284=CARTESIAN_POINT ( 'NONE',  ( -11.21656899573597954, 19.84217242128376668, 8.532680616503345306 ) ) ;
#45308=CARTESIAN_POINT ( 'NONE',  ( 0.000000000000000000, 1.005902684993156715, 0.000000000000000000 ) ) ;
#45342=CARTESIAN_POINT ( 'NONE',  ( 6.239770560962896617, 15.44424954685939255, -3.176762229947382998 ) ) ;
#45367=CARTESIAN_POINT ( 'NONE',  ( 12.44919954815503083, 7.219060511667757751, -8.177915604358730661 ) ) ;
#45390=CIRCLE ( 'NONE', #72911, 8.000000000000000000 ) ;
#45406=DIRECTION ( 'NONE',  ( 0.000000000000000000, -0.8802307401757925032, 0.4745459346044136328 ) ) ;
#45430=( GEOMETRIC_REPRESENTATION_CONTEXT ( 3 ) GLOBAL_UNCERTAINTY_ASSIGNED_CONTEXT ( ( #104177 ) ) GLOBAL_UNIT_ASSIGNED_CONTEXT ( ( #102638, #61678, #37410 ) ) REPRESENTATION_CONTEXT ( 'NONE', 'WORKASPACE' ) );
#45432=DIRECTION ( 'NONE',  ( -1.000000000000000000, -0.000000000000000000, -0.000000000000000000 ) ) ;
#45454=FACE_OUTER_BOUND ( 'NONE', #36343, .T. ) ;
#45469=DIRECTION ( 'NONE',  ( -1.000000000000000000, -0.000000000000000000, -0.000000000000000000 ) ) ;
#45514=CARTESIAN_POINT ( 'NONE',  ( -11.42555267934544005, 13.51116504447436206, -9.988710933107451950 ) ) ;
#45522=CARTESIAN_POINT ( 'NONE',  ( 15.74121454705160517, 22.21713694096877134, -3.427215416333057707 ) ) ;
#45530=COLOUR_RGB ( '', 0.08235294, 0.09019608, 0.10196078) ;
#45632=CARTESIAN_POINT ( 'NONE',  ( -11.69124344503904389, 21.01850713022480477, -7.685374053051364562 ) ) ;
#45693=( NAMED_UNIT ( * ) PLANE_ANGLE_UNIT ( ) SI_UNIT ( $, .RADIAN. ) );
#45707=PRESENTATION_STYLE_ASSIGNMENT (( #61920 ) ) ;
#45762=CARTESIAN_POINT ( 'NONE',  ( 11.42431500150486023, 20.37266984104267209, 8.170926251056844336 ) ) ;
#45799=AXIS2_PLACEMENT_3D ( 'NONE', #84523, #44060, #68882 ) ;
#45807=CARTESIAN_POINT ( 'NONE',  ( -11.40270841904595933, 18.20400957074633297, 8.563861102918378876 ) ) ;
#45810=( GEOMETRIC_REPRESENTATION_CONTEXT ( 3 ) GLOBAL_UNCERTAINTY_ASSIGNED_CONTEXT ( ( #85407 ) ) GLOBAL_UNIT_ASSIGNED_CONTEXT ( ( #54293, #62958, #36598 ) ) REPRESENTATION_CONTEXT ( 'NONE', 'WORKASPACE' ) );
#45814=CARTESIAN_POINT ( 'NONE',  ( -14.29190075644363489, 21.26710225492988116, -5.626279437295411689 ) ) ;
#45867=COLOUR_RGB ( '', 0.66274510, 0.83137255, 0.94901961) ;
#45891=( NAMED_UNIT ( * ) PLANE_ANGLE_UNIT ( ) SI_UNIT ( $, .RADIAN. ) );
#45939=CARTESIAN_POINT ( 'NONE',  ( -13.72104688144364992, 3.071979568406547401, -6.016404424592845857 ) ) ;
#45963=( GEOMETRIC_REPRESENTATION_CONTEXT ( 3 ) GLOBAL_UNCERTAINTY_ASSIGNED_CONTEXT ( ( #34365 ) ) GLOBAL_UNIT_ASSIGNED_CONTEXT ( ( #86523, #40060, #88092 ) ) REPRESENTATION_CONTEXT ( 'NONE', 'WORKASPACE' ) );
#46035=CARTESIAN_POINT ( 'NONE',  ( -11.41837999597691322, 13.88778927716229461, -9.962302244322264855 ) ) ;
#46040=CARTESIAN_POINT ( 'NONE',  ( 15.79067987436806852, 22.71383723441031677, 1.248691266792864019 ) ) ;
#46053=CARTESIAN_POINT ( 'NONE',  ( 15.51348069825422016, 2.608686647713930107, -0.4238655689582255803 ) ) ;
#46068=CIRCLE ( 'NONE', #13313, 8.750000000000033751 ) ;
#46092=CARTESIAN_POINT ( 'NONE',  ( -15.77973964953674724, 22.60063761605398369, -1.998938598361739150 ) ) ;
#46103=DIRECTION ( 'NONE',  ( 1.000000000000000000, 0.000000000000000000, -1.224646799147353207E-16 ) ) ;
#46127=CARTESIAN_POINT ( 'NONE',  ( 18.00000000000000355, 12.99999999999999289, 0.000000000000000000 ) ) ;
#46155=CARTESIAN_POINT ( 'NONE',  ( -14.83882035797137888, 4.620392632316137949, 5.701545570406011620 ) ) ;
#46160=CARTESIAN_POINT ( 'NONE',  ( -10.52583372651181115, 10.24894645679494509, -10.32074519161062476 ) ) ;
#46186=CARTESIAN_POINT ( 'NONE',  ( -6.770001855160698412, 9.416670812148407066, -1.796682604554742602 ) ) ;
#46214=CARTESIAN_POINT ( 'NONE',  ( 13.99175139092173481, 6.893215643474297494, -7.923894012196674552 ) ) ;
#46223=SURFACE_STYLE_FILL_AREA ( #45174 ) ;
#46233=CARTESIAN_POINT ( 'NONE',  ( 14.58597127887092526, 5.499146323182380058, -6.679532531461099154 ) ) ;
#46237=CARTESIAN_POINT ( 'NONE',  ( 15.85122647056135392, 4.114663126756306077, -4.288211754877241155 ) ) ;
#46258=CIRCLE ( 'NONE', #25581, 1.000000000000000888 ) ;
#46283=CARTESIAN_POINT ( 'NONE',  ( 0.000000000000000000, 0.9999999999999970024, 0.000000000000000000 ) ) ;
#46297=CARTESIAN_POINT ( 'NONE',  ( 15.55524313394574776, 4.752315816073751975, 5.679728908060340586 ) ) ;
#46323=B_SPLINE_CURVE_WITH_KNOTS ( 'NONE', 3,
 ( #76184, #68098, #27156, #15167, #39987, #38932 ),
 .UNSPECIFIED., .F., .F.,
 ( 4, 2, 4 ),
 ( 0.000000000000000000, 0.001916782365109756352, 0.003833564730219512703 ),
 .UNSPECIFIED. ) ;
#46338=CARTESIAN_POINT ( 'NONE',  ( -11.09991137466503197, 10.54797039668288150, 9.715157720006006414 ) ) ;
#46354=DIRECTION ( 'NONE',  ( -0.3048027540940019264, 0.4519649026942499925, -0.8383453988835919413 ) ) ;
#46357=ADVANCED_FACE ( 'NONE', ( #17088 ), #49955, .T. ) ;
#46392=EDGE_LOOP ( 'NONE', ( #79910, #30116, #74025, #77682 ) ) ;
#46421=FILL_AREA_STYLE ('',( #62099 ) ) ;
#46449=CARTESIAN_POINT ( 'NONE',  ( 0.000000000000000000, 1.005902684993156715, -14.99698745252234566 ) ) ;
#46457=DIRECTION ( 'NONE',  ( 0.000000000000000000, 0.000000000000000000, 1.000000000000000000 ) ) ;
#46466=CARTESIAN_POINT ( 'NONE',  ( -14.77855167844241535, 5.771020710681859178, -6.929713172033096669 ) ) ;
#46490=CARTESIAN_POINT ( 'NONE',  ( 1.489880555935390203E-15, 34.19642918197134662, 12.16579798332631945 ) ) ;
#46518=SURFACE_STYLE_USAGE ( .BOTH. , #55122 ) ;
#46562=CARTESIAN_POINT ( 'NONE',  ( 16.14595037822608603, 20.23371447308070259, -4.922994507608427384 ) ) ;
#46572=CARTESIAN_POINT ( 'NONE',  ( 14.71845092680647760, 2.464670597979462308, -2.845879451958821527 ) ) ;
#46574=DIRECTION ( 'NONE',  ( 0.000000000000000000, 0.000000000000000000, -1.000000000000000000 ) ) ;
#46597=MECHANICAL_DESIGN_GEOMETRIC_PRESENTATION_REPRESENTATION('',(#24219),#49);
#46612=CARTESIAN_POINT ( 'NONE',  ( -16.11696382278816841, 21.57140452653678153, 2.149593460082904972 ) ) ;
#46630=CARTESIAN_POINT ( 'NONE',  ( 13.58261091780133789, 24.75325252249499997, 0.6700394777244487177 ) ) ;
#46641=CARTESIAN_POINT ( 'NONE',  ( -11.52959627970376033, 12.35318608925452111, 9.999999999999845457 ) ) ;
#46673=CARTESIAN_POINT ( 'NONE',  ( -11.88733434657279808, 21.45620698160807294, 7.302873484819567551 ) ) ;
#46677=EDGE_CURVE ( 'NONE', #57533, #57762, #50032, .T. ) ;
#46704=CARTESIAN_POINT ( 'NONE',  ( -16.14595037822608603, 7.274337365578172232, 6.616591826369962348 ) ) ;
#46754=CARTESIAN_POINT ( 'NONE',  ( 14.29190075645222180, 6.456385560667814438, -7.561819230143195902 ) ) ;
#46757=CARTESIAN_POINT ( 'NONE',  ( 15.93251508686769036, 3.184445033430845839, -1.451444771589639915 ) ) ;
#46818=CARTESIAN_POINT ( 'NONE',  ( 10.70754322050349394, 12.38955932816331540, 10.00023628198462688 ) ) ;
#46929=CARTESIAN_POINT ( 'NONE',  ( -6.704772934685586883, 16.45971469038980217, 2.024104295774003415 ) ) ;
#46933=CARTESIAN_POINT ( 'NONE',  ( 12.15278015503357523, 17.47224881724134349, -8.961376170971080413 ) ) ;
#46971=AXIS2_PLACEMENT_3D ( 'NONE', #73246, #91070, #73790 ) ;
#46972=FILL_AREA_STYLE ('',( #22205 ) ) ;
#46981=CARTESIAN_POINT ( 'NONE',  ( -13.39439044838818837, 7.828241060370396021, -8.562929616685366341 ) ) ;
#46992=LINE ( 'NONE', #6001, #58702 ) ;
#47028=AXIS2_PLACEMENT_3D ( 'NONE', #7907, #89904, #40813 ) ;
#47038=CARTESIAN_POINT ( 'NONE',  ( 16.10302234481864403, 5.501632350609516386, 4.770674012950428811 ) ) ;
#47076=CARTESIAN_POINT ( 'NONE',  ( -15.28599664425101246, 3.173649883756319401, 3.309198297971303049 ) ) ;
#47132=CARTESIAN_POINT ( 'NONE',  ( -16.10370002540618373, 21.82456013744392109, 0.8668566224997985570 ) ) ;
#47146=( GEOMETRIC_REPRESENTATION_CONTEXT ( 3 ) GLOBAL_UNCERTAINTY_ASSIGNED_CONTEXT ( ( #7903 ) ) GLOBAL_UNIT_ASSIGNED_CONTEXT ( ( #56106, #72321, #73360 ) ) REPRESENTATION_CONTEXT ( 'NONE', 'WORKASPACE' ) );
#47153=CARTESIAN_POINT ( 'NONE',  ( 10.55307219781806616, 17.81967380046186022, 9.596392936463645995 ) ) ;
#47183=ORIENTED_EDGE ( 'NONE', *, *, #49470, .T. ) ;
#47195=CARTESIAN_POINT ( 'NONE',  ( -13.59375373143781651, 24.77294821207336639, -0.6337968656602750439 ) ) ;
#47203=ORIENTED_EDGE ( 'NONE', *, *, #36323, .F. ) ;
#47276=CARTESIAN_POINT ( 'NONE',  ( 15.91255636217487712, 3.418437750269127218, -2.532291868533038226 ) ) ;
#47286=ORIENTED_EDGE ( 'NONE', *, *, #32065, .F. ) ;
#47314=EDGE_CURVE ( 'NONE', #76857, #93549, #70752, .T. ) ;
#47326=DIRECTION ( 'NONE',  ( -1.000000000000000000, 0.000000000000000000, 0.000000000000000000 ) ) ;
#47382=CARTESIAN_POINT ( 'NONE',  ( -13.72579875526420068, 3.063920234766396966, 6.005637484505932377 ) ) ;
#47460=CARTESIAN_POINT ( 'NONE',  ( 11.97147371475453248, 19.60245619413215223, -7.526067045436439784 ) ) ;
#47507=CYLINDRICAL_SURFACE ( 'NONE', #1519, 7.500000000000000000 ) ;
#47508=ADVANCED_FACE ( 'NONE', ( #30112 ), #93165, .T. ) ;
#47510=CARTESIAN_POINT ( 'NONE',  ( -10.42678887926924958, 17.27620279768637701, -9.792472684408327410 ) ) ;
#47566=DIRECTION ( 'NONE',  ( 0.000000000000000000, 0.000000000000000000, -1.000000000000000000 ) ) ;
#47605=CARTESIAN_POINT ( 'NONE',  ( -16.03938085755613230, 4.451364308023405769, 3.146830695504104547 ) ) ;
#47618=CARTESIAN_POINT ( 'NONE',  ( 16.14595037822613932, 12.99999999999999289, 0.000000000000000000 ) ) ;
#47619=CARTESIAN_POINT ( 'NONE',  ( -14.59153803998622223, 1.704952136599680923, 3.465235867604003150 ) ) ;
#47632=ORIENTED_EDGE ( 'NONE', *, *, #63720, .F. ) ;
#47659=CARTESIAN_POINT ( 'NONE',  ( -16.10103572754771761, 21.87195731844465740, -0.4457938394067768595 ) ) ;
#47741=AXIS2_PLACEMENT_3D ( 'NONE', #62242, #3980, #95127 ) ;
#47783=CARTESIAN_POINT ( 'NONE',  ( 11.89481087122913294, 16.74404509406153352, 9.279772923664232565 ) ) ;
#47808=VERTEX_POINT ( 'NONE', #63424 ) ;
#47840=AXIS2_PLACEMENT_3D ( 'NONE', #18219, #67290, #52677 ) ;
#47845=CARTESIAN_POINT ( 'NONE',  ( -28.12328997684540610, 24.73290587908618932, -14.06164498842269772 ) ) ;
#47859=CARTESIAN_POINT ( 'NONE',  ( -16.05785784214753775, 4.775831776487168945, 3.710403933803116949 ) ) ;
#47863=CARTESIAN_POINT ( 'NONE',  ( 10.93132941745003350, 11.18092413548305153, 9.853954356400903336 ) ) ;
#47878=DIRECTION ( 'NONE',  ( 1.000000000000000000, 0.000000000000000000, 0.000000000000000000 ) ) ;
#47984=CARTESIAN_POINT ( 'NONE',  ( 11.09863704574016374, 8.438406359958083414, -9.825331742445492011 ) ) ;
#48020=CARTESIAN_POINT ( 'NONE',  ( 14.37349357814347250, 2.004823033966244950, -4.269535008049492042 ) ) ;
#48025=SURFACE_STYLE_FILL_AREA ( #31371 ) ;
#48031=CARTESIAN_POINT ( 'NONE',  ( -11.99663858561632601, 8.161776382637276228, -8.765865389969762944 ) ) ;
#48052=FACE_OUTER_BOUND ( 'NONE', #10291, .T. ) ;
#48063=CARTESIAN_POINT ( 'NONE',  ( -14.29190075645216851, 7.765108448528613039, 6.049455384109680978 ) ) ;
#48087=PRESENTATION_STYLE_ASSIGNMENT (( #15198 ) ) ;
#48130=DIRECTION ( 'NONE',  ( -1.000000000000000000, 0.000000000000000000, 0.000000000000000000 ) ) ;
#48135=CARTESIAN_POINT ( 'NONE',  ( -15.05785784214673129, 3.824195276770050445, -4.604276673498577388 ) ) ;
#48149=VERTEX_POINT ( 'NONE', #84365 ) ;
#48159=STYLED_ITEM ( 'NONE', ( #81712 ), #90878 ) ;
#48208=CARTESIAN_POINT ( 'NONE',  ( 11.08838757566412170, 8.467236466350284374, -9.834809068639062346 ) ) ;
#48236=AXIS2_PLACEMENT_3D ( 'NONE', #34158, #26085, #58943 ) ;
#48252=EDGE_CURVE ( 'NONE', #57762, #40845, #36665, .T. ) ;
#48345=EDGE_CURVE ( 'NONE', #24752, #16303, #80532, .T. ) ;
#48373=CARTESIAN_POINT ( 'NONE',  ( 16.11717644235050173, 21.56691778980479057, 2.165075456547000066 ) ) ;
#48382=CARTESIAN_POINT ( 'NONE',  ( 1.489880555935390203E-15, 34.19642918197134662, 12.16579798332631412 ) ) ;
#48401=CARTESIAN_POINT ( 'NONE',  ( 10.35528044502231992, 10.95055699629187629, 10.44180044207346647 ) ) ;
#48405=( LENGTH_UNIT ( ) NAMED_UNIT ( * ) SI_UNIT ( .MILLI., .METRE. ) );
#48421=B_SPLINE_CURVE_WITH_KNOTS ( 'NONE', 3,
 ( #678, #24511, #75124, #17459, #23983, #57347, #25027, #17986, #34187, #16369, #83754, #50846, #9862, #42774, #105903, #56825 ),
 .UNSPECIFIED., .F., .F.,
 ( 4, 2, 2, 2, 2, 2, 2, 4 ),
 ( 0.000000000000000000, 0.0009812749226899852590, 0.001962549845379970518, 0.002943824768069955994, 0.003925099690759941903, 0.005887649536139912855, 0.006868924458829897897, 0.007850199381519883807 ),
 .UNSPECIFIED. ) ;
#48425=EDGE_CURVE ( 'NONE', #57533, #48149, #46068, .T. ) ;
#48435=AXIS2_PLACEMENT_3D ( 'NONE', #82860, #90966, #59130 ) ;
#48439=CARTESIAN_POINT ( 'NONE',  ( -12.35207828293850696, 7.405331434952278080, 8.319135986740995747 ) ) ;
#48520=CARTESIAN_POINT ( 'NONE',  ( 10.94261262135061230, 16.63582817876949704, -9.322719357341762603 ) ) ;
#48538=DIRECTION ( 'NONE',  ( 0.000000000000000000, 1.000000000000000000, 1.224646799147353207E-16 ) ) ;
#48545=AXIS2_PLACEMENT_3D ( 'NONE', #83350, #68789, #84429 ) ;
#48562=SURFACE_STYLE_FILL_AREA ( #15672 ) ;
#48564=CARTESIAN_POINT ( 'NONE',  ( -11.59717644377422019, 15.61894086526454473, -9.655125550077977792 ) ) ;
#48591=CARTESIAN_POINT ( 'NONE',  ( -15.50996574327916022, 2.604740765350743281, 0.8136923573409686750 ) ) ;
#48626=CARTESIAN_POINT ( 'NONE',  ( 5.744562646538028616, 12.99999999999999289, 4.000000000000000000 ) ) ;
#48667=FILL_AREA_STYLE ('',( #89687 ) ) ;
#48678=CARTESIAN_POINT ( 'NONE',  ( -14.59067579026470796, 1.706082412479009269, -3.468700283484645652 ) ) ;
#48730=ORIENTED_EDGE ( 'NONE', *, *, #46677, .T. ) ;
#48732=CARTESIAN_POINT ( 'NONE',  ( 13.22785222780199277, 24.11548868975563309, -3.450552616380675452 ) ) ;
#48744=ORIENTED_EDGE ( 'NONE', *, *, #52281, .T. ) ;
#48788=DIRECTION ( 'NONE',  ( 0.000000000000000000, 0.000000000000000000, -1.000000000000000000 ) ) ;
#48841=CARTESIAN_POINT ( 'NONE',  ( 13.57036353025074682, 20.18065266528832069, 6.968136590762834537 ) ) ;
#48854=SURFACE_STYLE_USAGE ( .BOTH. , #89869 ) ;
#49047=CARTESIAN_POINT ( 'NONE',  ( 10.12831231167428925, 12.29606514004753492, -10.56315130349414844 ) ) ;
#49063=CARTESIAN_POINT ( 'NONE',  ( -15.38845442529095209, 22.75486601555547495, 2.273822911181871298 ) ) ;
#49089=CARTESIAN_POINT ( 'NONE',  ( -11.51257484515206997, 12.49334646015600292, -10.00308483352378630 ) ) ;
#49100=AXIS2_PLACEMENT_3D ( 'NONE', #62137, #87985, #104147 ) ;
#49175=CARTESIAN_POINT ( 'NONE',  ( -11.10298186479972316, 8.427547193095088929, 9.820813330727961699 ) ) ;
#49196=CARTESIAN_POINT ( 'NONE',  ( -15.92744018389476857, 3.245174460798382121, 1.809927857081228497 ) ) ;
#49267=CARTESIAN_POINT ( 'NONE',  ( 10.88267043231995501, 9.048817955964610249, -10.02405438266481497 ) ) ;
#49376=CARTESIAN_POINT ( 'NONE',  ( 13.71930391805453553, 20.41463764547162896, 6.718748382517820694 ) ) ;
#49400=VERTEX_POINT ( 'NONE', #77857 ) ;
#49406=CIRCLE ( 'NONE', #106224, 8.750000000000023093 ) ;
#49434=CARTESIAN_POINT ( 'NONE',  ( 16.10535093526683070, 21.79478144880583557, 1.090471457032648583 ) ) ;
#49470=EDGE_CURVE ( 'NONE', #40845, #57762, #91344, .T. ) ;
#49484=STYLED_ITEM ( 'NONE', ( #90528 ), #25990 ) ;
#49488=CIRCLE ( 'NONE', #56322, 10.00000000000000178 ) ;
#49498=CIRCLE ( 'NONE', #16778, 1.000000000000000888 ) ;
#49546=EDGE_LOOP ( 'NONE', ( #93088, #28712 ) ) ;
#49554=CARTESIAN_POINT ( 'NONE',  ( -16.05785784214673484, 4.775831776474317891, -3.710403933782548513 ) ) ;
#49591=CARTESIAN_POINT ( 'NONE',  ( 14.98940227155761384, 22.23241460859703267, 3.884032814068775874 ) ) ;
#49628=AXIS2_PLACEMENT_3D ( 'NONE', #66267, #50593, #99154 ) ;
#49634=CARTESIAN_POINT ( 'NONE',  ( -14.09421869355620593, 20.98092464764351561, -6.031492443631700340 ) ) ;
#49653=SURFACE_STYLE_USAGE ( .BOTH. , #90123 ) ;
#49711=CARTESIAN_POINT ( 'NONE',  ( 8.572527594031473190E-16, -6.938893903907228378E-15, -7.000000000000000000 ) ) ;
#49872=ORIENTED_EDGE ( 'NONE', *, *, #101208, .T. ) ;
#49915=CARTESIAN_POINT ( 'NONE',  ( 11.41228817278395091, 13.87733114462658257, 9.968491662189933322 ) ) ;
#49945=DIRECTION ( 'NONE',  ( 0.000000000000000000, 0.000000000000000000, 1.000000000000000000 ) ) ;
#49955=TOROIDAL_SURFACE ( 'NONE', #22446, 13.99700487351915612, 1.000000000000000000 ) ;
#49969=VERTEX_POINT ( 'NONE', #104648 ) ;
#50032=CIRCLE ( 'NONE', #27685, 2.000000000000000444 ) ;
#50067=CARTESIAN_POINT ( 'NONE',  ( 15.50036553200073719, 2.628019270337233149, 0.8101929630272969307 ) ) ;
#50112=AXIS2_PLACEMENT_3D ( 'NONE', #46283, #95899, #13887 ) ;
#50123=CARTESIAN_POINT ( 'NONE',  ( 13.30664220163338207, 22.17912454110582487, -4.025023027331216419 ) ) ;
#50137=MECHANICAL_DESIGN_GEOMETRIC_PRESENTATION_REPRESENTATION('',(#69108),#86366);
#50169=CARTESIAN_POINT ( 'NONE',  ( -13.75359951688389160, 20.47115004747033851, -6.669194425414865179 ) ) ;
#50263=CARTESIAN_POINT ( 'NONE',  ( 15.05785784214677392, 3.824195276769925655, -4.604276673498363337 ) ) ;
#50294=CARTESIAN_POINT ( 'NONE',  ( 14.82166267806915094, 22.90614510862747011, 2.002102660500554521 ) ) ;
#50349=TOROIDAL_SURFACE ( 'NONE', #36634, 7.999999999999998224, 2.000000000000000000 ) ;
#50380=ORIENTED_EDGE ( 'NONE', *, *, #84367, .F. ) ;
#50385=DIRECTION ( 'NONE',  ( -0.000000000000000000, 1.000000000000000000, -0.000000000000000000 ) ) ;
#50400=ORIENTED_EDGE ( 'NONE', *, *, #12497, .T. ) ;
#50492=AXIS2_PLACEMENT_3D ( 'NONE', #9308, #101919, #66498 ) ;
#50523=AXIS2_PLACEMENT_3D ( 'NONE', #34939, #59729, #1451 ) ;
#50524=ORIENTED_EDGE ( 'NONE', *, *, #22418, .T. ) ;
#50530=CARTESIAN_POINT ( 'NONE',  ( 14.97192734824148808, 2.056257465146328567, 0.8331214207672043015 ) ) ;
#50563=CARTESIAN_POINT ( 'NONE',  ( 6.879475648205856331, 9.213907405080439261, -1.316666052250857977 ) ) ;
#50575=CARTESIAN_POINT ( 'NONE',  ( 16.02742720722318026, 4.186773460852821316, 2.547561848287669850 ) ) ;
#50579=CARTESIAN_POINT ( 'NONE',  ( 15.46209624076536038, 2.722175477912782249, 1.608330402076072474 ) ) ;
#50593=DIRECTION ( 'NONE',  ( -1.000000000000000000, 0.000000000000000000, 0.000000000000000000 ) ) ;
#50632=CARTESIAN_POINT ( 'NONE',  ( 14.98461734045173088, 22.22601645454860986, -3.898224806824892141 ) ) ;
#50642=EDGE_CURVE ( 'NONE', #103416, #40845, #34700, .T. ) ;
#50674=CARTESIAN_POINT ( 'NONE',  ( -13.08561955852094627, 23.85450803358479988, -4.082908960275540622 ) ) ;
#50702=COLOUR_RGB ( '', 0.08235294, 0.09019608, 0.10196078) ;
#50707=CARTESIAN_POINT ( 'NONE',  ( -15.50036553200112444, 2.628019270336301449, -0.8101929630158405393 ) ) ;
#50746=AXIS2_PLACEMENT_3D ( 'NONE', #9417, #11021, #44480 ) ;
#50798=ORIENTED_EDGE ( 'NONE', *, *, #6916, .F. ) ;
#50846=CARTESIAN_POINT ( 'NONE',  ( 16.02336867590681990, 4.077607736802333349, -2.243736929340127695 ) ) ;
#50979=ADVANCED_FACE ( 'NONE', ( #91812 ), #41670, .T. ) ;
#51015=PRODUCT_DEFINITION_CONTEXT ( 'detailed design', #93438, 'design' ) ;
#51056=CYLINDRICAL_SURFACE ( 'NONE', #83725, 7.000000000000000000 ) ;
#51063=CARTESIAN_POINT ( 'NONE',  ( 14.85111941933868884, 2.241372557329905479, 2.058092574385571361 ) ) ;
#51075=CIRCLE ( 'NONE', #70111, 1.999999999999999778 ) ;
#51128=AXIS2_PLACEMENT_3D ( 'NONE', #29610, #88352, #54346 ) ;
#51169=VERTEX_POINT ( 'NONE', #55965 ) ;
#51171=CARTESIAN_POINT ( 'NONE',  ( 13.33593371540757033, 24.31301558282364539, 2.945959972171505292 ) ) ;
#51215=CARTESIAN_POINT ( 'NONE',  ( -13.33398839547953152, 24.30949496516709019, 2.956257427454192843 ) ) ;
#51256=B_SPLINE_CURVE_WITH_KNOTS ( 'NONE', 3,
 ( #51811, #93356, #77165, #10809, #91757, #42662, #26527, #75561, #1656, #27595, #76617, #59400, #92261, #101442, #51273, #3279, #84194, #10290, #104079, #94427, #53427, #87916, #102506, #38838, #29198, #79281, #45342, #12411, #69612, #95467, #86865, #53933, #54444, #70134 ),
 .UNSPECIFIED., .F., .F.,
 ( 4, 2, 2, 2, 2, 2, 2, 2, 2, 2, 2, 2, 2, 2, 2, 2, 4 ),
 ( 0.01279395524623341482, 0.01359199989167121127, 0.01439004453710900772, 0.01518808918254680243, 0.01598613382798460061, 0.01678417847342239533, 0.01758222311886019351, 0.01838026776429798823, 0.01917831240973578294, 0.01997635705517358112, 0.02077440170061137584, 0.02157244634604917055, 0.02237049099148696873, 0.02316853563692476692, 0.02396658028236256163, 0.02476462492780035635, 0.02556266957323815453 ),
 .UNSPECIFIED. ) ;
#51273=CARTESIAN_POINT ( 'NONE',  ( 6.924577185163239612, 16.86673950156980339, 1.057577261889345754 ) ) ;
#51302=CARTESIAN_POINT ( 'NONE',  ( -16.14595037822624946, 20.73037563562378338, -4.193214079430573449 ) ) ;
#51310=COLOUR_RGB ( '', 0.40784314, 0.44705882, 0.49803922) ;
#51439=SURFACE_SIDE_STYLE ('',( #101056 ) ) ;
#51459=FILL_AREA_STYLE_COLOUR ( '', #70705 ) ;
#51505=CARTESIAN_POINT ( 'NONE',  ( -14.99550388410368207, 1.250601500878925076, -0.4346214790565611774 ) ) ;
#51523=CARTESIAN_POINT ( 'NONE',  ( 28.12328997684540610, 24.73290587908618932, 14.06164498842269772 ) ) ;
#51545=VERTEX_POINT ( 'NONE', #100435 ) ;
#51644=CARTESIAN_POINT ( 'NONE',  ( 6.560397950766611253, 9.829122060748870737, -2.451970031105678682 ) ) ;
#51650=COLOUR_RGB ( '', 0.08235294, 0.09019608, 0.10196078) ;
#51712=( NAMED_UNIT ( * ) PLANE_ANGLE_UNIT ( ) SI_UNIT ( $, .RADIAN. ) );
#51714=CARTESIAN_POINT ( 'NONE',  ( 15.58050646327639299, 23.00052803995978223, 0.2687008445306368065 ) ) ;
#51721=DIRECTION ( 'NONE',  ( 0.000000000000000000, 0.000000000000000000, 1.000000000000000000 ) ) ;
#51758=CARTESIAN_POINT ( 'NONE',  ( -13.60252275386366705, 22.67888446432363381, -2.545037732601225233 ) ) ;
#51777=B_SPLINE_CURVE_WITH_KNOTS ( 'NONE', 3,
 ( #31201, #22033, #38739, #5819, #78634, #54890, #70573, #71610, #103981, #61968, #14428, #96962, #94859, #37710, #72153, #47859 ),
 .UNSPECIFIED., .F., .F.,
 ( 4, 2, 2, 2, 2, 2, 2, 4 ),
 ( 0.000000000000000000, 0.0009812749226930392397, 0.001962549845386078479, 0.002943824768079117069, 0.003925099690772156091, 0.005887649536158235872, 0.006868924458851274895, 0.007850199381544313917 ),
 .UNSPECIFIED. ) ;
#51779=STYLED_ITEM ( 'NONE', ( #18319 ), #102887 ) ;
#51811=CARTESIAN_POINT ( 'NONE',  ( 5.744562646538028616, 12.99999999999999289, 4.000000000000000000 ) ) ;
#51818=STYLED_ITEM ( 'NONE', ( #85493 ), #7605 ) ;
#51832=AXIS2_PLACEMENT_3D ( 'NONE', #52843, #77121, #85767 ) ;
#51837=CARTESIAN_POINT ( 'NONE',  ( -5.744562646538029504, 12.99999999999999289, 4.000000000000000000 ) ) ;
#51855=ADVANCED_FACE ( 'NONE', ( #30723 ), #62471, .T. ) ;
#51875=DIRECTION ( 'NONE',  ( 1.000000000000000000, 0.000000000000000000, 0.000000000000000000 ) ) ;
#51891=CARTESIAN_POINT ( 'NONE',  ( 14.58934900096333465, 5.487773041241286620, 6.668063844691364928 ) ) ;
#51943=ORIENTED_EDGE ( 'NONE', *, *, #97953, .T. ) ;
#51945=( NAMED_UNIT ( * ) SI_UNIT ( $, .STERADIAN. ) SOLID_ANGLE_UNIT ( ) );
#51987=FACE_BOUND ( 'NONE', #63072, .T. ) ;
#52016=ADVANCED_FACE ( 'NONE', ( #78055 ), #50349, .T. ) ;
#52181=FILL_AREA_STYLE_COLOUR ( '', #59909 ) ;
#52188=DIRECTION ( 'NONE',  ( -0.000000000000000000, -1.000000000000000000, -0.000000000000000000 ) ) ;
#52220=EDGE_CURVE ( 'NONE', #43916, #25504, #24681, .T. ) ;
#52247=CARTESIAN_POINT ( 'NONE',  ( 11.97038518901905668, 19.60005033863593837, 7.528208079863113689 ) ) ;
#52255=ORIENTED_EDGE ( 'NONE', *, *, #66503, .F. ) ;
#52281=EDGE_CURVE ( 'NONE', #95018, #49969, #2229, .T. ) ;
#52289=CARTESIAN_POINT ( 'NONE',  ( -12.05941008653503843, 19.79566280298742242, 7.352333506836349564 ) ) ;
#52303=( LENGTH_UNIT ( ) NAMED_UNIT ( * ) SI_UNIT ( .MILLI., .METRE. ) );
#52373=CARTESIAN_POINT ( 'NONE',  ( 12.98019590313349347, 8.542529574688673577, -8.955537626817529073 ) ) ;
#52439=CARTESIAN_POINT ( 'NONE',  ( 20.00100000000000477, 12.99999999999999289, 0.000000000000000000 ) ) ;
#52473=CARTESIAN_POINT ( 'NONE',  ( -16.13647630347073658, 6.334953579828353831, -5.738861489052294651 ) ) ;
#52500=CIRCLE ( 'NONE', #66280, 7.500000000000000000 ) ;
#52521=CARTESIAN_POINT ( 'NONE',  ( 16.10528882106936521, 21.79591095384835242, 1.082486061783650255 ) ) ;
#52569=FACE_OUTER_BOUND ( 'NONE', #84088, .T. ) ;
#52579=STYLED_ITEM ( 'NONE', ( #79868 ), #13656 ) ;
#52585=CARTESIAN_POINT ( 'NONE',  ( 3.444109705163657007E-15, 24.73290587908618932, 14.06164498842270483 ) ) ;
#52592=FILL_AREA_STYLE ('',( #19758 ) ) ;
#52631=DIRECTION ( 'NONE',  ( 0.000000000000000000, 0.000000000000000000, -1.000000000000000000 ) ) ;
#52636=UNCERTAINTY_MEASURE_WITH_UNIT (LENGTH_MEASURE( 1.000000000000000082E-05 ), #6914, 'distance_accuracy_value', 'NONE');
#52677=DIRECTION ( 'NONE',  ( 0.000000000000000000, 0.000000000000000000, -1.000000000000000000 ) ) ;
#52691=CARTESIAN_POINT ( 'NONE',  ( 0.000000000000000000, 34.19642918197134662, -12.16579798332631945 ) ) ;
#52706=CARTESIAN_POINT ( 'NONE',  ( 5.817469134863316960, 12.07282864079881790, 3.893337541178056416 ) ) ;
#52716=DIRECTION ( 'NONE',  ( 1.000000000000000000, -0.000000000000000000, -0.000000000000000000 ) ) ;
#52729=DIRECTION ( 'NONE',  ( 0.000000000000000000, 1.000000000000000000, 1.224646799147353207E-16 ) ) ;
#52785=CARTESIAN_POINT ( 'NONE',  ( 13.10236887572196274, 21.82069291473259298, 4.738654922942245662 ) ) ;
#52827=CARTESIAN_POINT ( 'NONE',  ( -12.41697196639879586, 22.56423331549411415, 6.101092351693879756 ) ) ;
#52843=CARTESIAN_POINT ( 'NONE',  ( 19.50000000000000000, 12.99999999999999289, 0.000000000000000000 ) ) ;
#52909=CARTESIAN_POINT ( 'NONE',  ( -18.00000000000000355, 12.99999999999999289, 0.000000000000000000 ) ) ;
#52916=CARTESIAN_POINT ( 'NONE',  ( -16.11737681246611942, 21.56249621366126945, -2.179529459285463933 ) ) ;
#52917=CARTESIAN_POINT ( 'NONE',  ( 16.00000000000008882, 4.197692598229698646, -4.745459346021210223 ) ) ;
#52991=( NAMED_UNIT ( * ) PLANE_ANGLE_UNIT ( ) SI_UNIT ( $, .RADIAN. ) );
#53025=CYLINDRICAL_SURFACE ( 'NONE', #81571, 10.00000000000000178 ) ;
#53038=VERTEX_POINT ( 'NONE', #63908 ) ;
#53121=FILL_AREA_STYLE_COLOUR ( '', #5341 ) ;
#53165=EDGE_CURVE ( 'NONE', #12223, #43916, #26542, .T. ) ;
#53190=CARTESIAN_POINT ( 'NONE',  ( -11.53828704146876660, 7.329576385473249189, -9.371820186362002758 ) ) ;
#53263=CARTESIAN_POINT ( 'NONE',  ( 14.44581512914855459, 5.963299184997036484, -7.135127315211338583 ) ) ;
#53267=CARTESIAN_POINT ( 'NONE',  ( 15.20015366321729466, 3.406002745425039890, -3.875710626021652949 ) ) ;
#53329=CARTESIAN_POINT ( 'NONE',  ( 11.52612706373040119, 20.62001236652582747, 7.987291842674246745 ) ) ;
#53369=CARTESIAN_POINT ( 'NONE',  ( -11.82426874482432133, 21.31901130677117351, 7.426196524752196382 ) ) ;
#53423=EDGE_CURVE ( 'NONE', #1532, #93240, #51256, .T. ) ;
#53427=CARTESIAN_POINT ( 'NONE',  ( 6.880652008360423899, 16.78823603829223643, -1.310808761845548620 ) ) ;
#53455=CARTESIAN_POINT ( 'NONE',  ( 13.94390863237126155, 6.957792695931584781, -7.985806807401195861 ) ) ;
#53494=CARTESIAN_POINT ( 'NONE',  ( 14.78113245926357777, 22.77943572013436579, -2.487919536197025216 ) ) ;
#53497=FILL_AREA_STYLE ('',( #69167 ) ) ;
#53518=UNCERTAINTY_MEASURE_WITH_UNIT (LENGTH_MEASURE( 1.000000000000000082E-05 ), #26770, 'distance_accuracy_value', 'NONE');
#53594=CARTESIAN_POINT ( 'NONE',  ( 15.68546860017339384, 21.68927415056955965, -4.769872285904347642 ) ) ;
#53737=DIRECTION ( 'NONE',  ( -0.000000000000000000, -1.000000000000000000, -0.000000000000000000 ) ) ;
#53739=CARTESIAN_POINT ( 'NONE',  ( -6.086031112480590366, 10.98017962735528386, -3.462237351910362193 ) ) ;
#53773=CARTESIAN_POINT ( 'NONE',  ( 5.763702088647362665, 12.46422006045349917, 3.972887565972252233 ) ) ;
#53784=CARTESIAN_POINT ( 'NONE',  ( 15.38120149535017234, 2.925591750578491634, -2.537117285856969939 ) ) ;
#53845=CARTESIAN_POINT ( 'NONE',  ( 10.83667890787061516, 18.77600344465571780, 9.158742226827682131 ) ) ;
#53881=CARTESIAN_POINT ( 'NONE',  ( -10.18285864187934209, 15.98045425121740237, 10.18118249357682359 ) ) ;
#53895=DIRECTION ( 'NONE',  ( 0.000000000000000000, -0.8267102254944250772, -0.5626279437274306350 ) ) ;
#53900=DIRECTION ( 'NONE',  ( 0.000000000000000000, 0.000000000000000000, 1.000000000000000000 ) ) ;
#53933=CARTESIAN_POINT ( 'NONE',  ( 5.763828452502797184, 13.53687047224920192, -3.972702736835264314 ) ) ;
#54013=CARTESIAN_POINT ( 'NONE',  ( -14.97192734824248461, 2.056257465145892027, -0.8331214207561096208 ) ) ;
#54050=( LENGTH_UNIT ( ) NAMED_UNIT ( * ) SI_UNIT ( .MILLI., .METRE. ) );
#54095=CARTESIAN_POINT ( 'NONE',  ( -13.27104247666666126, 19.68897887149177350, -7.441391031246531007 ) ) ;
#54107=DIRECTION ( 'NONE',  ( 0.000000000000000000, 0.000000000000000000, 1.000000000000000000 ) ) ;
#54114=FACE_OUTER_BOUND ( 'NONE', #30507, .T. ) ;
#54149=CARTESIAN_POINT ( 'NONE',  ( -14.81542429970186348, 22.88666905516585004, 2.089502384907108379 ) ) ;
#54153=EDGE_CURVE ( 'NONE', #83606, #80083, #93642, .T. ) ;
#54160=DIRECTION ( 'NONE',  ( 0.000000000000000000, 0.6543614439339219269, -0.7561819230137102332 ) ) ;
#54210=CARTESIAN_POINT ( 'NONE',  ( -15.79261075262893677, 4.810720122707396129, 5.431533035186010494 ) ) ;
#54214=CARTESIAN_POINT ( 'NONE',  ( -13.59282890840906610, 24.77131182429118184, 0.3401920232233912045 ) ) ;
#54293=( LENGTH_UNIT ( ) NAMED_UNIT ( * ) SI_UNIT ( .MILLI., .METRE. ) );
#54346=DIRECTION ( 'NONE',  ( 0.000000000000000000, 0.000000000000000000, 1.000000000000000000 ) ) ;
#54349=CARTESIAN_POINT ( 'NONE',  ( 11.60150500652189187, 15.64056042777739108, 9.649354197112575804 ) ) ;
#54391=CARTESIAN_POINT ( 'NONE',  ( -13.36211432089984008, 5.554967171257831460, 6.704703839142655220 ) ) ;
#54410=DIRECTION ( 'NONE',  ( -1.000000000000000000, -0.000000000000000000, -0.000000000000000000 ) ) ;
#54411=DIRECTION ( 'NONE',  ( 0.000000000000000000, 0.8802307401770304018, 0.4745459346021176361 ) ) ;
#54426=ORIENTED_EDGE ( 'NONE', *, *, #54948, .F. ) ;
#54444=CARTESIAN_POINT ( 'NONE',  ( 5.744562646538029504, 13.27049502477010101, -4.000000000000000000 ) ) ;
#54475=CARTESIAN_POINT ( 'NONE',  ( 12.29569164674513715, 5.691851931703239664, -8.450287346665382060 ) ) ;
#54517=CYLINDRICAL_SURFACE ( 'NONE', #66361, 7.500000000000000000 ) ;
#54524=CARTESIAN_POINT ( 'NONE',  ( -13.46505580176244443, 5.376787718356499823, -6.519559750597839098 ) ) ;
#54535=ADVANCED_FACE ( 'NONE', ( #36175, #102993 ), #68509, .F. ) ;
#54536=CARTESIAN_POINT ( 'NONE',  ( -15.26104615578577928, 3.717029890783185575, 4.293899008437970899 ) ) ;
#54549=VECTOR ( 'NONE', #37853, 1000.000000000000000 ) ;
#54577=CARTESIAN_POINT ( 'NONE',  ( 20.00100000000000122, 12.99999999999999289, 4.000000000000000000 ) ) ;
#54616=CARTESIAN_POINT ( 'NONE',  ( -12.90950653571874440, 8.668901470952793176, -9.019737229616362484 ) ) ;
#54624=CARTESIAN_POINT ( 'NONE',  ( 16.14328335387614644, 20.70972091798899228, -4.174903250152583567 ) ) ;
#54641=CARTESIAN_POINT ( 'NONE',  ( 14.59561887823619131, 1.699647480220895179, -3.448601310181623081 ) ) ;
#54703=CARTESIAN_POINT ( 'NONE',  ( 13.51444770131055506, 24.63227180702373076, 1.633238822480681751 ) ) ;
#54722=EDGE_LOOP ( 'NONE', ( #75198, #4229, #94356, #57367, #83310, #70962, #74639, #39681, #63862 ) ) ;
#54752=CARTESIAN_POINT ( 'NONE',  ( -10.14845555286485634, 12.14994169254081413, -10.55496323469460940 ) ) ;
#54783=CARTESIAN_POINT ( 'NONE',  ( -6.984567718307133077, 9.026830075772876327, 0.5333114754527584767 ) ) ;
#54805=( GEOMETRIC_REPRESENTATION_CONTEXT ( 3 ) GLOBAL_UNCERTAINTY_ASSIGNED_CONTEXT ( ( #38764 ) ) GLOBAL_UNIT_ASSIGNED_CONTEXT ( ( #93981, #52991, #102603 ) ) REPRESENTATION_CONTEXT ( 'NONE', 'WORKASPACE' ) );
#54834=CARTESIAN_POINT ( 'NONE',  ( 15.05785784214663003, 3.824195276769948748, -4.604276673498405970 ) ) ;
#54847=VERTEX_POINT ( 'NONE', #63878 ) ;
#54890=CARTESIAN_POINT ( 'NONE',  ( -16.01731089354314364, 3.899811580358419238, -1.614417983583379623 ) ) ;
#54915=UNCERTAINTY_MEASURE_WITH_UNIT (LENGTH_MEASURE( 1.000000000000000082E-05 ), #57288, 'distance_accuracy_value', 'NONE');
#54936=CARTESIAN_POINT ( 'NONE',  ( -12.81127490048529616, 6.521419762692401534, 7.655175377805322867 ) ) ;
#54948=EDGE_CURVE ( 'NONE', #93080, #19141, #69537, .T. ) ;
#55013=CARTESIAN_POINT ( 'NONE',  ( 10.02943974854914622, 14.35851092449367528, -10.48560778031837692 ) ) ;
#55058=( NAMED_UNIT ( * ) PLANE_ANGLE_UNIT ( ) SI_UNIT ( $, .RADIAN. ) );
#55062=CARTESIAN_POINT ( 'NONE',  ( 14.61381071247569885, 22.25732077882019411, -3.894453577683311352 ) ) ;
#55064=CARTESIAN_POINT ( 'NONE',  ( -11.40808538165298991, 18.21887386053882452, -8.554671220380841490 ) ) ;
#55076=CARTESIAN_POINT ( 'NONE',  ( -15.36579003345534034, 3.191525062052813499, 3.226546488166880611 ) ) ;
#55078=CARTESIAN_POINT ( 'NONE',  ( 11.46409645960816626, 12.99999999999817923, -10.00000000000000178 ) ) ;
#55122=SURFACE_SIDE_STYLE ('',( #103694 ) ) ;
#55124=CARTESIAN_POINT ( 'NONE',  ( 16.14595037822608603, 7.274337365584589321, 6.616591826375515240 ) ) ;
#55163=CARTESIAN_POINT ( 'NONE',  ( -16.04721880643867493, 4.604982429972173996, -3.436919038178856578 ) ) ;
#55171=FILL_AREA_STYLE_COLOUR ( '', #8103 ) ;
#55220=CARTESIAN_POINT ( 'NONE',  ( -14.89085744133982558, 23.12183015427705612, -0.5456866263935301609 ) ) ;
#55236=ORIENTED_EDGE ( 'NONE', *, *, #11088, .T. ) ;
#55239=CARTESIAN_POINT ( 'NONE',  ( 11.43292703283759337, 7.596344060119427866, 9.480118827291864392 ) ) ;
#55274=DIRECTION ( 'NONE',  ( 0.000000000000000000, 0.000000000000000000, -1.000000000000000000 ) ) ;
#55279=B_SPLINE_CURVE_WITH_KNOTS ( 'NONE', 3,
 ( #97765, #89697, #82112, #47619, #55699, #7164, #8232, #65417, #81562, #32005, #104812, #7691, #48678, #65943, #40602, #31489 ),
 .UNSPECIFIED., .F., .F.,
 ( 4, 2, 2, 2, 2, 2, 2, 4 ),
 ( 9.697399036122160616E-19, 0.001337001954499136835, 0.002674003908998272803, 0.005348007817996543872, 0.006685009772495679840, 0.008022011726994815808, 0.009359013681493952644, 0.01069601563599308948 ),
 .UNSPECIFIED. ) ;
#55281=CARTESIAN_POINT ( 'NONE',  ( -10.07715742286756821, 12.79177078999071604, -10.57225269177452631 ) ) ;
#55341=EDGE_CURVE ( 'NONE', #29736, #63378, #92003, .T. ) ;
#55363=CARTESIAN_POINT ( 'NONE',  ( 15.93923796801722581, 3.103382665672758112, -0.7338764874896186452 ) ) ;
#55406=CARTESIAN_POINT ( 'NONE',  ( 1.836601268058451273E-15, 1.005902684993158047, 14.99698745252234566 ) ) ;
#55428=CARTESIAN_POINT ( 'NONE',  ( -15.00099999999999767, 12.99999999999999289, 0.000000000000000000 ) ) ;
#55461=CARTESIAN_POINT ( 'NONE',  ( -15.79117028497290676, 4.455738443839065255, 5.224106130487632171 ) ) ;
#55476=FACE_OUTER_BOUND ( 'NONE', #28000, .T. ) ;
#55534=CARTESIAN_POINT ( 'NONE',  ( -5.817469134863317848, 13.92717135920117499, -3.893337541178055972 ) ) ;
#55539=CARTESIAN_POINT ( 'NONE',  ( 10.70645837388809696, 12.39743528853116850, -10.00073793910723730 ) ) ;
#55559=CARTESIAN_POINT ( 'NONE',  ( -14.88762942959811575, 23.11179094003107792, 0.4991395141700474825 ) ) ;
#55581=( LENGTH_UNIT ( ) NAMED_UNIT ( * ) SI_UNIT ( .MILLI., .METRE. ) );
#55585=CARTESIAN_POINT ( 'NONE',  ( -10.23665139305246008, 16.32373278757852120, -10.09226983855738347 ) ) ;
#55606=DIRECTION ( 'NONE',  ( 0.000000000000000000, 1.000000000000000000, 0.000000000000000000 ) ) ;
#55614=VERTEX_POINT ( 'NONE', #14361 ) ;
#55627=ORIENTED_EDGE ( 'NONE', *, *, #79053, .T. ) ;
#55634=SURFACE_STYLE_FILL_AREA ( #96663 ) ;
#55652=ORIENTED_EDGE ( 'NONE', *, *, #56761, .T. ) ;
#55664=CARTESIAN_POINT ( 'NONE',  ( 0.000000000000000000, 34.00000000000000000, 0.000000000000000000 ) ) ;
#55670=AXIS2_PLACEMENT_3D ( 'NONE', #83984, #35476, #68346 ) ;
#55681=CARTESIAN_POINT ( 'NONE',  ( -15.89812512823622015, 3.583431000110255837, 3.067165457295355946 ) ) ;
#55683=CARTESIAN_POINT ( 'NONE',  ( 15.64030048137865592, 21.26710225494213091, 5.626279437277405648 ) ) ;
#55699=CARTESIAN_POINT ( 'NONE',  ( -14.68532172034886507, 1.589195250049053598, 3.050719247027746217 ) ) ;
#55715=AXIS2_PLACEMENT_3D ( 'NONE', #5618, #38541, #61765 ) ;
#55755=CARTESIAN_POINT ( 'NONE',  ( 12.27263865982193991, 5.738677695749484720, 8.480951842185072920 ) ) ;
#55770=ADVANCED_FACE ( 'NONE', ( #8937, #811 ), #86138, .F. ) ;
#55831=ORIENTED_EDGE ( 'NONE', *, *, #27246, .T. ) ;
#55857=MECHANICAL_DESIGN_GEOMETRIC_PRESENTATION_REPRESENTATION('',(#66282),#83454);
#55905=SURFACE_SIDE_STYLE ('',( #65630 ) ) ;
#55945=( GEOMETRIC_REPRESENTATION_CONTEXT ( 3 ) GLOBAL_UNCERTAINTY_ASSIGNED_CONTEXT ( ( #87144 ) ) GLOBAL_UNIT_ASSIGNED_CONTEXT ( ( #36460, #43448, #103275 ) ) REPRESENTATION_CONTEXT ( 'NONE', 'WORKASPACE' ) );
#55965=CARTESIAN_POINT ( 'NONE',  ( 18.00000000000000355, 12.99999999999999467, -7.500000000000000000 ) ) ;
#55982=CARTESIAN_POINT ( 'NONE',  ( -13.67323925869998646, 5.035284030722468884, 6.079275982674877454 ) ) ;
#56011=COLOUR_RGB ( '', 0.40784314, 0.44705882, 0.49803922) ;
#56062=CARTESIAN_POINT ( 'NONE',  ( 11.22447282797537227, 19.86299956823604163, -8.519236578064418808 ) ) ;
#56087=STYLED_ITEM ( 'NONE', ( #45707 ), #88291 ) ;
#56106=( LENGTH_UNIT ( ) NAMED_UNIT ( * ) SI_UNIT ( .MILLI., .METRE. ) );
#56110=CARTESIAN_POINT ( 'NONE',  ( -11.94205703464897717, 10.81404306920174463, -9.773533727217355249 ) ) ;
#56120=CARTESIAN_POINT ( 'NONE',  ( -14.68864207889024520, 1.585199049508030367, 3.034365436914247205 ) ) ;
#56127=DIRECTION ( 'NONE',  ( -1.000000000000000000, 0.000000000000000000, 0.000000000000000000 ) ) ;
#56139=ORIENTED_EDGE ( 'NONE', *, *, #94290, .T. ) ;
#56162=EDGE_LOOP ( 'NONE', ( #62020, #64878, #64663, #103145 ) ) ;
#56194=PLANE ( 'NONE',  #7985 ) ;
#56209=CARTESIAN_POINT ( 'NONE',  ( -15.35975064870708984, 2.980508189496250182, 2.732879807911750447 ) ) ;
#56265=CARTESIAN_POINT ( 'NONE',  ( -16.11139379967456620, 21.68073351268998294, -1.735103873195799284 ) ) ;
#56287=CARTESIAN_POINT ( 'NONE',  ( 13.55593332801579010, 24.70634882861434178, -1.273199631155955025 ) ) ;
#56312=AXIS2_PLACEMENT_3D ( 'NONE', #74855, #81351, #939 ) ;
#56322=AXIS2_PLACEMENT_3D ( 'NONE', #40076, #56774, #57831 ) ;
#56358=( GEOMETRIC_REPRESENTATION_CONTEXT ( 3 ) GLOBAL_UNCERTAINTY_ASSIGNED_CONTEXT ( ( #20331 ) ) GLOBAL_UNIT_ASSIGNED_CONTEXT ( ( #54050, #37405, #62203 ) ) REPRESENTATION_CONTEXT ( 'NONE', 'WORKASPACE' ) );
#56400=CARTESIAN_POINT ( 'NONE',  ( 12.39290798559944839, 18.01462319283537994, 8.658749452403840863 ) ) ;
#56458=CARTESIAN_POINT ( 'NONE',  ( 16.11142072793885305, 21.68022463236152930, 1.737955725794386730 ) ) ;
#56471=CARTESIAN_POINT ( 'NONE',  ( -2.979761111870779618E-15, 34.19642918197134662, -12.16579798332631412 ) ) ;
#56498=ORIENTED_EDGE ( 'NONE', *, *, #76613, .T. ) ;
#56499=MECHANICAL_DESIGN_GEOMETRIC_PRESENTATION_REPRESENTATION('',(#96184),#54805);
#56524=CARTESIAN_POINT ( 'NONE',  ( -14.05151807610724646, 4.424082237322779498, 5.201963304297035684 ) ) ;
#56594=CARTESIAN_POINT ( 'NONE',  ( -18.00000000000000355, 12.99999999999999289, -7.500000000000000000 ) ) ;
#56612=CARTESIAN_POINT ( 'NONE',  ( 10.24044431011775025, 16.34647364769404732, -10.08608596195729135 ) ) ;
#56630=CARTESIAN_POINT ( 'NONE',  ( -14.87651757722494139, 23.07725274647275526, -1.016940421418421892 ) ) ;
#56648=CARTESIAN_POINT ( 'NONE',  ( 14.37299415487856713, 2.005565780252362540, 4.271091604485595106 ) ) ;
#56656=CARTESIAN_POINT ( 'NONE',  ( -10.51652355666575467, 10.28136275940053856, -10.32830338406821902 ) ) ;
#56673=ORIENTED_EDGE ( 'NONE', *, *, #54948, .T. ) ;
#56677=( LENGTH_UNIT ( ) NAMED_UNIT ( * ) SI_UNIT ( .MILLI., .METRE. ) );
#56679=UNCERTAINTY_MEASURE_WITH_UNIT (LENGTH_MEASURE( 1.000000000000000082E-05 ), #58996, 'distance_accuracy_value', 'NONE');
#56754=CARTESIAN_POINT ( 'NONE',  ( -15.86692673747445603, 3.934633648119529425, -3.950574283722150248 ) ) ;
#56761=EDGE_CURVE ( 'NONE', #92197, #70305, #104310, .T. ) ;
#56774=DIRECTION ( 'NONE',  ( 1.000000000000000000, -0.000000000000000000, -0.000000000000000000 ) ) ;
#56817=( GEOMETRIC_REPRESENTATION_CONTEXT ( 3 ) GLOBAL_UNCERTAINTY_ASSIGNED_CONTEXT ( ( #28948 ) ) GLOBAL_UNIT_ASSIGNED_CONTEXT ( ( #80219, #87807, #79696 ) ) REPRESENTATION_CONTEXT ( 'NONE', 'WORKASPACE' ) );
#56825=CARTESIAN_POINT ( 'NONE',  ( 16.05785784214673129, 4.775831776474256607, -3.710403933782447261 ) ) ;
#56826=EDGE_CURVE ( 'NONE', #102396, #12309, #95704, .T. ) ;
#56832=CARTESIAN_POINT ( 'NONE',  ( 12.50584327394879303, 22.74509139218984544, -5.893325311387099141 ) ) ;
#56896=EDGE_LOOP ( 'NONE', ( #66497, #12941, #77117, #75542 ) ) ;
#56913=FILL_AREA_STYLE_COLOUR ( '', #11978 ) ;
#56934=CARTESIAN_POINT ( 'NONE',  ( 12.43927466310973173, 9.603553788038196259, 9.411862679792397657 ) ) ;
#56946=ORIENTED_EDGE ( 'NONE', *, *, #40476, .T. ) ;
#56953=FACE_BOUND ( 'NONE', #9216, .T. ) ;
#56992=CARTESIAN_POINT ( 'NONE',  ( 16.10155864910916534, 21.86284619731734935, 0.4346306502230241620 ) ) ;
#57005=SURFACE_STYLE_FILL_AREA ( #30649 ) ;
#57021=CARTESIAN_POINT ( 'NONE',  ( 11.99918652032940436, 8.156082305580584446, 8.762798087422753568 ) ) ;
#57033=DIRECTION ( 'NONE',  ( 0.000000000000000000, 0.000000000000000000, 1.000000000000000000 ) ) ;
#57041=ORIENTED_EDGE ( 'NONE', *, *, #103892, .F. ) ;
#57049=PRESENTATION_STYLE_ASSIGNMENT (( #106128 ) ) ;
#57058=CARTESIAN_POINT ( 'NONE',  ( 20.00100000000000477, 12.99999999999999289, 10.00000000000000178 ) ) ;
#57119=STYLED_ITEM ( 'NONE', ( #33495 ), #8082 ) ;
#57143=CARTESIAN_POINT ( 'NONE',  ( 10.82137645999426034, 16.06255650797403334, -9.525625210853387870 ) ) ;
#57181=EDGE_CURVE ( 'NONE', #103416, #37313, #95997, .T. ) ;
#57185=CARTESIAN_POINT ( 'NONE',  ( -11.44715097168767493, 7.561630284056658269, -9.465016000907271021 ) ) ;
#57190=AXIS2_PLACEMENT_3D ( 'NONE', #88387, #6375, #105096 ) ;
#57198=CARTESIAN_POINT ( 'NONE',  ( 12.01340667464404710, 17.09192326160534492, -9.133615181541646422 ) ) ;
#57249=CARTESIAN_POINT ( 'NONE',  ( -11.62298468832406328, 15.73209527160812904, 9.621853404307836755 ) ) ;
#57265=CARTESIAN_POINT ( 'NONE',  ( -11.07540909475009450, 19.47767444011234161, 8.771819969050072885 ) ) ;
#57282=CARTESIAN_POINT ( 'NONE',  ( -16.02335565827205954, 4.077236164004103713, -2.242500883993121530 ) ) ;
#57288=( LENGTH_UNIT ( ) NAMED_UNIT ( * ) SI_UNIT ( .MILLI., .METRE. ) );
#57347=CARTESIAN_POINT ( 'NONE',  ( 16.01731089354320048, 3.899811580360073471, 1.614417983590256123 ) ) ;
#57356=CARTESIAN_POINT ( 'NONE',  ( 13.24339100265629376, 3.909282924590824937, -6.957567076447526588 ) ) ;
#57363=EDGE_LOOP ( 'NONE', ( #27212, #62225, #19697 ) ) ;
#57367=ORIENTED_EDGE ( 'NONE', *, *, #11082, .T. ) ;
#57464=CARTESIAN_POINT ( 'NONE',  ( 13.11993966223870522, 19.43011205168758693, 7.666318333318653089 ) ) ;
#57476=MECHANICAL_DESIGN_GEOMETRIC_PRESENTATION_REPRESENTATION('',(#9289),#45430);
#57519=CARTESIAN_POINT ( 'NONE',  ( 14.29190075645216851, 12.99999999999999289, 7.999999999999998224 ) ) ;
#57533=VERTEX_POINT ( 'NONE', #92269 ) ;
#57551=DIRECTION ( 'NONE',  ( 0.000000000000000000, 0.000000000000000000, -1.000000000000000000 ) ) ;
#57605=SURFACE_STYLE_FILL_AREA ( #24757 ) ;
#57668=CARTESIAN_POINT ( 'NONE',  ( 15.50375927216468774, 22.90274012999477904, 1.420239429929072594 ) ) ;
#57709=CARTESIAN_POINT ( 'NONE',  ( -13.41661347689002959, 22.36574897157366237, 3.535290152413994136 ) ) ;
#57762=VERTEX_POINT ( 'NONE', #45814 ) ;
#57780=CARTESIAN_POINT ( 'NONE',  ( -11.82990717643122913, 16.52431529527237686, 9.360596964331460157 ) ) ;
#57800=CARTESIAN_POINT ( 'NONE',  ( -12.20022513325955060, 22.12076576512997761, -6.617748350316168704 ) ) ;
#57817=CARTESIAN_POINT ( 'NONE',  ( -15.05785784214101675, 3.824195276787174524, 4.604276673525165009 ) ) ;
#57831=DIRECTION ( 'NONE',  ( 0.000000000000000000, 1.734723475976806700E-15, 1.000000000000000000 ) ) ;
#57863=DIRECTION ( 'NONE',  ( 0.000000000000000000, 0.000000000000000000, -1.000000000000000000 ) ) ;
#57890=CARTESIAN_POINT ( 'NONE',  ( 12.30767636227396267, 22.34822279547523749, -6.380817737059023109 ) ) ;
#57943=ORIENTED_EDGE ( 'NONE', *, *, #5860, .T. ) ;
#58034=CARTESIAN_POINT ( 'NONE',  ( -14.29190075645216851, 12.99999999999999289, 0.000000000000000000 ) ) ;
#58035=EDGE_LOOP ( 'NONE', ( #69086, #70462, #40451, #12246 ) ) ;
#58036=UNCERTAINTY_MEASURE_WITH_UNIT (LENGTH_MEASURE( 1.000000000000000082E-05 ), #61330, 'distance_accuracy_value', 'NONE');
#58054=DIRECTION ( 'NONE',  ( -0.000000000000000000, -1.000000000000000000, -0.000000000000000000 ) ) ;
#58141=CARTESIAN_POINT ( 'NONE',  ( 6.925232610679094236, 9.132088611198859951, 1.053462737155419715 ) ) ;
#58154=( NAMED_UNIT ( * ) SI_UNIT ( $, .STERADIAN. ) SOLID_ANGLE_UNIT ( ) );
#58217=CARTESIAN_POINT ( 'NONE',  ( 14.09725510805089854, 20.98540075817746597, -6.025598037645925942 ) ) ;
#58264=CARTESIAN_POINT ( 'NONE',  ( -13.79692543861649590, 23.00056648293360695, 0.4954180079795145741 ) ) ;
#58276=CARTESIAN_POINT ( 'NONE',  ( 11.45228732919311554, 14.70820108121607106, -9.862212453994716910 ) ) ;
#58331=DIRECTION ( 'NONE',  ( 0.000000000000000000, 0.000000000000000000, -1.000000000000000000 ) ) ;
#58370=SURFACE_SIDE_STYLE ('',( #7673 ) ) ;
#58378=DIRECTION ( 'NONE',  ( 0.000000000000000000, 0.000000000000000000, 1.000000000000000000 ) ) ;
#58410=CYLINDRICAL_SURFACE ( 'NONE', #71919, 7.500000000000000000 ) ;
#58445=CARTESIAN_POINT ( 'NONE',  ( 12.26443481952583525, 5.755067855938387211, -8.492088444537413849 ) ) ;
#58460=FACE_OUTER_BOUND ( 'NONE', #97107, .T. ) ;
#58518=CARTESIAN_POINT ( 'NONE',  ( 14.29190075645216851, 7.765108448534480345, 6.049455384114757805 ) ) ;
#58527=ORIENTED_EDGE ( 'NONE', *, *, #91450, .F. ) ;
#58566=B_SPLINE_CURVE_WITH_KNOTS ( 'NONE', 3,
 ( #1741, #27139, #647, #82673, #83723, #33613 ),
 .UNSPECIFIED., .F., .F.,
 ( 4, 2, 4 ),
 ( 5.299864126966940009E-16, 0.002016319290306485372, 0.004032638580612440786 ),
 .UNSPECIFIED. ) ;
#58622=ORIENTED_EDGE ( 'NONE', *, *, #63462, .F. ) ;
#58650=( NAMED_UNIT ( * ) SI_UNIT ( $, .STERADIAN. ) SOLID_ANGLE_UNIT ( ) );
#58656=CARTESIAN_POINT ( 'NONE',  ( 14.97109678640431696, 2.057467188489078946, -0.8486206380088415768 ) ) ;
#58691=CIRCLE ( 'NONE', #101729, 4.000000000000000000 ) ;
#58702=VECTOR ( 'NONE', #105242, 1000.000000000000000 ) ;
#58722=VERTEX_POINT ( 'NONE', #20272 ) ;
#58765=CARTESIAN_POINT ( 'NONE',  ( 15.85122647056153689, 4.114663126756284761, 4.288211754877275794 ) ) ;
#58767=CARTESIAN_POINT ( 'NONE',  ( 15.37770065074485792, 22.74086236292912488, -2.279734282488619979 ) ) ;
#58813=CARTESIAN_POINT ( 'NONE',  ( -15.19979302622828854, 22.50962311628596879, -3.105710245049020379 ) ) ;
#58943=DIRECTION ( 'NONE',  ( 0.000000000000000000, 0.000000000000000000, -1.000000000000000000 ) ) ;
#58996=( LENGTH_UNIT ( ) NAMED_UNIT ( * ) SI_UNIT ( .MILLI., .METRE. ) );
#59085=CARTESIAN_POINT ( 'NONE',  ( -14.11595029532502110, 2.410436752314748521, -5.024000119269303788 ) ) ;
#59130=DIRECTION ( 'NONE',  ( 0.000000000000000000, -0.8802307401770257389, 0.4745459346021264069 ) ) ;
#59144=UNCERTAINTY_MEASURE_WITH_UNIT (LENGTH_MEASURE( 1.000000000000000082E-05 ), #11342, 'distance_accuracy_value', 'NONE');
#59158=UNCERTAINTY_MEASURE_WITH_UNIT (LENGTH_MEASURE( 1.000000000000000082E-05 ), #69373, 'distance_accuracy_value', 'NONE');
#59230=CARTESIAN_POINT ( 'NONE',  ( 6.084941413214105310, 10.98348070165863888, 3.464128533964752510 ) ) ;
#59236=ORIENTED_EDGE ( 'NONE', *, *, #104553, .T. ) ;
#59240=CARTESIAN_POINT ( 'NONE',  ( 15.93262767509089350, 3.183098147203142769, 1.443311391229760376 ) ) ;
#59243=FACE_OUTER_BOUND ( 'NONE', #29801, .T. ) ;
#59253=AXIS2_PLACEMENT_3D ( 'NONE', #98552, #82378, #57551 ) ;
#59293=ADVANCED_FACE ( 'NONE', ( #93188 ), #15209, .T. ) ;
#59299=CARTESIAN_POINT ( 'NONE',  ( 13.59349846140866447, 24.77249653569413823, 0.2813197656736000085 ) ) ;
#59319=DIRECTION ( 'NONE',  ( 0.000000000000000000, 0.000000000000000000, 1.000000000000000000 ) ) ;
#59335=PRODUCT_DEFINITION_FORMATION_WITH_SPECIFIED_SOURCE ( 'ANY', '', #28705, .NOT_KNOWN. ) ;
#59343=CARTESIAN_POINT ( 'NONE',  ( -15.58067260655142761, 23.00073928917876032, 0.5609666062011725574 ) ) ;
#59400=CARTESIAN_POINT ( 'NONE',  ( 6.705020855549795655, 16.46018158102737061, 2.023228926981749165 ) ) ;
#59422=PRESENTATION_STYLE_ASSIGNMENT (( #93378 ) ) ;
#59453=AXIS2_PLACEMENT_3D ( 'NONE', #95779, #86117, #95254 ) ;
#59605=CARTESIAN_POINT ( 'NONE',  ( 0.000000000000000000, -6.938893903907228378E-15, 7.000000000000000000 ) ) ;
#59626=CARTESIAN_POINT ( 'NONE',  ( -14.85111941933941360, 2.241372557327220960, -2.058092574375395500 ) ) ;
#59629=CARTESIAN_POINT ( 'NONE',  ( -15.76884112491384649, 22.48937974161067999, -2.489079047167402692 ) ) ;
#59704=FACE_OUTER_BOUND ( 'NONE', #1033, .T. ) ;
#59726=CARTESIAN_POINT ( 'NONE',  ( 15.22818746203032703, 3.929489829918875632, 4.609438620807825515 ) ) ;
#59729=DIRECTION ( 'NONE',  ( 1.000000000000000000, 0.000000000000000000, 0.000000000000000000 ) ) ;
#59732=( NAMED_UNIT ( * ) PLANE_ANGLE_UNIT ( ) SI_UNIT ( $, .RADIAN. ) );
#59792=ORIENTED_EDGE ( 'NONE', *, *, #85599, .T. ) ;
#59822=B_SPLINE_CURVE_WITH_KNOTS ( 'NONE', 3,
 ( #101820, #27986, #12801, #77556, #13328, #4197 ),
 .UNSPECIFIED., .F., .F.,
 ( 4, 2, 4 ),
 ( 9.697399036122160616E-19, 0.002016319290324490501, 0.004032638580648980134 ),
 .UNSPECIFIED. ) ;
#59836=CARTESIAN_POINT ( 'NONE',  ( 15.26512326535558373, 22.59485187131588901, -2.832032051335056533 ) ) ;
#59883=CARTESIAN_POINT ( 'NONE',  ( -11.97156449694083946, 19.60962570912202096, -7.534720397356830190 ) ) ;
#59904=EDGE_CURVE ( 'NONE', #80083, #38642, #6429, .T. ) ;
#59909=COLOUR_RGB ( '', 0.09019608, 0.27058824, 0.51372549) ;
#59965=SURFACE_SIDE_STYLE ('',( #44837 ) ) ;
#60018=AXIS2_PLACEMENT_3D ( 'NONE', #52439, #2286, #44915 ) ;
#60125=FACE_OUTER_BOUND ( 'NONE', #65223, .T. ) ;
#60172=CARTESIAN_POINT ( 'NONE',  ( -15.47474416541280995, 2.749750016663679464, 1.674624973627630187 ) ) ;
#60198=DIRECTION ( 'NONE',  ( 0.000000000000000000, 0.000000000000000000, 1.000000000000000000 ) ) ;
#60236=CARTESIAN_POINT ( 'NONE',  ( -15.64030048137934870, 6.456385560660732104, 7.561819230134807945 ) ) ;
#60252=DIRECTION ( 'NONE',  ( 0.000000000000000000, 0.000000000000000000, 1.000000000000000000 ) ) ;
#60258=ORIENTED_EDGE ( 'NONE', *, *, #82521, .F. ) ;
#60273=SURFACE_STYLE_FILL_AREA ( #70329 ) ;
#60307=SURFACE_STYLE_FILL_AREA ( #27430 ) ;
#60335=CARTESIAN_POINT ( 'NONE',  ( 9.797174393178825657E-16, 0.9999999999999970024, -8.000000000000000000 ) ) ;
#60373=CARTESIAN_POINT ( 'NONE',  ( 16.13590653351296211, 6.313628335806327208, 5.716602451448080657 ) ) ;
#60375=CARTESIAN_POINT ( 'NONE',  ( 12.69243684000737993, 23.10840795830348782, 5.362199319019091526 ) ) ;
#60411=AXIS2_PLACEMENT_3D ( 'NONE', #44976, #85974, #12044 ) ;
#60420=CARTESIAN_POINT ( 'NONE',  ( -11.51927709202785266, 20.60355208861105325, 7.999819647742008044 ) ) ;
#60437=EDGE_LOOP ( 'NONE', ( #24396, #96953, #1989, #36206 ) ) ;
#60505=CARTESIAN_POINT ( 'NONE',  ( 13.11292558562340815, 8.306547552537741907, -8.834142966937790220 ) ) ;
#60546=( NAMED_UNIT ( * ) SI_UNIT ( $, .STERADIAN. ) SOLID_ANGLE_UNIT ( ) );
#60640=STYLED_ITEM ( 'NONE', ( #106371 ), #50979 ) ;
#60696=CARTESIAN_POINT ( 'NONE',  ( -16.14328335387691027, 20.70972091797312231, -4.174903250177856684 ) ) ;
#60712=CARTESIAN_POINT ( 'NONE',  ( 3.673202536116901758E-15, 1.005902684993158047, 14.99698745252234566 ) ) ;
#60758=CARTESIAN_POINT ( 'NONE',  ( -15.85122647056043732, 4.114663126769221968, 4.288211754900368433 ) ) ;
#60849=AXIS2_PLACEMENT_3D ( 'NONE', #75799, #69322, #76858 ) ;
#60896=CARTESIAN_POINT ( 'NONE',  ( 10.36345999819431896, 16.99173003315943831, 9.890529223011252924 ) ) ;
#60939=CARTESIAN_POINT ( 'NONE',  ( -10.06321370107148816, 14.98786682347728672, 10.39688774717462039 ) ) ;
#60954=FILL_AREA_STYLE_COLOUR ( '', #101802 ) ;
#61024=CARTESIAN_POINT ( 'NONE',  ( -16.11717644235027791, 21.56691778980941621, 2.165075456531270870 ) ) ;
#61026=CARTESIAN_POINT ( 'NONE',  ( 13.03070029080557646, 4.293758741504203336, -7.331204502238938048 ) ) ;
#61097=AXIS2_PLACEMENT_3D ( 'NONE', #87457, #101505, #45406 ) ;
#61154=ORIENTED_EDGE ( 'NONE', *, *, #82945, .T. ) ;
#61169=CARTESIAN_POINT ( 'NONE',  ( 14.88719829190570465, 23.11045037498492505, 0.5284321866356167519 ) ) ;
#61203=ORIENTED_EDGE ( 'NONE', *, *, #4360, .F. ) ;
#61227=DIRECTION ( 'NONE',  ( 0.000000000000000000, -0.6543614439331889576, -0.7561819230143446147 ) ) ;
#61232=FILL_AREA_STYLE ('',( #19222 ) ) ;
#61278=CARTESIAN_POINT ( 'NONE',  ( -14.29190075645470870, 6.456385560659953171, 7.561819230136401337 ) ) ;
#61288=ADVANCED_FACE ( 'NONE', ( #58460 ), #84860, .T. ) ;
#61310=COLOUR_RGB ( '', 0.40784314, 0.44705882, 0.49803922) ;
#61330=( LENGTH_UNIT ( ) NAMED_UNIT ( * ) SI_UNIT ( .MILLI., .METRE. ) );
#61355=( NAMED_UNIT ( * ) PLANE_ANGLE_UNIT ( ) SI_UNIT ( $, .RADIAN. ) );
#61368=CARTESIAN_POINT ( 'NONE',  ( 16.05785784214672773, 4.775831776474238843, 3.710403933782422836 ) ) ;
#61420=ADVANCED_FACE ( 'NONE', ( #79415 ), #53025, .T. ) ;
#61432=CARTESIAN_POINT ( 'NONE',  ( 12.60473757244623094, 22.93756007865150437, 5.608979574771352894 ) ) ;
#61475=CARTESIAN_POINT ( 'NONE',  ( -12.68805576174265504, 23.09990985348045456, 5.374855948767180536 ) ) ;
#61562=( NAMED_UNIT ( * ) SI_UNIT ( $, .STERADIAN. ) SOLID_ANGLE_UNIT ( ) );
#61678=( NAMED_UNIT ( * ) PLANE_ANGLE_UNIT ( ) SI_UNIT ( $, .RADIAN. ) );
#61709=CARTESIAN_POINT ( 'NONE',  ( -11.69375096826101768, 11.66688986588565591, -9.917519730966944280 ) ) ;
#61718=CARTESIAN_POINT ( 'NONE',  ( 15.74152552778519443, 22.22013712430071308, 3.418714015814440454 ) ) ;
#61765=DIRECTION ( 'NONE',  ( 0.000000000000000000, 0.000000000000000000, 1.000000000000000000 ) ) ;
#61778=PRESENTATION_STYLE_ASSIGNMENT (( #10530 ) ) ;
#61787=CARTESIAN_POINT ( 'NONE',  ( 14.11595029532508860, 2.410436752314647713, 5.024000119269133258 ) ) ;
#61801=ORIENTED_EDGE ( 'NONE', *, *, #50642, .F. ) ;
#61826=PRESENTATION_STYLE_ASSIGNMENT (( #28954 ) ) ;
#61869=CARTESIAN_POINT ( 'NONE',  ( 18.00000000000000355, 12.99999999999999467, 9.500000000000000000 ) ) ;
#61889=CARTESIAN_POINT ( 'NONE',  ( 13.53904809976053691, 7.592565540055561613, -8.416763124031669818 ) ) ;
#61896=( NAMED_UNIT ( * ) SI_UNIT ( $, .STERADIAN. ) SOLID_ANGLE_UNIT ( ) );
#61912=CARTESIAN_POINT ( 'NONE',  ( 16.03050524006189548, 4.255071776846901521, -2.702720838580708662 ) ) ;
#61920=SURFACE_STYLE_USAGE ( .BOTH. , #95324 ) ;
#61927=DIRECTION ( 'NONE',  ( 0.000000000000000000, -1.000000000000000000, 0.000000000000000000 ) ) ;
#61968=CARTESIAN_POINT ( 'NONE',  ( -16.01236936003244438, 3.722446712627851984, 0.6596918664871591620 ) ) ;
#61973=CARTESIAN_POINT ( 'NONE',  ( 11.01232928683251977, 16.91647149312766274, 9.208423644124117402 ) ) ;
#61994=TOROIDAL_SURFACE ( 'NONE', #72272, 7.999999999999998224, 2.000000000000000000 ) ;
#62013=CARTESIAN_POINT ( 'NONE',  ( -10.76371368059873390, 15.73337048095761403, 9.625036908677250480 ) ) ;
#62020=ORIENTED_EDGE ( 'NONE', *, *, #27433, .F. ) ;
#62093=CARTESIAN_POINT ( 'NONE',  ( -6.705159343100833169, 16.46048476709899688, -2.022944797798715388 ) ) ;
#62099=FILL_AREA_STYLE_COLOUR ( '', #45530 ) ;
#62119=CARTESIAN_POINT ( 'NONE',  ( 20.00100000000000122, 12.99999999999999289, -4.000000000000000000 ) ) ;
#62124=AXIS2_PLACEMENT_3D ( 'NONE', #55664, #5032, #39532 ) ;
#62137=CARTESIAN_POINT ( 'NONE',  ( 14.11571568429345369, 5.211159435664226791, 3.514002131771331250 ) ) ;
#62145=CARTESIAN_POINT ( 'NONE',  ( -14.21470604016367290, 4.169147088453041050, -4.752692181068058908 ) ) ;
#62156=CARTESIAN_POINT ( 'NONE',  ( -15.45234973294482117, 2.833591715794670396, 2.076776216679724119 ) ) ;
#62203=( NAMED_UNIT ( * ) SI_UNIT ( $, .STERADIAN. ) SOLID_ANGLE_UNIT ( ) );
#62225=ORIENTED_EDGE ( 'NONE', *, *, #32310, .T. ) ;
#62242=CARTESIAN_POINT ( 'NONE',  ( 16.14595037822613932, 12.99999999999999289, 0.000000000000000000 ) ) ;
#62253=SURFACE_STYLE_USAGE ( .BOTH. , #29884 ) ;
#62290=CARTESIAN_POINT ( 'NONE',  ( -14.37785056367358116, 21.52979621148618250, 5.240284069518001964 ) ) ;
#62310=CARTESIAN_POINT ( 'NONE',  ( 10.98741596925694353, 19.21026732195910824, 8.912652956011438476 ) ) ;
#62329=DIRECTION ( 'NONE',  ( -1.224646799147351482E-16, 0.000000000000000000, -1.000000000000000000 ) ) ;
#62354=CARTESIAN_POINT ( 'NONE',  ( -11.28474606562284777, 20.02052538581057917, -8.415621975122691723 ) ) ;
#62383=CARTESIAN_POINT ( 'NONE',  ( -5.835236874069059887, 11.94353909508101985, -3.867049007331976540 ) ) ;
#62417=DIRECTION ( 'NONE',  ( 0.000000000000000000, 0.000000000000000000, 1.000000000000000000 ) ) ;
#62424=CARTESIAN_POINT ( 'NONE',  ( 15.82318872385482145, 4.444012391124124939, -4.874853782843320715 ) ) ;
#62428=CARTESIAN_POINT ( 'NONE',  ( 15.92744018389458915, 3.245174460793482041, -1.809927857062401557 ) ) ;
#62433=FILL_AREA_STYLE ('',( #29051 ) ) ;
#62439=ORIENTED_EDGE ( 'NONE', *, *, #49470, .F. ) ;
#62441=DIRECTION ( 'NONE',  ( -1.000000000000000000, 0.000000000000000000, 0.000000000000000000 ) ) ;
#62471=TOROIDAL_SURFACE ( 'NONE', #46971, 11.18527996897366528, 1.000000000000000000 ) ;
#62486=CARTESIAN_POINT ( 'NONE',  ( 11.68473590324837730, 18.93084228341375663, 8.064254821439817533 ) ) ;
#62529=CARTESIAN_POINT ( 'NONE',  ( -14.09102575900082321, 20.97624040389351663, 6.037758616000266088 ) ) ;
#62606=CARTESIAN_POINT ( 'NONE',  ( -5.744562646538028616, 12.99999999999999289, -4.000000000000000000 ) ) ;
#62611=CARTESIAN_POINT ( 'NONE',  ( 13.72095418692558511, 3.072081172788998504, -6.016902580136559209 ) ) ;
#62750=CARTESIAN_POINT ( 'NONE',  ( -1.829579891623863134E-15, 10.71892156097790583, -14.93965356295127478 ) ) ;
#62752=CARTESIAN_POINT ( 'NONE',  ( -12.02519846569306239, 10.60060048072689298, -9.714517618948729449 ) ) ;
#62760=CARTESIAN_POINT ( 'NONE',  ( 15.77973964953668862, 22.60063761606701149, -1.998938598334726757 ) ) ;
#62831=CARTESIAN_POINT ( 'NONE',  ( 10.35049317287506732, 16.92759726105998652, 9.911179642419414293 ) ) ;
#62878=CARTESIAN_POINT ( 'NONE',  ( -12.58912078539690960, 22.90675615147189959, -5.652532877199186068 ) ) ;
#62951=SURFACE_STYLE_USAGE ( .BOTH. , #69973 ) ;
#62953=CARTESIAN_POINT ( 'NONE',  ( 15.89812512823695378, 3.583431000102802244, -3.067165457272547968 ) ) ;
#62958=( NAMED_UNIT ( * ) PLANE_ANGLE_UNIT ( ) SI_UNIT ( $, .RADIAN. ) );
#62995=STYLED_ITEM ( 'NONE', ( #101992 ), #86700 ) ;
#63015=CARTESIAN_POINT ( 'NONE',  ( 13.39710689387089460, 7.823780487645683124, 8.560214244964429398 ) ) ;
#63020=FACE_OUTER_BOUND ( 'NONE', #79931, .T. ) ;
#63056=COLOUR_RGB ( '', 0.66274510, 0.83137255, 0.94901961) ;
#63065=ORIENTED_EDGE ( 'NONE', *, *, #74282, .T. ) ;
#63072=EDGE_LOOP ( 'NONE', ( #43796, #3413 ) ) ;
#63138=CARTESIAN_POINT ( 'NONE',  ( 11.51042249250562399, 12.50642680738181944, -10.00378701082364152 ) ) ;
#63139=CARTESIAN_POINT ( 'NONE',  ( 18.00000000000000355, 12.99999999999999289, 7.500000000000000000 ) ) ;
#63149=VECTOR ( 'NONE', #45469, 1000.000000000000000 ) ;
#63160=DIRECTION ( 'NONE',  ( 0.000000000000000000, 0.000000000000000000, 1.000000000000000000 ) ) ;
#63186=LINE ( 'NONE', #70736, #76921 ) ;
#63189=CARTESIAN_POINT ( 'NONE',  ( -12.11070743667100480, 7.914088390801861550, -8.625134750327234201 ) ) ;
#63282=CARTESIAN_POINT ( 'NONE',  ( -13.94397698975202537, 6.955966708351442485, -7.994131391027606170 ) ) ;
#63288=CARTESIAN_POINT ( 'NONE',  ( -16.01234866802003154, 3.721647123655093203, -0.3211924699071123657 ) ) ;
#63297=CARTESIAN_POINT ( 'NONE',  ( -18.00000000000000355, 12.99999999999999289, 0.000000000000000000 ) ) ;
#63306=CARTESIAN_POINT ( 'NONE',  ( 14.37676598791153104, 2.000025124005285093, -4.258993516738696528 ) ) ;
#63316=ORIENTED_EDGE ( 'NONE', *, *, #44650, .T. ) ;
#63349=CARTESIAN_POINT ( 'NONE',  ( -15.79412934197575602, 22.74951556322103130, -1.014593669880072380 ) ) ;
#63378=VERTEX_POINT ( 'NONE', #4251 ) ;
#63421=CARTESIAN_POINT ( 'NONE',  ( -13.01334625365200992, 23.72039682945885630, 4.358981111881473858 ) ) ;
#63424=CARTESIAN_POINT ( 'NONE',  ( 11.46409645960816626, 12.99999999999817923, -10.00000000000000178 ) ) ;
#63431=CARTESIAN_POINT ( 'NONE',  ( -20.00000000000000000, 12.99999999999999289, 0.000000000000000000 ) ) ;
#63454=AXIS2_PLACEMENT_3D ( 'NONE', #10541, #43459, #60198 ) ;
#63462=EDGE_CURVE ( 'NONE', #77575, #58722, #18253, .T. ) ;
#63490=( NAMED_UNIT ( * ) SI_UNIT ( $, .STERADIAN. ) SOLID_ANGLE_UNIT ( ) );
#63492=CARTESIAN_POINT ( 'NONE',  ( 15.50988061984581634, 2.604948194298077002, -0.4026888889232626556 ) ) ;
#63537=CARTESIAN_POINT ( 'NONE',  ( 1.722054852581828504E-15, 24.73290587908618932, 14.06164498842270483 ) ) ;
#63599=CARTESIAN_POINT ( 'NONE',  ( -11.11281763409552603, 8.399929652088387044, 9.811721095437990314 ) ) ;
#63674=CARTESIAN_POINT ( 'NONE',  ( -6.999768563658489207, 16.99959498610098052, 0.2746924679829753080 ) ) ;
#63679=CARTESIAN_POINT ( 'NONE',  ( 11.17923199892331887, 10.30837800928391168, -9.638854972992653813 ) ) ;
#63717=CARTESIAN_POINT ( 'NONE',  ( 14.59153803999176802, 1.704952136592581935, -3.465235867580846563 ) ) ;
#63720=EDGE_CURVE ( 'NONE', #70305, #49400, #104298, .T. ) ;
#63722=PRESENTATION_STYLE_ASSIGNMENT (( #38390 ) ) ;
#63728=CARTESIAN_POINT ( 'NONE',  ( -10.62175334653542791, 14.24948917130530113, -9.926452663087374617 ) ) ;
#63752=ORIENTED_EDGE ( 'NONE', *, *, #5294, .T. ) ;
#63767=B_SPLINE_CURVE_WITH_KNOTS ( 'NONE', 3,
 ( #20929, #30578, #46214, #80153, #61889, #39191, #79100, #4695, #5224, #20400, #38152, #78045 ),
 .UNSPECIFIED., .F., .F.,
 ( 4, 2, 2, 2, 2, 4 ),
 ( 0.05929940015525115432, 0.06027543776436967288, 0.06125147537348819143, 0.06320355059172522161, 0.06515562580996224484, 0.06710770102819928196 ),
 .UNSPECIFIED. ) ;
#63776=FILL_AREA_STYLE_COLOUR ( '', #39075 ) ;
#63821=CARTESIAN_POINT ( 'NONE',  ( -16.01731991787316645, 3.900165755870967033, 1.616345057655150574 ) ) ;
#63862=ORIENTED_EDGE ( 'NONE', *, *, #86666, .F. ) ;
#63878=CARTESIAN_POINT ( 'NONE',  ( -5.744562646538028616, 12.99999999999999289, -4.000000000000000000 ) ) ;
#63898=CARTESIAN_POINT ( 'NONE',  ( 10.52825140974290008, 10.23960916619757100, 10.31893537375141889 ) ) ;
#63908=CARTESIAN_POINT ( 'NONE',  ( 14.29190075645216496, 21.26710225494213802, 5.626279437277409201 ) ) ;
#63934=VERTEX_POINT ( 'NONE', #46704 ) ;
#63937=CARTESIAN_POINT ( 'NONE',  ( 19.50000000000000000, 12.99999999999999289, 0.000000000000000000 ) ) ;
#64019=ORIENTED_EDGE ( 'NONE', *, *, #34620, .T. ) ;
#64074=PRESENTATION_STYLE_ASSIGNMENT (( #89918 ) ) ;
#64123=CARTESIAN_POINT ( 'NONE',  ( -15.05785784214257461, 3.824195276785042896, 4.604276673521232155 ) ) ;
#64134=CARTESIAN_POINT ( 'NONE',  ( -11.81728811066984086, 6.698763365558540350, 9.056117883122757561 ) ) ;
#64209=CARTESIAN_POINT ( 'NONE',  ( 11.43665049262130928, 13.07896887865097213, -10.01657062917009000 ) ) ;
#64249=SHAPE_REPRESENTATION_RELATIONSHIP ( 'NONE' , 'NONE' ,  #66748, #78240 ) ;
#64256=CARTESIAN_POINT ( 'NONE',  ( -10.35656535444040216, 10.94469993726888468, -10.44094449561934290 ) ) ;
#64315=CARTESIAN_POINT ( 'NONE',  ( -14.13609923219729758, 21.04331586717165337, 5.955105079798755696 ) ) ;
#64344=CIRCLE ( 'NONE', #50523, 4.000000000000000000 ) ;
#64354=CARTESIAN_POINT ( 'NONE',  ( -15.50079525336249731, 2.626985771265121450, 0.7904007781020662149 ) ) ;
#64411=ORIENTED_EDGE ( 'NONE', *, *, #72527, .F. ) ;
#64426=CARTESIAN_POINT ( 'NONE',  ( 13.36238532258455614, 3.698099845770522531, -6.736202370257811545 ) ) ;
#64543=CARTESIAN_POINT ( 'NONE',  ( 0.000000000000000000, -3.138931148610827481E-15, 0.000000000000000000 ) ) ;
#64553=DIRECTION ( 'NONE',  ( -1.000000000000000000, -0.000000000000000000, -0.000000000000000000 ) ) ;
#64607=CARTESIAN_POINT ( 'NONE',  ( 14.35785620000815754, 3.948300967435905751, 4.282865182293652317 ) ) ;
#64625=UNCERTAINTY_MEASURE_WITH_UNIT (LENGTH_MEASURE( 1.000000000000000082E-05 ), #65092, 'distance_accuracy_value', 'NONE');
#64663=ORIENTED_EDGE ( 'NONE', *, *, #15999, .T. ) ;
#64667=AXIS2_PLACEMENT_3D ( 'NONE', #20440, #61927, #28501 ) ;
#64674=ORIENTED_EDGE ( 'NONE', *, *, #5485, .T. ) ;
#64723=CARTESIAN_POINT ( 'NONE',  ( 11.88624655040385214, 16.70885896114117486, -9.290919399962746184 ) ) ;
#64760=CARTESIAN_POINT ( 'NONE',  ( -14.11571568429346968, 5.211159435664322714, -3.514002131771437831 ) ) ;
#64769=CARTESIAN_POINT ( 'NONE',  ( -12.45589307813304814, 7.205894838730145580, -8.168563394729352112 ) ) ;
#64780=CARTESIAN_POINT ( 'NONE',  ( -14.11595029531375900, 2.410436752333459776, 5.024000119300219502 ) ) ;
#64786=FILL_AREA_STYLE_COLOUR ( '', #43369 ) ;
#64804=( LENGTH_UNIT ( ) NAMED_UNIT ( * ) SI_UNIT ( .MILLI., .METRE. ) );
#64834=CARTESIAN_POINT ( 'NONE',  ( -13.97088187905699108, 20.79957665017152735, 6.270615721353047789 ) ) ;
#64863=CARTESIAN_POINT ( 'NONE',  ( -16.01731991114684206, 3.900112512633671980, -1.615757124594061400 ) ) ;
#64878=ORIENTED_EDGE ( 'NONE', *, *, #44650, .F. ) ;
#64939=CARTESIAN_POINT ( 'NONE',  ( 13.28963858130279441, 24.22795872967301634, -3.151957778078536609 ) ) ;
#65092=( LENGTH_UNIT ( ) NAMED_UNIT ( * ) SI_UNIT ( .MILLI., .METRE. ) );
#65127=CARTESIAN_POINT ( 'NONE',  ( 11.66741649944374615, 8.917103227961233003, 9.153057184382511480 ) ) ;
#65164=CARTESIAN_POINT ( 'NONE',  ( -13.93128718024267165, 2.716980047703895451, 5.530599625801929875 ) ) ;
#65213=COLOUR_RGB ( '', 0.09019608, 0.27058824, 0.51372549) ;
#65223=EDGE_LOOP ( 'NONE', ( #3469, #995, #63065, #50400 ) ) ;
#65252=CARTESIAN_POINT ( 'NONE',  ( 10.87357903135575121, 11.49182943363048359, -9.891806379494946455 ) ) ;
#65285=CARTESIAN_POINT ( 'NONE',  ( 14.59067579026366701, 1.706082412480378396, 3.468700283488842739 ) ) ;
#65296=CARTESIAN_POINT ( 'NONE',  ( -10.07644798939788267, 15.01242816752345099, -10.37971395138495367 ) ) ;
#65337=CARTESIAN_POINT ( 'NONE',  ( -15.79261075262967040, 4.810720122702830004, -5.431533035174125779 ) ) ;
#65384=CARTESIAN_POINT ( 'NONE',  ( -12.48597083465239876, 22.70279443506876760, 5.925685832145178189 ) ) ;
#65400=CARTESIAN_POINT ( 'NONE',  ( -15.46526232232293907, 2.714356162034628817, -1.556038473642534115 ) ) ;
#65417=CARTESIAN_POINT ( 'NONE',  ( -14.99515772855993134, 1.250937070399350537, -0.4481625125107416840 ) ) ;
#65474=CARTESIAN_POINT ( 'NONE',  ( 12.51321390371315267, 5.264046911284898655, -8.149122212578729929 ) ) ;
#65547=CARTESIAN_POINT ( 'NONE',  ( -6.770546484616568605, 9.415636748037993442, 1.794795801736669638 ) ) ;
#65574=( GEOMETRIC_REPRESENTATION_CONTEXT ( 3 ) GLOBAL_UNCERTAINTY_ASSIGNED_CONTEXT ( ( #103814 ) ) GLOBAL_UNIT_ASSIGNED_CONTEXT ( ( #16698, #51712, #467 ) ) REPRESENTATION_CONTEXT ( 'NONE', 'WORKASPACE' ) );
#65579=CARTESIAN_POINT ( 'NONE',  ( 11.79490731899838885, 11.29963343840072021, 9.860884599382247373 ) ) ;
#65630=SURFACE_STYLE_FILL_AREA ( #6307 ) ;
#65634=CARTESIAN_POINT ( 'NONE',  ( 16.10339698264846930, 21.83175592238090346, -0.8850307878419493290 ) ) ;
#65720=EDGE_CURVE ( 'NONE', #15534, #20022, #24244, .T. ) ;
#65786=CARTESIAN_POINT ( 'NONE',  ( 15.53256180499085914, 22.93947847607967105, 1.135875605542641775 ) ) ;
#65825=CARTESIAN_POINT ( 'NONE',  ( -15.27610976668421650, 22.61015309965470976, 2.822488379715081486 ) ) ;
#65910=CARTESIAN_POINT ( 'NONE',  ( -12.27768440095290536, 5.728514393148000927, 8.474169079004697736 ) ) ;
#65943=CARTESIAN_POINT ( 'NONE',  ( -14.37299415487917109, 2.005565780251463259, -4.271091604483703286 ) ) ;
#65971=ADVANCED_FACE ( 'NONE', ( #89424 ), #23556, .T. ) ;
#66083=CARTESIAN_POINT ( 'NONE',  ( 14.29190075645216851, 12.99999999999999289, 0.000000000000000000 ) ) ;
#66106=ADVANCED_FACE ( 'NONE', ( #19306, #68334 ), #51056, .F. ) ;
#66154=EDGE_LOOP ( 'NONE', ( #8340, #50380, #1721, #58527 ) ) ;
#66227=DIRECTION ( 'NONE',  ( 0.000000000000000000, 0.000000000000000000, 1.000000000000000000 ) ) ;
#66255=CARTESIAN_POINT ( 'NONE',  ( 15.43348245327038804, 2.792842261935781778, 2.002630087556611649 ) ) ;
#66267=CARTESIAN_POINT ( 'NONE',  ( -16.14595037822616419, 12.99999999999999289, 0.000000000000000000 ) ) ;
#66280=AXIS2_PLACEMENT_3D ( 'NONE', #63937, #30514, #55274 ) ;
#66282=STYLED_ITEM ( 'NONE', ( #81746 ), #55770 ) ;
#66309=CARTESIAN_POINT ( 'NONE',  ( 14.83882035797480370, 4.620392632306892899, 5.701545570394880968 ) ) ;
#66311=CARTESIAN_POINT ( 'NONE',  ( 12.53415426001211763, 20.77299430586604601, -6.330093763739077950 ) ) ;
#66351=CARTESIAN_POINT ( 'NONE',  ( -12.41941622641344622, 22.56916116445944454, -6.095008768951160505 ) ) ;
#66361=AXIS2_PLACEMENT_3D ( 'NONE', #78809, #13540, #46457 ) ;
#66376=CARTESIAN_POINT ( 'NONE',  ( -16.14595037822607182, 6.785770140110558124, 6.193810554580664984 ) ) ;
#66449=CARTESIAN_POINT ( 'NONE',  ( 14.29190075645216851, 6.456385560668102208, -7.561819230143448145 ) ) ;
#66460=DIRECTION ( 'NONE',  ( 0.000000000000000000, 0.000000000000000000, 1.000000000000000000 ) ) ;
#66497=ORIENTED_EDGE ( 'NONE', *, *, #66503, .T. ) ;
#66498=DIRECTION ( 'NONE',  ( 0.000000000000000000, 0.000000000000000000, -1.000000000000000000 ) ) ;
#66503=EDGE_CURVE ( 'NONE', #29837, #93080, #51075, .T. ) ;
#66702=STYLED_ITEM ( 'NONE', ( #48087 ), #29321 ) ;
#66728=CARTESIAN_POINT ( 'NONE',  ( -16.14595037822608603, 7.274337365584598203, -6.616591826375523233 ) ) ;
#66748=SHAPE_REPRESENTATION ( '5. Joint', ( #10728 ), #47146 ) ;
#66778=CARTESIAN_POINT ( 'NONE',  ( 5.763785242774020823, 12.46408377182749661, -3.972758706198394663 ) ) ;
#66852=CARTESIAN_POINT ( 'NONE',  ( 14.20884251306467760, 21.14818849446572813, -5.803600968828524387 ) ) ;
#66876=CIRCLE ( 'NONE', #1395, 8.000000000000000000 ) ;
#66900=CARTESIAN_POINT ( 'NONE',  ( -13.55991250221987166, 24.71331123137162677, 1.199625589988368768 ) ) ;
#66930=CARTESIAN_POINT ( 'NONE',  ( -15.05785784214257461, 3.824195276785042896, 4.604276673521232155 ) ) ;
#67006=VECTOR ( 'NONE', #80270, 1000.000000000000000 ) ;
#67030=CARTESIAN_POINT ( 'NONE',  ( 14.87694226783599838, 23.07857475180312434, -1.005178106818441996 ) ) ;
#67047=CARTESIAN_POINT ( 'NONE',  ( -14.11595029531626722, 2.410436752329290222, 5.024000119293328126 ) ) ;
#67148=ORIENTED_EDGE ( 'NONE', *, *, #96759, .F. ) ;
#67178=CARTESIAN_POINT ( 'NONE',  ( -14.89969599197564065, 1.346844969880335308, -1.740400043373642402 ) ) ;
#67246=ORIENTED_EDGE ( 'NONE', *, *, #57181, .F. ) ;
#67247=DIRECTION ( 'NONE',  ( 0.000000000000000000, 1.000000000000000000, 0.000000000000000000 ) ) ;
#67270=ADVANCED_FACE ( 'NONE', ( #43540 ), #27188, .T. ) ;
#67290=DIRECTION ( 'NONE',  ( 1.000000000000000000, 0.000000000000000000, 0.000000000000000000 ) ) ;
#67320=CARTESIAN_POINT ( 'NONE',  ( 7.000111909206518490, 8.999804158740396076, 0.1284026198027884424 ) ) ;
#67326=EDGE_LOOP ( 'NONE', ( #20488, #82599 ) ) ;
#67332=( LENGTH_UNIT ( ) NAMED_UNIT ( * ) SI_UNIT ( .MILLI., .METRE. ) );
#67336=DIRECTION ( 'NONE',  ( 0.000000000000000000, 0.000000000000000000, -1.000000000000000000 ) ) ;
#67388=SURFACE_STYLE_USAGE ( .BOTH. , #100794 ) ;
#67390=CARTESIAN_POINT ( 'NONE',  ( 12.60415904244543484, 22.93641037622941070, -5.610498527788345235 ) ) ;
#67397=MECHANICAL_DESIGN_GEOMETRIC_PRESENTATION_REPRESENTATION('',(#51818),#26090);
#67398=VECTOR ( 'NONE', #12985, 1000.000000000000000 ) ;
#67400=DIRECTION ( 'NONE',  ( 1.000000000000000000, -0.000000000000000000, -0.000000000000000000 ) ) ;
#67415=CARTESIAN_POINT ( 'NONE',  ( -20.00000000000000000, 12.99999999999999289, 0.000000000000000000 ) ) ;
#67435=CARTESIAN_POINT ( 'NONE',  ( -12.87067482339596758, 21.40376567796203133, -5.445097966235947773 ) ) ;
#67464=EDGE_CURVE ( 'NONE', #23419, #43519, #25501, .T. ) ;
#67490=FACE_OUTER_BOUND ( 'NONE', #72631, .T. ) ;
#67498=LINE ( 'NONE', #77176, #20736 ) ;
#67574=( NAMED_UNIT ( * ) SI_UNIT ( $, .STERADIAN. ) SOLID_ANGLE_UNIT ( ) );
#67618=AXIS2_PLACEMENT_3D ( 'NONE', #105920, #23999, #7228 ) ;
#67726=COLOUR_RGB ( '', 0.08235294, 0.09019608, 0.10196078) ;
#67734=ORIENTED_EDGE ( 'NONE', *, *, #24419, .F. ) ;
#67804=CARTESIAN_POINT ( 'NONE',  ( 15.29454505947262177, 3.501281615901158162, 3.973654925238538027 ) ) ;
#67809=PLANE ( 'NONE',  #55670 ) ;
#67850=CARTESIAN_POINT ( 'NONE',  ( 16.02335565827205599, 4.077236164005316965, 2.242500883998115757 ) ) ;
#67909=CARTESIAN_POINT ( 'NONE',  ( 12.79009255231004971, 21.25547159246564277, -5.667716523303968579 ) ) ;
#67955=CARTESIAN_POINT ( 'NONE',  ( -13.56142784925484968, 22.61021997758750146, -2.795891692239694137 ) ) ;
#68032=CARTESIAN_POINT ( 'NONE',  ( -16.10155864910909074, 21.86284619731855372, 0.4346306502030854446 ) ) ;
#68094=CYLINDRICAL_SURFACE ( 'NONE', #10216, 4.000000000000000000 ) ;
#68098=CARTESIAN_POINT ( 'NONE',  ( 16.07917213302812698, 5.118112109469847404, -4.258304778695102932 ) ) ;
#68150=DIRECTION ( 'NONE',  ( 0.000000000000000000, -0.8267102254948328621, 0.5626279437268314476 ) ) ;
#68163=FACE_OUTER_BOUND ( 'NONE', #69870, .T. ) ;
#68183=PRESENTATION_STYLE_ASSIGNMENT (( #10465 ) ) ;
#68204=EDGE_LOOP ( 'NONE', ( #19093, #9928, #70632, #30836 ) ) ;
#68235=CARTESIAN_POINT ( 'NONE',  ( -14.99524476912838367, 1.250852691628805857, 0.4434096853180573006 ) ) ;
#68239=CARTESIAN_POINT ( 'NONE',  ( -14.77017712487166534, 22.74518112338312648, -2.603937284893117710 ) ) ;
#68304=FILL_AREA_STYLE ('',( #79043 ) ) ;
#68334=FACE_OUTER_BOUND ( 'NONE', #891, .T. ) ;
#68346=DIRECTION ( 'NONE',  ( 0.000000000000000000, 0.000000000000000000, -1.000000000000000000 ) ) ;
#68376=COLOUR_RGB ( '', 0.72549020, 0.75294118, 0.79215686) ;
#68451=CARTESIAN_POINT ( 'NONE',  ( 10.04228541497385763, 14.34591999596507605, 10.47348714142258963 ) ) ;
#68499=CARTESIAN_POINT ( 'NONE',  ( -11.41761984211839831, 20.35610067118025768, 8.182845679249426851 ) ) ;
#68509=PLANE ( 'NONE',  #50492 ) ;
#68578=DIRECTION ( 'NONE',  ( -1.000000000000000000, 0.000000000000000000, 0.000000000000000000 ) ) ;
#68587=CARTESIAN_POINT ( 'NONE',  ( -16.10373777989384791, 21.82388053253103877, 0.8730104594837211351 ) ) ;
#68707=ORIENTED_EDGE ( 'NONE', *, *, #67464, .F. ) ;
#68736=CARTESIAN_POINT ( 'NONE',  ( 0.000000000000000000, -6.938893903907228378E-15, 0.000000000000000000 ) ) ;
#68786=CARTESIAN_POINT ( 'NONE',  ( -16.12882272094105218, 21.28108484451415094, -2.990375924008328745 ) ) ;
#68789=DIRECTION ( 'NONE',  ( 0.000000000000000000, 1.000000000000000000, 0.000000000000000000 ) ) ;
#68852=CARTESIAN_POINT ( 'NONE',  ( -12.26692696938333782, 5.750203097402547314, -8.488608934173381471 ) ) ;
#68864=SURFACE_SIDE_STYLE ('',( #35990 ) ) ;
#68882=DIRECTION ( 'NONE',  ( 0.000000000000000000, 0.000000000000000000, 1.000000000000000000 ) ) ;
#68894=( NAMED_UNIT ( * ) SI_UNIT ( $, .STERADIAN. ) SOLID_ANGLE_UNIT ( ) );
#68933=CARTESIAN_POINT ( 'NONE',  ( 15.13200660511079754, 3.596720279097880724, 4.250825932782807293 ) ) ;
#68971=VERTEX_POINT ( 'NONE', #94519 ) ;
#68992=CARTESIAN_POINT ( 'NONE',  ( 11.80622600566693770, 16.45187812399441896, 9.389573745708821306 ) ) ;
#69034=CARTESIAN_POINT ( 'NONE',  ( -12.14245043011195335, 17.44669189061015047, 8.974181497934978324 ) ) ;
#69060=DIRECTION ( 'NONE',  ( 0.000000000000000000, -1.000000000000000000, 0.000000000000000000 ) ) ;
#69086=ORIENTED_EDGE ( 'NONE', *, *, #2942, .F. ) ;
#69108=STYLED_ITEM ( 'NONE', ( #78179 ), #79642 ) ;
#69119=CARTESIAN_POINT ( 'NONE',  ( 13.26742752227355737, 3.866425058570867712, -6.913453055525036639 ) ) ;
#69164=CARTESIAN_POINT ( 'NONE',  ( 14.47547278523829739, 21.82816532775421337, 4.801868590621356070 ) ) ;
#69167=FILL_AREA_STYLE_COLOUR ( '', #36090 ) ;
#69174=B_SPLINE_CURVE_WITH_KNOTS ( 'NONE', 3,
 ( #32494, #89643, #23877, #16818, #6050, #53, #15210, #57249, #90169, #24927, #57780, #6579, #97188, #7113, #14662, #41089, #106329, #40029, #80468, #64834, #64315, #89114 ),
 .UNSPECIFIED., .F., .F.,
 ( 4, 2, 2, 2, 2, 2, 2, 2, 2, 2, 4 ),
 ( 0.06722862433541047789, 0.06787642855568201683, 0.06852423277595354190, 0.06981984121649660591, 0.07046764543676813097, 0.07111544965703966992, 0.07241105809758273393, 0.07370666653812581182, 0.07500227497866887583, 0.07629788341921195371, 0.07759349185975501773 ),
 .UNSPECIFIED. ) ;
#69190=PRESENTATION_STYLE_ASSIGNMENT (( #43303 ) ) ;
#69202=DIRECTION ( 'NONE',  ( 0.000000000000000000, 0.000000000000000000, 1.000000000000000000 ) ) ;
#69254=CARTESIAN_POINT ( 'NONE',  ( -20.00000000000000000, 12.99999999999999289, 0.000000000000000000 ) ) ;
#69267=CARTESIAN_POINT ( 'NONE',  ( 16.14595037817326428, 20.48388002517883066, -4.555408037434820478 ) ) ;
#69322=DIRECTION ( 'NONE',  ( 1.000000000000000000, 0.000000000000000000, -1.224646799147353207E-16 ) ) ;
#69373=( LENGTH_UNIT ( ) NAMED_UNIT ( * ) SI_UNIT ( .MILLI., .METRE. ) );
#69408=MECHANICAL_DESIGN_GEOMETRIC_PRESENTATION_REPRESENTATION('',(#76228),#36706);
#69512=ADVANCED_FACE ( 'NONE', ( #63020 ), #22591, .F. ) ;
#69516=CARTESIAN_POINT ( 'NONE',  ( 11.51161983637667774, 12.49912708945058348, 10.00339853150599367 ) ) ;
#69537=CIRCLE ( 'NONE', #55715, 10.00000000000000178 ) ;
#69557=CARTESIAN_POINT ( 'NONE',  ( -13.15523420476091054, 19.48922470848437172, 7.613334812991558564 ) ) ;
#69607=EDGE_CURVE ( 'NONE', #80083, #83606, #11965, .T. ) ;
#69612=CARTESIAN_POINT ( 'NONE',  ( 6.013035130119651406, 14.79159814833020725, -3.585725784831612195 ) ) ;
#69618=SURFACE_SIDE_STYLE ('',( #42668 ) ) ;
#69632=UNCERTAINTY_MEASURE_WITH_UNIT (LENGTH_MEASURE( 1.000000000000000082E-05 ), #56677, 'distance_accuracy_value', 'NONE');
#69684=SURFACE_STYLE_USAGE ( .BOTH. , #93435 ) ;
#69693=COLOUR_RGB ( '', 0.66274510, 0.83137255, 0.94901961) ;
#69780=CARTESIAN_POINT ( 'NONE',  ( -14.29190075644363489, 21.26710225492988116, -5.626279437295411689 ) ) ;
#69789=CARTESIAN_POINT ( 'NONE',  ( -5.744562646538029504, 12.99999999999999289, 4.000000000000000000 ) ) ;
#69845=CIRCLE ( 'NONE', #49100, 2.000000000000000000 ) ;
#69850=CARTESIAN_POINT ( 'NONE',  ( 29.87930712590254956, 10.71892156097790583, 14.93965356295126945 ) ) ;
#69856=CARTESIAN_POINT ( 'NONE',  ( 10.71636377871695700, 18.38929554378958287, 9.346910711729506716 ) ) ;
#69870=EDGE_LOOP ( 'NONE', ( #3368, #91720, #86671, #33262, #32224, #92809, #41369, #4637 ) ) ;
#69897=SURFACE_STYLE_FILL_AREA ( #68304 ) ;
#69963=SURFACE_STYLE_USAGE ( .BOTH. , #44642 ) ;
#69973=SURFACE_SIDE_STYLE ('',( #95316 ) ) ;
#69993=DIRECTION ( 'NONE',  ( 0.000000000000000000, 0.000000000000000000, 1.000000000000000000 ) ) ;
#70030=ORIENTED_EDGE ( 'NONE', *, *, #74282, .F. ) ;
#70035=CARTESIAN_POINT ( 'NONE',  ( 12.03383601979006912, 21.77374900303325944, 6.997788882831823543 ) ) ;
#70044=( BOUNDED_SURFACE ( )  B_SPLINE_SURFACE ( 3, 3, ( 
 ( #48382, #30109, #14412, #56471 ),
 ( #63537, #88863, #47845, #32231 ),
 ( #105048, #38728, #71597, #73176 ),
 ( #55406, #105565, #80752, #31189 ) ),
 .UNSPECIFIED., .F., .F., .F. ) 
 B_SPLINE_SURFACE_WITH_KNOTS ( ( 4, 4 ),
 ( 4, 4 ),
 ( 0.02698643027831503644, 0.9670246242088337274 ),
 ( 0.000000000000000000, 1.000000000000000000 ),
 .UNSPECIFIED. ) 
 GEOMETRIC_REPRESENTATION_ITEM ( )  RATIONAL_B_SPLINE_SURFACE ( (
 ( 1.000000000000000000, 0.3333333333333334259, 0.3333333333333334259, 1.000000000000000000),
 ( 1.000000000000000000, 0.3333333333333334259, 0.3333333333333334259, 1.000000000000000000),
 ( 1.000000000000000000, 0.3333333333333334259, 0.3333333333333334259, 1.000000000000000000),
 ( 1.000000000000000000, 0.3333333333333334259, 0.3333333333333334259, 1.000000000000000000) ) ) 
 REPRESENTATION_ITEM ( '' )  SURFACE ( )  );
#70056=( GEOMETRIC_REPRESENTATION_CONTEXT ( 3 ) GLOBAL_UNCERTAINTY_ASSIGNED_CONTEXT ( ( #86966 ) ) GLOBAL_UNIT_ASSIGNED_CONTEXT ( ( #30600, #102338, #63490 ) ) REPRESENTATION_CONTEXT ( 'NONE', 'WORKASPACE' ) );
#70080=CARTESIAN_POINT ( 'NONE',  ( -10.42385298587354470, 17.26331716369242741, 9.797020416222427031 ) ) ;
#70090=AXIS2_PLACEMENT_3D ( 'NONE', #11099, #67247, #3028 ) ;
#70111=AXIS2_PLACEMENT_3D ( 'NONE', #58518, #75207, #34263 ) ;
#70125=MECHANICAL_DESIGN_GEOMETRIC_PRESENTATION_REPRESENTATION('',(#49484),#16759);
#70134=CARTESIAN_POINT ( 'NONE',  ( 5.744562646538029504, 12.99999999999999112, -4.000000000000000000 ) ) ;
#70161=CARTESIAN_POINT ( 'NONE',  ( -6.924369423635565290, 16.86636905560499855, 1.059067681833820940 ) ) ;
#70165=CARTESIAN_POINT ( 'NONE',  ( 15.55338204050653594, 4.754590481644285660, -5.683686875341236622 ) ) ;
#70176=ORIENTED_EDGE ( 'NONE', *, *, #72527, .T. ) ;
#70182=LINE ( 'NONE', #62119, #54549 ) ;
#70211=CARTESIAN_POINT ( 'NONE',  ( -14.35785620000810958, 3.948300967435982578, -4.282865182293815742 ) ) ;
#70305=VERTEX_POINT ( 'NONE', #95719 ) ;
#70318=CARTESIAN_POINT ( 'NONE',  ( 16.13463197906254720, 21.11076038461946425, 3.387067249047301498 ) ) ;
#70323=FACE_OUTER_BOUND ( 'NONE', #82094, .T. ) ;
#70329=FILL_AREA_STYLE ('',( #103227 ) ) ;
#70388=CARTESIAN_POINT ( 'NONE',  ( 10.03807929566702839, 14.08216048671749476, 10.50070806742469642 ) ) ;
#70431=CARTESIAN_POINT ( 'NONE',  ( -16.14595037822608603, 7.274337365576361236, 6.616591826368398266 ) ) ;
#70436=CARTESIAN_POINT ( 'NONE',  ( -10.38059036996056861, 10.84158485851692788, 10.42428711140174080 ) ) ;
#70462=ORIENTED_EDGE ( 'NONE', *, *, #24419, .T. ) ;
#70514=CARTESIAN_POINT ( 'NONE',  ( 16.01290064681821335, 3.743845801208731672, 0.6463026410229945062 ) ) ;
#70573=CARTESIAN_POINT ( 'NONE',  ( -16.01537606005192771, 3.832707337346620502, -1.292662844555364066 ) ) ;
#70578=CARTESIAN_POINT ( 'NONE',  ( 14.52498819721216705, 21.59802860051696172, 5.113706971753962272 ) ) ;
#70613=CARTESIAN_POINT ( 'NONE',  ( -20.00000000000000000, 12.99999999999999289, 4.000000000000000000 ) ) ;
#70615=CARTESIAN_POINT ( 'NONE',  ( -10.13439797861699709, 12.24732348816224459, 10.56111555127041335 ) ) ;
#70632=ORIENTED_EDGE ( 'NONE', *, *, #17205, .T. ) ;
#70693=CARTESIAN_POINT ( 'NONE',  ( -6.880814520906026743, 16.78853395715312757, -1.310034959478670658 ) ) ;
#70698=CARTESIAN_POINT ( 'NONE',  ( 14.63753376598433142, 5.968491795188165305, -7.115311643837329392 ) ) ;
#70705=COLOUR_RGB ( '', 0.66274510, 0.83137255, 0.94901961) ;
#70736=CARTESIAN_POINT ( 'NONE',  ( -15.00099999999999767, 12.99999999999999289, 4.000000000000000000 ) ) ;
#70737=DIRECTION ( 'NONE',  ( 0.000000000000000000, 0.000000000000000000, 1.000000000000000000 ) ) ;
#70752=CIRCLE ( 'NONE', #105243, 1.000000000000000888 ) ;
#70836=CARTESIAN_POINT ( 'NONE',  ( -12.43846442553448917, 9.605310817031497805, -9.412495108624300499 ) ) ;
#70844=CARTESIAN_POINT ( 'NONE',  ( 14.81450998444705114, 22.88381389413250133, -2.101451306568737909 ) ) ;
#70891=CARTESIAN_POINT ( 'NONE',  ( -15.74152552778569181, 22.22013712430564780, 3.418714015797057471 ) ) ;
#70911=CARTESIAN_POINT ( 'NONE',  ( 10.07813983907271904, 12.78063534312769178, 10.57220526254674375 ) ) ;
#70954=CARTESIAN_POINT ( 'NONE',  ( 20.00000000000000000, 12.99999999999999289, 0.000000000000000000 ) ) ;
#70956=CARTESIAN_POINT ( 'NONE',  ( -10.03922187546495515, 13.76626433127010962, -10.52687670776041884 ) ) ;
#70962=ORIENTED_EDGE ( 'NONE', *, *, #28690, .F. ) ;
#70984=CARTESIAN_POINT ( 'NONE',  ( -6.924577185163238724, 9.133260498430180618, -1.057577261889347309 ) ) ;
#71001=VERTEX_POINT ( 'NONE', #11076 ) ;
#71029=CARTESIAN_POINT ( 'NONE',  ( 16.10173312979610216, 5.477053992169538255, -4.739458514411119872 ) ) ;
#71032=CARTESIAN_POINT ( 'NONE',  ( 16.02187926457672873, 4.033883445130388878, -2.088897399353103257 ) ) ;
#71095=CARTESIAN_POINT ( 'NONE',  ( 12.34269817833570215, 7.431323128372670617, 8.323352676710362275 ) ) ;
#71208=CARTESIAN_POINT ( 'NONE',  ( -5.744562646538029504, 13.27032591418342378, -4.000000000000000000 ) ) ;
#71213=CARTESIAN_POINT ( 'NONE',  ( 14.22499876634535809, 6.546626909046912246, -7.657221783520114400 ) ) ;
#71232=CARTESIAN_POINT ( 'NONE',  ( -14.29190075644363489, 21.26710225492988116, -5.626279437295411689 ) ) ;
#71249=SURFACE_STYLE_FILL_AREA ( #46972 ) ;
#71261=CARTESIAN_POINT ( 'NONE',  ( -10.06188242486691209, 12.95829428950482232, -10.57356846006649320 ) ) ;
#71351=ORIENTED_EDGE ( 'NONE', *, *, #101121, .T. ) ;
#71357=CARTESIAN_POINT ( 'NONE',  ( 15.79338834186268592, 22.74219270459462194, 1.000334277943696337 ) ) ;
#71370=CARTESIAN_POINT ( 'NONE',  ( 14.27029591641832518, 3.391655494167657103, -4.551126452496739638 ) ) ;
#71407=CARTESIAN_POINT ( 'NONE',  ( -14.88719829190656796, 23.11045037498637100, 0.5284321866101354681 ) ) ;
#71472=CARTESIAN_POINT ( 'NONE',  ( -10.71234647142379259, 18.37622138056130083, 9.353201953075975794 ) ) ;
#71478=ORIENTED_EDGE ( 'NONE', *, *, #4360, .T. ) ;
#71547=PRESENTATION_STYLE_ASSIGNMENT (( #62951 ) ) ;
#71597=CARTESIAN_POINT ( 'NONE',  ( -29.87930712590254956, 10.71892156097790583, -14.93965356295126945 ) ) ;
#71610=CARTESIAN_POINT ( 'NONE',  ( -16.01290373797195699, 3.743961321038779655, -0.6473776100927145505 ) ) ;
#71614=CARTESIAN_POINT ( 'NONE',  ( 11.09032228048933888, 10.58111460472058951, 9.723575691952698108 ) ) ;
#71634=EDGE_LOOP ( 'NONE', ( #32149, #51943 ) ) ;
#71652=CARTESIAN_POINT ( 'NONE',  ( -13.77096284681266170, 4.875919819223138774, 5.864315561264231924 ) ) ;
#71680=TOROIDAL_SURFACE ( 'NONE', #92402, 7.999999999999998224, 2.000000000000000000 ) ;
#71719=UNCERTAINTY_MEASURE_WITH_UNIT (LENGTH_MEASURE( 1.000000000000000082E-05 ), #85879, 'distance_accuracy_value', 'NONE');
#71730=CARTESIAN_POINT ( 'NONE',  ( 10.43175756363495488, 17.29745240936010120, -9.784780675101240277 ) ) ;
#71778=EDGE_CURVE ( 'NONE', #58722, #92197, #67498, .T. ) ;
#71781=CARTESIAN_POINT ( 'NONE',  ( -11.21715996676264737, 19.86009903824175638, -8.535609670724019438 ) ) ;
#71794=ORIENTED_EDGE ( 'NONE', *, *, #104587, .F. ) ;
#71797=COLOUR_RGB ( '', 0.72549020, 0.75294118, 0.79215686) ;
#71810=CIRCLE ( 'NONE', #73580, 1.999999999999999334 ) ;
#71826=CARTESIAN_POINT ( 'NONE',  ( -14.83882035797429566, 4.620392632309972214, -5.701545570398202756 ) ) ;
#71890=CARTESIAN_POINT ( 'NONE',  ( -15.93251508686752160, 3.184445033434176509, 1.451444771606926754 ) ) ;
#71903=AXIS2_PLACEMENT_3D ( 'NONE', #9599, #52729, #75409 ) ;
#71919=AXIS2_PLACEMENT_3D ( 'NONE', #17964, #75098, #42215 ) ;
#71950=CARTESIAN_POINT ( 'NONE',  ( -16.14327244186403476, 20.71081664949755918, 4.173128809987454169 ) ) ;
#71957=COLOUR_RGB ( '', 0.40784314, 0.44705882, 0.49803922) ;
#71971=CARTESIAN_POINT ( 'NONE',  ( 10.03941004420479466, 13.75456597456546781, 10.52769693539611495 ) ) ;
#71982=CARTESIAN_POINT ( 'NONE',  ( -13.09726150444772053, 8.332934222693051396, 8.848836478249873849 ) ) ;
#72002=EDGE_CURVE ( 'NONE', #87076, #12223, #106731, .T. ) ;
#72086=ORIENTED_EDGE ( 'NONE', *, *, #75675, .T. ) ;
#72122=SURFACE_STYLE_USAGE ( .BOTH. , #55905 ) ;
#72153=CARTESIAN_POINT ( 'NONE',  ( -16.04705908622477750, 4.602417526221017852, 3.432813300977638704 ) ) ;
#72158=CARTESIAN_POINT ( 'NONE',  ( 11.45735263127505021, 9.453390557368402725, 9.374188611738238919 ) ) ;
#72190=ORIENTED_EDGE ( 'NONE', *, *, #3101, .F. ) ;
#72193=SURFACE_STYLE_FILL_AREA ( #16072 ) ;
#72201=CARTESIAN_POINT ( 'NONE',  ( -13.46865723075405441, 5.375093227679321295, 6.499662672654775264 ) ) ;
#72212=SURFACE_SIDE_STYLE ('',( #39332 ) ) ;
#72250=ORIENTED_EDGE ( 'NONE', *, *, #47314, .T. ) ;
#72252=VERTEX_POINT ( 'NONE', #98912 ) ;
#72272=AXIS2_PLACEMENT_3D ( 'NONE', #66083, #74167, #105483 ) ;
#72278=CARTESIAN_POINT ( 'NONE',  ( 10.94020704007013656, 11.19319730264500024, -9.841999159912100836 ) ) ;
#72296=DIRECTION ( 'NONE',  ( 0.000000000000000000, 0.000000000000000000, -1.000000000000000000 ) ) ;
#72321=( NAMED_UNIT ( * ) PLANE_ANGLE_UNIT ( ) SI_UNIT ( $, .RADIAN. ) );
#72326=CARTESIAN_POINT ( 'NONE',  ( -13.53249398123303848, 7.603952788152932740, -8.423294693568777802 ) ) ;
#72339=CARTESIAN_POINT ( 'NONE',  ( -14.37676598790170956, 2.000025124018793843, 4.258993516771657717 ) ) ;
#72340=ORIENTED_EDGE ( 'NONE', *, *, #46677, .F. ) ;
#72361=CARTESIAN_POINT ( 'NONE',  ( -16.10173312979620874, 5.477053992169603980, -4.739458514410732626 ) ) ;
#72416=CARTESIAN_POINT ( 'NONE',  ( 0.000000000000000000, 35.00000000000000000, 0.000000000000000000 ) ) ;
#72424=CARTESIAN_POINT ( 'NONE',  ( -16.02742720722309144, 4.186773460851249240, -2.547561848284168207 ) ) ;
#72463=SURFACE_STYLE_FILL_AREA ( #9305 ) ;
#72476=CARTESIAN_POINT ( 'NONE',  ( -16.10155139016692516, 21.86297139503206921, 0.4316986452184163325 ) ) ;
#72495=CARTESIAN_POINT ( 'NONE',  ( 13.59379325674309946, 24.77301814849831274, -0.6326043077446807938 ) ) ;
#72527=EDGE_CURVE ( 'NONE', #102396, #95018, #105124, .T. ) ;
#72601=CARTESIAN_POINT ( 'NONE',  ( 14.29190075645216673, 6.456385560668102208, 7.561819230143447257 ) ) ;
#72608=EDGE_CURVE ( 'NONE', #43519, #29837, #25955, .T. ) ;
#72631=EDGE_LOOP ( 'NONE', ( #55627, #3150, #73413 ) ) ;
#72680=CARTESIAN_POINT ( 'NONE',  ( 11.94036525613893573, 10.81871501779890110, 9.774666796827323978 ) ) ;
#72710=DIRECTION ( 'NONE',  ( -1.000000000000000000, 0.000000000000000000, 0.000000000000000000 ) ) ;
#72717=CARTESIAN_POINT ( 'NONE',  ( -13.39394377584697615, 3.642522405528196394, 6.675362191836228476 ) ) ;
#72794=CARTESIAN_POINT ( 'NONE',  ( 10.60908664556402137, 14.26876572314972158, -9.938912124272945903 ) ) ;
#72811=CARTESIAN_POINT ( 'NONE',  ( -14.89087697664241183, 23.12189093368899506, -0.5159772465389643736 ) ) ;
#72831=CARTESIAN_POINT ( 'NONE',  ( 14.83962450834943780, 1.409789280635078468, 2.191244623890550081 ) ) ;
#72838=CARTESIAN_POINT ( 'NONE',  ( -10.70840817853610005, 12.38332293683050267, -9.999832067087631060 ) ) ;
#72840=DIRECTION ( 'NONE',  ( 0.000000000000000000, 0.000000000000000000, 1.000000000000000000 ) ) ;
#72896=CIRCLE ( 'NONE', #19545, 0.5000000000000004441 ) ;
#72911=AXIS2_PLACEMENT_3D ( 'NONE', #8482, #74278, #89937 ) ;
#72935=ORIENTED_EDGE ( 'NONE', *, *, #84367, .T. ) ;
#72937=CARTESIAN_POINT ( 'NONE',  ( -16.05785784214673484, 4.775831776474317003, -3.710403933782549846 ) ) ;
#73098=CARTESIAN_POINT ( 'NONE',  ( -20.00000000000000000, 12.99999999999999289, 6.999999999999999112 ) ) ;
#73113=( GEOMETRIC_REPRESENTATION_CONTEXT ( 3 ) GLOBAL_UNCERTAINTY_ASSIGNED_CONTEXT ( ( #91893 ) ) GLOBAL_UNIT_ASSIGNED_CONTEXT ( ( #93905, #18440, #19528 ) ) REPRESENTATION_CONTEXT ( 'NONE', 'WORKASPACE' ) );
#73176=CARTESIAN_POINT ( 'NONE',  ( -3.659159783247727057E-15, 10.71892156097790583, -14.93965356295127478 ) ) ;
#73195=CARTESIAN_POINT ( 'NONE',  ( 10.88890915545092142, 9.027303679840910533, 10.01895505698042754 ) ) ;
#73205=( NAMED_UNIT ( * ) PLANE_ANGLE_UNIT ( ) SI_UNIT ( $, .RADIAN. ) );
#73227=( NAMED_UNIT ( * ) SI_UNIT ( $, .STERADIAN. ) SOLID_ANGLE_UNIT ( ) );
#73234=CARTESIAN_POINT ( 'NONE',  ( -15.99999999999008438, 4.197692598242061202, 4.745459346044129667 ) ) ;
#73246=CARTESIAN_POINT ( 'NONE',  ( 0.000000000000000000, 34.00000000000000711, 0.000000000000000000 ) ) ;
#73320=CARTESIAN_POINT ( 'NONE',  ( 11.23686421050524586, 17.72294612705177030, -8.838715948563953262 ) ) ;
#73360=( NAMED_UNIT ( * ) SI_UNIT ( $, .STERADIAN. ) SOLID_ANGLE_UNIT ( ) );
#73365=CARTESIAN_POINT ( 'NONE',  ( -11.76332149636490598, 11.37125156745868004, -9.882589870049462988 ) ) ;
#73392=CARTESIAN_POINT ( 'NONE',  ( -15.12883458092753841, 3.606451457941037830, -4.265946247306469097 ) ) ;
#73393=EDGE_CURVE ( 'NONE', #24576, #79056, #82797, .T. ) ;
#73395=STYLED_ITEM ( 'NONE', ( #41916 ), #65971 ) ;
#73413=ORIENTED_EDGE ( 'NONE', *, *, #53165, .T. ) ;
#73438=FACE_OUTER_BOUND ( 'NONE', #68204, .T. ) ;
#73452=CARTESIAN_POINT ( 'NONE',  ( -11.08827160299917480, 19.49528337425789104, -8.747723196539737955 ) ) ;
#73469=CARTESIAN_POINT ( 'NONE',  ( -16.02187926457684597, 4.033883445135416856, 2.088897399371232311 ) ) ;
#73540=CARTESIAN_POINT ( 'NONE',  ( 10.29549899077097486, 16.65270026559913319, -9.997496007081116076 ) ) ;
#73541=EDGE_CURVE ( 'NONE', #18205, #91522, #38176, .T. ) ;
#73580=AXIS2_PLACEMENT_3D ( 'NONE', #48063, #21324, #54160 ) ;
#73617=AXIS2_PLACEMENT_3D ( 'NONE', #63297, #28846, #54107 ) ;
#73630=FACE_OUTER_BOUND ( 'NONE', #101835, .T. ) ;
#73655=CARTESIAN_POINT ( 'NONE',  ( 12.00983892818876697, 17.07531081145824103, 9.138738903015008574 ) ) ;
#73684=DIRECTION ( 'NONE',  ( 0.000000000000000000, 0.000000000000000000, 1.000000000000000000 ) ) ;
#73698=AXIS2_PLACEMENT_3D ( 'NONE', #75104, #10378, #57863 ) ;
#73790=DIRECTION ( 'NONE',  ( 0.000000000000000000, 0.000000000000000000, -1.000000000000000000 ) ) ;
#73805=SURFACE_SIDE_STYLE ('',( #57605 ) ) ;
#73866=CARTESIAN_POINT ( 'NONE',  ( 11.80490210714441801, 16.44756287846985288, -9.391209061505895406 ) ) ;
#73900=TOROIDAL_SURFACE ( 'NONE', #39519, 8.000000000000000000, 1.000000000000000000 ) ;
#73902=PRESENTATION_STYLE_ASSIGNMENT (( #81452 ) ) ;
#73904=CARTESIAN_POINT ( 'NONE',  ( -13.51713435554249720, 20.10123978775306242, -7.061460334258709004 ) ) ;
#73919=CARTESIAN_POINT ( 'NONE',  ( 12.60424787139770153, 18.50010450913565307, -8.389313221795688946 ) ) ;
#73991=CARTESIAN_POINT ( 'NONE',  ( -11.79034953273680664, 6.758388275560107239, 9.087657628957359179 ) ) ;
#74013=DIRECTION ( 'NONE',  ( -0.000000000000000000, -1.000000000000000000, -0.000000000000000000 ) ) ;
#74025=ORIENTED_EDGE ( 'NONE', *, *, #25686, .T. ) ;
#74118=ORIENTED_EDGE ( 'NONE', *, *, #10077, .F. ) ;
#74167=DIRECTION ( 'NONE',  ( -1.000000000000000000, -0.000000000000000000, -0.000000000000000000 ) ) ;
#74193=CARTESIAN_POINT ( 'NONE',  ( 16.00000000000008882, 2.437231117875652053, -5.694551215225447827 ) ) ;
#74204=DIRECTION ( 'NONE',  ( 0.000000000000000000, 1.000000000000000000, 0.000000000000000000 ) ) ;
#74245=CARTESIAN_POINT ( 'NONE',  ( 16.14595037822613932, 20.23371447307438586, 4.922994507617745263 ) ) ;
#74252=ORIENTED_EDGE ( 'NONE', *, *, #19350, .F. ) ;
#74278=DIRECTION ( 'NONE',  ( -0.000000000000000000, -1.000000000000000000, -0.000000000000000000 ) ) ;
#74279=CARTESIAN_POINT ( 'NONE',  ( 14.29190075645216851, 12.99999999999999289, 0.000000000000000000 ) ) ;
#74282=EDGE_CURVE ( 'NONE', #80083, #95018, #99499, .T. ) ;
#74387=ORIENTED_EDGE ( 'NONE', *, *, #69607, .F. ) ;
#74388=FILL_AREA_STYLE_COLOUR ( '', #19128 ) ;
#74390=CARTESIAN_POINT ( 'NONE',  ( 13.77302195033687937, 22.96143443510463200, -1.023475060063897768 ) ) ;
#74434=CARTESIAN_POINT ( 'NONE',  ( -13.59263768938421713, 24.77097348052605597, -0.6145898399614796448 ) ) ;
#74448=CARTESIAN_POINT ( 'NONE',  ( 13.63566925393123164, 20.28444567501044915, -6.862276106173472279 ) ) ;
#74505=DIRECTION ( 'NONE',  ( 1.000000000000000000, -0.000000000000000000, -0.000000000000000000 ) ) ;
#74509=DIRECTION ( 'NONE',  ( 0.000000000000000000, 0.8267102254928009319, -0.5626279437298172814 ) ) ;
#74510=B_SPLINE_CURVE_WITH_KNOTS ( 'NONE', 3,
 ( #44028, #36511, #85018, #28960, #94178, #76920, #68852, #20344, #53190, #94727, #73, #46160, #87684, #54752, #55281, #70956, #79572, #13235, #14291, #82079, #96313, #79048, #87155, #98275, #73452, #62354, #37571, #45632, #95244, #57800, #106350, #38096, #62878, #29477, #21376, #5167, #32512, #40570, #47195, #54214, #103847, #29992, #95769, #21905, #13764, #63421, #38609, #41109, #65384, #24433, #33044, #46673, #5685, #80095, #57265, #71472, #104372, #22441, #16290, #30523, #88210, #7653, #4640, #70436, #90188, #12703, #49175, #8198, #73991, #65910, #98790, #24947, #78507, #103331, #17911, #82628 ),
 .UNSPECIFIED., .F., .F.,
 ( 4, 2, 2, 2, 2, 2, 2, 2, 2, 2, 2, 2, 2, 2, 2, 2, 2, 2, 2, 2, 2, 2, 2, 2, 2, 2, 2, 2, 2, 2, 2, 2, 2, 2, 2, 2, 2, 4 ),
 ( 0.02393199801744600591, 0.02587788593328142414, 0.02782377384911684237, 0.02976966176495226060, 0.03171554968078767883, 0.03366143759662310053, 0.03560732551245852223, 0.03755321342829394393, 0.03852615738621165825, 0.03949910134412936563, 0.04144498925996478733, 0.04339087717580021597, 0.04436382113371792335, 0.04533676509163563073, 0.04728265300747104549, 0.04825559696538875981, 0.04922854092330646719, 0.05117442883914188889, 0.05312031675497731753, 0.05506620467081274617, 0.05603914862873046049, 0.05701209258664816787, 0.05895798050248358957, 0.06090386841831902515, 0.06187681237623673253, 0.06284975633415444685, 0.06479564424998987548, 0.06674153216582529025, 0.06868742008166071888, 0.07063330799749614752, 0.07257919591333157616, 0.07452508382916700480, 0.07647097174500241956, 0.07841685966083784820, 0.08036274757667327684, 0.08230863549250871936, 0.08425452340834414799, 0.08620041132417957663 ),
 .UNSPECIFIED. ) ;
#74532=MECHANICAL_DESIGN_GEOMETRIC_PRESENTATION_REPRESENTATION('',(#5631),#79698);
#74539=CARTESIAN_POINT ( 'NONE',  ( -15.85122647056015488, 4.114663126770048862, 4.288211754903009876 ) ) ;
#74544=( NAMED_UNIT ( * ) PLANE_ANGLE_UNIT ( ) SI_UNIT ( $, .RADIAN. ) );
#74607=CARTESIAN_POINT ( 'NONE',  ( 11.89626370526795185, 6.535353899124712207, -8.953647278333551895 ) ) ;
#74639=ORIENTED_EDGE ( 'NONE', *, *, #91450, .T. ) ;
#74684=CARTESIAN_POINT ( 'NONE',  ( 19.50000000000000000, 12.99999999999999467, -7.500000000000000000 ) ) ;
#74855=CARTESIAN_POINT ( 'NONE',  ( -19.50000000000000000, 12.99999999999999289, 0.000000000000000000 ) ) ;
#74858=CARTESIAN_POINT ( 'NONE',  ( 15.35683281173218973, 2.987586243233406602, 2.780571802877160881 ) ) ;
#74862=VERTEX_POINT ( 'NONE', #52691 ) ;
#74913=CARTESIAN_POINT ( 'NONE',  ( 15.79261075262969527, 4.810720122700525181, 5.431533035173099044 ) ) ;
#74915=CARTESIAN_POINT ( 'NONE',  ( 14.42176108926845757, 21.45314454056250142, -5.349682917995179032 ) ) ;
#74960=CARTESIAN_POINT ( 'NONE',  ( -13.02750095097563587, 21.68772054867059751, -4.979202728191992833 ) ) ;
#74980=CARTESIAN_POINT ( 'NONE',  ( 20.00100000000000477, 12.99999999999999289, 0.000000000000000000 ) ) ;
#74983=CYLINDRICAL_SURFACE ( 'NONE', #89321, 10.00000000000000178 ) ;
#75064=CARTESIAN_POINT ( 'NONE',  ( -16.04706613565624451, 4.602530725778174236, 3.432994500434128238 ) ) ;
#75088=CARTESIAN_POINT ( 'NONE',  ( 14.89106961510137062, 23.12249028321820532, -0.5049748053441320828 ) ) ;
#75098=DIRECTION ( 'NONE',  ( 1.000000000000000000, -0.000000000000000000, -0.000000000000000000 ) ) ;
#75104=CARTESIAN_POINT ( 'NONE',  ( 20.00000000000000000, 12.99999999999999289, 0.000000000000000000 ) ) ;
#75124=CARTESIAN_POINT ( 'NONE',  ( 16.03926360544220486, 4.449054639248220866, 3.142406330836459372 ) ) ;
#75152=FILL_AREA_STYLE_COLOUR ( '', #97828 ) ;
#75171=FILL_AREA_STYLE ('',( #26160 ) ) ;
#75198=ORIENTED_EDGE ( 'NONE', *, *, #4807, .F. ) ;
#75207=DIRECTION ( 'NONE',  ( 5.710694965406835788E-17, -0.7561819230143446147, -0.6543614439331888466 ) ) ;
#75241=CARTESIAN_POINT ( 'NONE',  ( -15.51358515996878573, 2.608314655049470687, -0.4154586159635258458 ) ) ;
#75409=DIRECTION ( 'NONE',  ( 0.000000000000000000, 0.000000000000000000, 1.000000000000000000 ) ) ;
#75463=CARTESIAN_POINT ( 'NONE',  ( 13.10137785350333672, 21.81893118045620028, -4.741824893705198107 ) ) ;
#75505=CARTESIAN_POINT ( 'NONE',  ( -13.77400323909053981, 22.96304823656091543, 1.009181881714518836 ) ) ;
#75536=CARTESIAN_POINT ( 'NONE',  ( -15.35683281173281500, 2.987586243231799443, -2.780571802872013887 ) ) ;
#75542=ORIENTED_EDGE ( 'NONE', *, *, #92928, .F. ) ;
#75561=CARTESIAN_POINT ( 'NONE',  ( 6.241401647512419437, 15.44846771700987809, 3.173604836376809679 ) ) ;
#75567=PRESENTATION_STYLE_ASSIGNMENT (( #27599 ) ) ;
#75570=ORIENTED_EDGE ( 'NONE', *, *, #22073, .T. ) ;
#75675=EDGE_CURVE ( 'NONE', #18398, #105603, #96120, .T. ) ;
#75742=MECHANICAL_DESIGN_GEOMETRIC_PRESENTATION_REPRESENTATION('',(#48159),#24107);
#75752=VERTEX_POINT ( 'NONE', #67047 ) ;
#75787=CARTESIAN_POINT ( 'NONE',  ( -14.65167870846473441, 2.576877453023403319, -3.244758155282446932 ) ) ;
#75791=CARTESIAN_POINT ( 'NONE',  ( -16.11715839250255655, 21.56713793042588279, -2.163674775881553103 ) ) ;
#75799=CARTESIAN_POINT ( 'NONE',  ( 9.797174393178825657E-16, 34.00000000000000000, 8.000000000000000000 ) ) ;
#75846=UNCERTAINTY_MEASURE_WITH_UNIT (LENGTH_MEASURE( 1.000000000000000082E-05 ), #26225, 'distance_accuracy_value', 'NONE');
#75887=SURFACE_SIDE_STYLE ('',( #60273 ) ) ;
#75941=PRESENTATION_STYLE_ASSIGNMENT (( #85646 ) ) ;
#75994=CARTESIAN_POINT ( 'NONE',  ( 13.26904190672035888, 24.19056840945213338, -3.252525987528880780 ) ) ;
#76035=CARTESIAN_POINT ( 'NONE',  ( -14.81362254366326248, 21.99737691636699566, -4.398778852034027409 ) ) ;
#76057=DIRECTION ( 'NONE',  ( 1.000000000000000000, 0.000000000000000000, 0.000000000000000000 ) ) ;
#76148=CIRCLE ( 'NONE', #57190, 2.000000000000000000 ) ;
#76162=CARTESIAN_POINT ( 'NONE',  ( 14.78104354000378251, 22.77915615417240147, 2.489457476759114218 ) ) ;
#76184=CARTESIAN_POINT ( 'NONE',  ( 16.05785784214673129, 4.775831776474256607, -3.710403933782447261 ) ) ;
#76193=ORIENTED_EDGE ( 'NONE', *, *, #21568, .F. ) ;
#76228=STYLED_ITEM ( 'NONE', ( #6267 ), #52016 ) ;
#76310=PRESENTATION_STYLE_ASSIGNMENT (( #9433 ) ) ;
#76415=FACE_OUTER_BOUND ( 'NONE', #20743, .T. ) ;
#76419=EDGE_CURVE ( 'NONE', #39650, #92807, #3195, .T. ) ;
#76420=PRESENTATION_STYLE_ASSIGNMENT (( #36550 ) ) ;
#76448=CARTESIAN_POINT ( 'NONE',  ( 6.769785244694104698, 9.417081608196284037, -1.797443303175162876 ) ) ;
#76460=CARTESIAN_POINT ( 'NONE',  ( 15.43760447746161546, 2.782577468887291072, 1.950845582985621940 ) ) ;
#76521=CARTESIAN_POINT ( 'NONE',  ( 11.88722850048356960, 16.71180228297125936, 9.289706601079268822 ) ) ;
#76524=CARTESIAN_POINT ( 'NONE',  ( 0.000000000000000000, -3.035766082959412415E-15, 8.000000000000000000 ) ) ;
#76561=CARTESIAN_POINT ( 'NONE',  ( -12.34390528153764421, 20.39976729514925680, 6.763647308493165866 ) ) ;
#76598=TOROIDAL_SURFACE ( 'NONE', #26691, 9.500000000000000000, 2.000000000000000000 ) ;
#76613=EDGE_CURVE ( 'NONE', #43945, #18398, #29120, .T. ) ;
#76617=CARTESIAN_POINT ( 'NONE',  ( 6.561040333616081632, 16.17219201178938448, 2.450206053579249144 ) ) ;
#76646=EDGE_LOOP ( 'NONE', ( #57041, #86911, #34213, #8334 ) ) ;
#76663=ORIENTED_EDGE ( 'NONE', *, *, #12497, .F. ) ;
#76732=AXIS2_PLACEMENT_3D ( 'NONE', #1812, #84353, #26679 ) ;
#76844=AXIS2_PLACEMENT_3D ( 'NONE', #30271, #48538, #63160 ) ;
#76852=PRODUCT_DEFINITION_SHAPE ( 'NONE', 'NONE',  #81205 ) ;
#76857=VERTEX_POINT ( 'NONE', #46449 ) ;
#76858=DIRECTION ( 'NONE',  ( -1.224646799147353454E-16, 0.000000000000000000, -1.000000000000000000 ) ) ;
#76910=CARTESIAN_POINT ( 'NONE',  ( 14.29190075645216851, 12.99999999999999289, 0.000000000000000000 ) ) ;
#76915=CARTESIAN_POINT ( 'NONE',  ( -16.14595037866683924, 6.775806037745283561, 6.185188124841822344 ) ) ;
#76920=CARTESIAN_POINT ( 'NONE',  ( -12.51486567167142283, 5.260823752922433982, -8.146766300809140660 ) ) ;
#76921=VECTOR ( 'NONE', #104153, 1000.000000000000000 ) ;
#76931=CARTESIAN_POINT ( 'NONE',  ( -19.50000000000000000, 12.99999999999999289, 0.000000000000000000 ) ) ;
#77008=AXIS2_PLACEMENT_3D ( 'NONE', #85814, #19512, #43732 ) ;
#77011=STYLED_ITEM ( 'NONE', ( #77884 ), #101792 ) ;
#77061=CARTESIAN_POINT ( 'NONE',  ( 12.35017993402607317, 20.41240526430823365, 6.749814137266258562 ) ) ;
#77108=CARTESIAN_POINT ( 'NONE',  ( -14.71476209775949151, 21.86062043620323436, 4.643882332649849509 ) ) ;
#77117=ORIENTED_EDGE ( 'NONE', *, *, #13590, .T. ) ;
#77121=DIRECTION ( 'NONE',  ( 1.000000000000000000, 0.000000000000000000, 0.000000000000000000 ) ) ;
#77165=CARTESIAN_POINT ( 'NONE',  ( 5.763898627153208665, 13.53725938914606353, 3.972597389303859750 ) ) ;
#77176=CARTESIAN_POINT ( 'NONE',  ( -20.00000000000000000, 12.99999999999999467, 7.500000000000000000 ) ) ;
#77212=CIRCLE ( 'NONE', #49628, 8.750000000000033751 ) ;
#77240=CARTESIAN_POINT ( 'NONE',  ( -12.29994342143133856, 5.683500474366485200, -8.444376441994753790 ) ) ;
#77244=UNCERTAINTY_MEASURE_WITH_UNIT (LENGTH_MEASURE( 1.000000000000000082E-05 ), #64804, 'distance_accuracy_value', 'NONE');
#77266=FILL_AREA_STYLE ('',( #101541 ) ) ;
#77278=DIRECTION ( 'NONE',  ( -1.000000000000000000, 0.000000000000000000, 0.000000000000000000 ) ) ;
#77279=SURFACE_SIDE_STYLE ('',( #44384 ) ) ;
#77306=DIRECTION ( 'NONE',  ( 3.997486475784785298E-16, 0.5626279437268310035, 0.8267102254948331952 ) ) ;
#77328=ORIENTED_EDGE ( 'NONE', *, *, #101121, .F. ) ;
#77336=CARTESIAN_POINT ( 'NONE',  ( -11.46558483138156603, 15.01111260705223849, -9.824584598569959581 ) ) ;
#77344=CARTESIAN_POINT ( 'NONE',  ( 16.12882272094003611, 21.28108484452593174, -2.990375923983669360 ) ) ;
#77393=CARTESIAN_POINT ( 'NONE',  ( -16.14595037822576273, 20.23371447306055870, -4.922994507639441686 ) ) ;
#77456=( NAMED_UNIT ( * ) PLANE_ANGLE_UNIT ( ) SI_UNIT ( $, .RADIAN. ) );
#77502=SURFACE_STYLE_FILL_AREA ( #100692 ) ;
#77540=CARTESIAN_POINT ( 'NONE',  ( 15.88105853605375906, 3.776612129046490907, 3.593753328290308247 ) ) ;
#77556=CARTESIAN_POINT ( 'NONE',  ( -14.58934900096332221, 5.487773041241340799, -6.668063844691409336 ) ) ;
#77575=VERTEX_POINT ( 'NONE', #8370 ) ;
#77603=CARTESIAN_POINT ( 'NONE',  ( 12.06580744102501157, 19.80956736058091749, 7.339492630969226106 ) ) ;
#77646=CARTESIAN_POINT ( 'NONE',  ( -10.23422886744656068, 16.30953289564795483, 10.09620275774212139 ) ) ;
#77682=ORIENTED_EDGE ( 'NONE', *, *, #65720, .F. ) ;
#77733=CARTESIAN_POINT ( 'NONE',  ( 14.11595029532510992, 2.410436752314608633, -5.024000119269073750 ) ) ;
#77857=CARTESIAN_POINT ( 'NONE',  ( -16.14595037822608248, 20.23371447308014481, 4.922994507609256054 ) ) ;
#77875=FILL_AREA_STYLE ('',( #44990 ) ) ;
#77877=CARTESIAN_POINT ( 'NONE',  ( 16.11139379967212548, 21.68073351270184546, -1.735103873172237465 ) ) ;
#77884=PRESENTATION_STYLE_ASSIGNMENT (( #62253 ) ) ;
#77926=CARTESIAN_POINT ( 'NONE',  ( -15.64030048137735207, 21.26710225493047091, -5.626279437303003839 ) ) ;
#77946=CARTESIAN_POINT ( 'NONE',  ( 12.49205219477306095, 22.71772351425832781, 5.929143317787740841 ) ) ;
#77965=DIRECTION ( 'NONE',  ( 1.000000000000000000, 0.000000000000000000, -1.224646799147353207E-16 ) ) ;
#77985=VERTEX_POINT ( 'NONE', #7702 ) ;
#78016=EDGE_LOOP ( 'NONE', ( #87936, #42442, #72250, #81877 ) ) ;
#78045=CARTESIAN_POINT ( 'NONE',  ( 11.46409645960816626, 12.99999999999817923, -10.00000000000000178 ) ) ;
#78055=FACE_OUTER_BOUND ( 'NONE', #8328, .T. ) ;
#78061=CARTESIAN_POINT ( 'NONE',  ( 16.14595037866564908, 6.775806037743102195, -6.185188124844921198 ) ) ;
#78124=CARTESIAN_POINT ( 'NONE',  ( 11.12323130174675256, 19.59210383280182910, 8.689352701389447375 ) ) ;
#78164=CARTESIAN_POINT ( 'NONE',  ( -10.82859631130528655, 18.75128085564791292, 9.171573219068584137 ) ) ;
#78179=PRESENTATION_STYLE_ASSIGNMENT (( #43686 ) ) ;
#78221=MECHANICAL_DESIGN_GEOMETRIC_PRESENTATION_REPRESENTATION('',(#62995),#31742);
#78240=ADVANCED_BREP_SHAPE_REPRESENTATION ( '', ( #88291, #10728 ), #47146 ) ;
#78250=CARTESIAN_POINT ( 'NONE',  ( 11.92367304074753598, 6.475998827537138958, -8.920379189304513901 ) ) ;
#78275=ORIENTED_EDGE ( 'NONE', *, *, #48425, .F. ) ;
#78307=DIRECTION ( 'NONE',  ( 0.000000000000000000, 0.000000000000000000, 1.000000000000000000 ) ) ;
#78390=ADVANCED_FACE ( 'NONE', ( #13546 ), #17290, .T. ) ;
#78392=ORIENTED_EDGE ( 'NONE', *, *, #57181, .T. ) ;
#78395=CARTESIAN_POINT ( 'NONE',  ( 14.66373388272351441, 22.41296547518495075, 3.537915336787654574 ) ) ;
#78468=CARTESIAN_POINT ( 'NONE',  ( 11.09614018901123345, 8.445801345000054638, 9.827501351701041443 ) ) ;
#78507=CARTESIAN_POINT ( 'NONE',  ( -13.25913213669673674, 3.878272661654435183, 6.943805427999512503 ) ) ;
#78549=DIRECTION ( 'NONE',  ( 0.000000000000000000, 1.000000000000000000, -1.224646799147353207E-16 ) ) ;
#78587=VERTEX_POINT ( 'NONE', #70613 ) ;
#78634=CARTESIAN_POINT ( 'NONE',  ( -16.02333492353049138, 4.076663811951506844, -2.240748598612071429 ) ) ;
#78638=CARTESIAN_POINT ( 'NONE',  ( 12.32576155738170520, 22.37954607397292150, 6.324133886429093465 ) ) ;
#78683=CARTESIAN_POINT ( 'NONE',  ( -14.41717015766604604, 21.44666408806050129, 5.359973845151366767 ) ) ;
#78769=CARTESIAN_POINT ( 'NONE',  ( 13.38407207131497501, 3.659884948878311839, -6.694498904168558973 ) ) ;
#78798=ORIENTED_EDGE ( 'NONE', *, *, #42849, .F. ) ;
#78801=AXIS2_PLACEMENT_3D ( 'NONE', #61869, #78549, #29517 ) ;
#78809=CARTESIAN_POINT ( 'NONE',  ( 20.00000000000000000, 12.99999999999999289, 0.000000000000000000 ) ) ;
#78816=CARTESIAN_POINT ( 'NONE',  ( 14.29190075645646907, 21.26710225494832329, -5.626279437268317807 ) ) ;
#78818=CARTESIAN_POINT ( 'NONE',  ( -15.55348733900250124, 4.754504522411744816, -5.683216791855722150 ) ) ;
#78874=CARTESIAN_POINT ( 'NONE',  ( 18.00000000000000355, 12.99999999999999289, 0.000000000000000000 ) ) ;
#78925=( NAMED_UNIT ( * ) PLANE_ANGLE_UNIT ( ) SI_UNIT ( $, .RADIAN. ) );
#78938=( NAMED_UNIT ( * ) PLANE_ANGLE_UNIT ( ) SI_UNIT ( $, .RADIAN. ) );
#78977=CARTESIAN_POINT ( 'NONE',  ( -14.86018380392287241, 23.02630934695395126, 1.319261379087336206 ) ) ;
#78996=STYLED_ITEM ( 'NONE', ( #73902 ), #5817 ) ;
#78999=CARTESIAN_POINT ( 'NONE',  ( 13.01536098179566281, 4.316280655867278604, 7.368423276989370940 ) ) ;
#79015=DIRECTION ( 'NONE',  ( 1.000000000000000000, 0.000000000000000000, 0.000000000000000000 ) ) ;
#79043=FILL_AREA_STYLE_COLOUR ( '', #17672 ) ;
#79048=CARTESIAN_POINT ( 'NONE',  ( -10.55482376525340094, 17.82747234158580696, -9.593668801698457926 ) ) ;
#79053=EDGE_CURVE ( 'NONE', #43916, #47808, #63767, .T. ) ;
#79056=VERTEX_POINT ( 'NONE', #73098 ) ;
#79078=CARTESIAN_POINT ( 'NONE',  ( -6.879789419156628227, 9.213335847798312273, -1.315101155215614881 ) ) ;
#79100=CARTESIAN_POINT ( 'NONE',  ( 12.80748990434369716, 8.843371560882051341, -9.113774775587792476 ) ) ;
#79122=CARTESIAN_POINT ( 'NONE',  ( 15.31219705632019235, 3.104419271452464990, -3.118400172706347284 ) ) ;
#79123=CARTESIAN_POINT ( 'NONE',  ( 1.489880555935390203E-15, 34.19642918197134662, 12.16579798332631945 ) ) ;
#79139=ORIENTED_EDGE ( 'NONE', *, *, #37328, .T. ) ;
#79178=ADVANCED_FACE ( 'NONE', ( #11038 ), #11107, .F. ) ;
#79186=CARTESIAN_POINT ( 'NONE',  ( 14.04890433743131872, 4.428206803761019827, 5.208796089510552285 ) ) ;
#79226=CARTESIAN_POINT ( 'NONE',  ( -14.35785620000130969, 3.948300967446466636, 4.282865182316123231 ) ) ;
#79252=DIRECTION ( 'NONE',  ( 0.000000000000000000, 0.000000000000000000, -1.000000000000000000 ) ) ;
#79281=CARTESIAN_POINT ( 'NONE',  ( 6.321708934325914520, 15.64391652793080034, -3.012444762083619221 ) ) ;
#79300=ORIENTED_EDGE ( 'NONE', *, *, #80792, .T. ) ;
#79303=CARTESIAN_POINT ( 'NONE',  ( -6.925232610679096901, 16.86791138880112584, -1.053462737155420381 ) ) ;
#79307=CARTESIAN_POINT ( 'NONE',  ( 11.79976288999368528, 6.746418028092196373, -9.068817350359527296 ) ) ;
#79354=EDGE_CURVE ( 'NONE', #43945, #23419, #46992, .T. ) ;
#79415=FACE_OUTER_BOUND ( 'NONE', #28721, .T. ) ;
#79447=CARTESIAN_POINT ( 'NONE',  ( -11.43540210466514218, 13.32389838193370579, -9.996488892513244906 ) ) ;
#79456=CARTESIAN_POINT ( 'NONE',  ( 15.76884112491604562, 22.48937974161447073, -2.489079047138151424 ) ) ;
#79467=CARTESIAN_POINT ( 'NONE',  ( 14.68864207889602724, 1.585199049501273105, -3.034365436886341971 ) ) ;
#79473=AXIS2_PLACEMENT_3D ( 'NONE', #103216, #39016, #30406 ) ;
#79509=CARTESIAN_POINT ( 'NONE',  ( -16.12871211736532118, 21.28428926969061408, 2.982820907284539746 ) ) ;
#79526=CARTESIAN_POINT ( 'NONE',  ( 11.27810499350236384, 20.00336526192103648, 8.427062764154296559 ) ) ;
#79538=DIRECTION ( 'NONE',  ( 0.000000000000000000, 0.000000000000000000, -1.000000000000000000 ) ) ;
#79572=CARTESIAN_POINT ( 'NONE',  ( -10.03820104914963984, 14.09414544201339758, -10.49954271116794580 ) ) ;
#79622=MECHANICAL_DESIGN_GEOMETRIC_PRESENTATION_REPRESENTATION('',(#22850),#19407);
#79642=ADVANCED_FACE ( 'NONE', ( #2147 ), #20946, .T. ) ;
#79651=CARTESIAN_POINT ( 'NONE',  ( 16.02800152098294717, 4.194749798097111793, -2.552193233489410407 ) ) ;
#79696=( NAMED_UNIT ( * ) SI_UNIT ( $, .STERADIAN. ) SOLID_ANGLE_UNIT ( ) );
#79698=( GEOMETRIC_REPRESENTATION_CONTEXT ( 3 ) GLOBAL_UNCERTAINTY_ASSIGNED_CONTEXT ( ( #88374 ) ) GLOBAL_UNIT_ASSIGNED_CONTEXT ( ( #92104, #40367, #7451 ) ) REPRESENTATION_CONTEXT ( 'NONE', 'WORKASPACE' ) );
#79699=DIRECTION ( 'NONE',  ( 0.000000000000000000, 0.000000000000000000, 1.000000000000000000 ) ) ;
#79715=CARTESIAN_POINT ( 'NONE',  ( 12.45811832932207608, 7.201502433278960780, 8.165472859347126189 ) ) ;
#79744=ORIENTED_EDGE ( 'NONE', *, *, #56761, .F. ) ;
#79753=CARTESIAN_POINT ( 'NONE',  ( -13.12744080586892537, 8.268327554377737698, 8.825841405457195421 ) ) ;
#79832=CARTESIAN_POINT ( 'NONE',  ( 10.29730654639191378, 11.29257185708027755, -10.47295643394610209 ) ) ;
#79868=PRESENTATION_STYLE_ASSIGNMENT (( #37871 ) ) ;
#79872=( NAMED_UNIT ( * ) SI_UNIT ( $, .STERADIAN. ) SOLID_ANGLE_UNIT ( ) );
#79879=CARTESIAN_POINT ( 'NONE',  ( -13.12174090438720953, 8.291105618454766457, -8.825937222380286329 ) ) ;
#79888=CARTESIAN_POINT ( 'NONE',  ( -14.63960045772152263, 2.604522098982320344, 3.217332696247229062 ) ) ;
#79910=ORIENTED_EDGE ( 'NONE', *, *, #91542, .T. ) ;
#79917=CARTESIAN_POINT ( 'NONE',  ( -15.72218280906590593, 5.595371698621922185, -6.516822309426167692 ) ) ;
#79931=EDGE_LOOP ( 'NONE', ( #95908, #97038, #101125, #4753 ) ) ;
#79937=CARTESIAN_POINT ( 'NONE',  ( 16.07917213302808790, 5.118112109469848292, 4.258304778695062964 ) ) ;
#80022=ORIENTED_EDGE ( 'NONE', *, *, #72002, .F. ) ;
#80027=CARTESIAN_POINT ( 'NONE',  ( -14.77180908113605362, 22.75028154196801822, 2.587654188242820563 ) ) ;
#80047=CARTESIAN_POINT ( 'NONE',  ( 11.68384993704314567, 21.00149377200780165, 7.699446549790801342 ) ) ;
#80083=VERTEX_POINT ( 'NONE', #29036 ) ;
#80095=CARTESIAN_POINT ( 'NONE',  ( -11.27547330588923913, 20.00714579501138246, 8.438865621785792470 ) ) ;
#80153=CARTESIAN_POINT ( 'NONE',  ( 13.69035467268384032, 7.353514859321120589, -8.258215124936253204 ) ) ;
#80170=CARTESIAN_POINT ( 'NONE',  ( 16.05785784214673129, 4.775831776474257495, -3.710403933782447261 ) ) ;
#80174=CARTESIAN_POINT ( 'NONE',  ( 16.05785784214651812, 4.775831776474217527, -3.710403933782383756 ) ) ;
#80176=CARTESIAN_POINT ( 'NONE',  ( 0.000000000000000000, 10.71892156097790583, 14.93965356295127478 ) ) ;
#80219=( LENGTH_UNIT ( ) NAMED_UNIT ( * ) SI_UNIT ( .MILLI., .METRE. ) );
#80270=DIRECTION ( 'NONE',  ( -1.000000000000000000, 0.000000000000000000, 0.000000000000000000 ) ) ;
#80353=CARTESIAN_POINT ( 'NONE',  ( 12.06665022449565150, 19.81138878756394917, -7.337788469117366930 ) ) ;
#80395=DIRECTION ( 'NONE',  ( 0.06744659395731769647, -0.6445107564549842349, 0.7616146281272312413 ) ) ;
#80400=FILL_AREA_STYLE_COLOUR ( '', #65213 ) ;
#80402=CARTESIAN_POINT ( 'NONE',  ( -11.93081618615098449, 6.460648502060225340, -8.911612056469465415 ) ) ;
#80443=CARTESIAN_POINT ( 'NONE',  ( -15.85122647056153156, 4.114663126756377132, -4.288211754877429449 ) ) ;
#80458=COLOUR_RGB ( '', 0.09019608, 0.27058824, 0.51372549) ;
#80464=CARTESIAN_POINT ( 'NONE',  ( 16.14595037822608603, 6.785770140112262538, 6.193810554583017769 ) ) ;
#80468=CARTESIAN_POINT ( 'NONE',  ( -13.63548989270066158, 20.28416372052714323, 6.862577965993339468 ) ) ;
#80477=ORIENTED_EDGE ( 'NONE', *, *, #48345, .F. ) ;
#80500=CARTESIAN_POINT ( 'NONE',  ( -15.88105853605327766, 3.776612129045478827, -3.593753328288301407 ) ) ;
#80517=CARTESIAN_POINT ( 'NONE',  ( 15.22818746203033591, 3.929489829918852983, -4.609438620807785547 ) ) ;
#80519=DIRECTION ( 'NONE',  ( 1.000000000000000000, 0.000000000000000000, 0.000000000000000000 ) ) ;
#80532=CIRCLE ( 'NONE', #47741, 8.750000000000023093 ) ;
#80555=CARTESIAN_POINT ( 'NONE',  ( -16.10099483391875808, 21.87267635329494198, 0.2108314046237644568 ) ) ;
#80576=CARTESIAN_POINT ( 'NONE',  ( 13.00302362776394816, 4.344380092746527922, -7.377937999068717723 ) ) ;
#80586=AXIS2_PLACEMENT_3D ( 'NONE', #20902, #53737, #86665 ) ;
#80664=( NAMED_UNIT ( * ) SI_UNIT ( $, .STERADIAN. ) SOLID_ANGLE_UNIT ( ) );
#80685=CARTESIAN_POINT ( 'NONE',  ( 11.48763805786517800, 14.98694146577114950, 9.807607930316668998 ) ) ;
#80714=ORIENTED_EDGE ( 'NONE', *, *, #84416, .T. ) ;
#80752=CARTESIAN_POINT ( 'NONE',  ( -29.99397490504469133, 1.005902684993158047, -14.99698745252234033 ) ) ;
#80770=CARTESIAN_POINT ( 'NONE',  ( 12.80519380915450078, 6.532562108030647074, 7.664627944857000053 ) ) ;
#80776=SURFACE_STYLE_USAGE ( .BOTH. , #105586 ) ;
#80792=EDGE_CURVE ( 'NONE', #68971, #78587, #58691, .T. ) ;
#80809=CARTESIAN_POINT ( 'NONE',  ( -10.52472853799489094, 10.25003985121227856, 10.32210089392438412 ) ) ;
#80873=ADVANCED_FACE ( 'NONE', ( #60125, #51987 ), #9387, .F. ) ;
#80886=CARTESIAN_POINT ( 'NONE',  ( -6.996281870428058269, 16.99350475219344148, -0.2643931112039912268 ) ) ;
#80891=CARTESIAN_POINT ( 'NONE',  ( 10.36448145403546839, 10.96207040866273630, -10.43058775967166873 ) ) ;
#80921=STYLED_ITEM ( 'NONE', ( #64074 ), #32799 ) ;
#80930=CARTESIAN_POINT ( 'NONE',  ( 14.68532172035349959, 1.589195250043442087, -3.050719247005512003 ) ) ;
#80939=CARTESIAN_POINT ( 'NONE',  ( -11.10308954262782599, 8.426119584744682811, -9.821132823669547207 ) ) ;
#81001=CARTESIAN_POINT ( 'NONE',  ( 1.836601268058450879E-15, 1.005902684993156715, 14.99698745252234566 ) ) ;
#81032=CARTESIAN_POINT ( 'NONE',  ( -15.92744347757545853, 3.245128719852651056, -1.809264762054266562 ) ) ;
#81047=CARTESIAN_POINT ( 'NONE',  ( 14.46400437354099644, 2.949852469114451647, -3.921916857588237715 ) ) ;
#81053=ADVANCED_FACE ( 'NONE', ( #83298 ), #27227, .T. ) ;
#81089=AXIS2_PLACEMENT_3D ( 'NONE', #67415, #100291, #59319 ) ;
#81111=CARTESIAN_POINT ( 'NONE',  ( 13.92251770464348937, 2.731537496222212535, -5.554657554294999855 ) ) ;
#81181=CARTESIAN_POINT ( 'NONE',  ( -6.880652008360423899, 9.211763961707752912, 1.310808761845548620 ) ) ;
#81205=PRODUCT_DEFINITION ( 'UNKNOWN', '', #59335, #51015 ) ;
#81237=CARTESIAN_POINT ( 'NONE',  ( 14.29190075645216851, 12.99999999999999289, 0.000000000000000000 ) ) ;
#81266=CARTESIAN_POINT ( 'NONE',  ( 16.13482245078226285, 21.13350007393007601, 3.415357648796183199 ) ) ;
#81291=CARTESIAN_POINT ( 'NONE',  ( 11.93318256644231745, 6.455544146699622843, 8.908725066499764367 ) ) ;
#81292=DIRECTION ( 'NONE',  ( 0.000000000000000000, 0.000000000000000000, -1.000000000000000000 ) ) ;
#81351=DIRECTION ( 'NONE',  ( -1.000000000000000000, 0.000000000000000000, 0.000000000000000000 ) ) ;
#81385=ORIENTED_EDGE ( 'NONE', *, *, #94290, .F. ) ;
#81411=CARTESIAN_POINT ( 'NONE',  ( 12.36022260502946324, 17.95405137183332300, -8.703727511220279212 ) ) ;
#81419=EDGE_CURVE ( 'NONE', #47808, #12223, #102551, .T. ) ;
#81446=CARTESIAN_POINT ( 'NONE',  ( 14.99515772855951568, 1.250937070399753770, 0.4481625125234917628 ) ) ;
#81452=SURFACE_STYLE_USAGE ( .BOTH. , #8107 ) ;
#81455=CARTESIAN_POINT ( 'NONE',  ( -11.88042901237385074, 16.69099646536233550, -9.298101453719690213 ) ) ;
#81466=CARTESIAN_POINT ( 'NONE',  ( 11.66210838966212293, 15.93376395241612897, -9.569172803016048334 ) ) ;
#81480=CARTESIAN_POINT ( 'NONE',  ( -15.30823401445666043, 3.112986885588304276, -3.167215778809110649 ) ) ;
#81531=DIRECTION ( 'NONE',  ( 0.000000000000000000, 0.000000000000000000, -1.000000000000000000 ) ) ;
#81536=CARTESIAN_POINT ( 'NONE',  ( 14.95520043898952522, 4.194724623210934311, -5.164345506890662740 ) ) ;
#81546=CARTESIAN_POINT ( 'NONE',  ( -15.90404091945035070, 3.516460376326330017, -2.884095128127718066 ) ) ;
#81562=CARTESIAN_POINT ( 'NONE',  ( -14.97540207516782118, 1.269614109200695840, -0.8865648853131175011 ) ) ;
#81571=AXIS2_PLACEMENT_3D ( 'NONE', #104750, #30901, #47566 ) ;
#81623=CARTESIAN_POINT ( 'NONE',  ( 10.14798799572017529, 15.71901827466141377, -10.24181171185648331 ) ) ;
#81712=PRESENTATION_STYLE_ASSIGNMENT (( #104965 ) ) ;
#81746=PRESENTATION_STYLE_ASSIGNMENT (( #48854 ) ) ;
#81766=ORIENTED_EDGE ( 'NONE', *, *, #52220, .T. ) ;
#81877=ORIENTED_EDGE ( 'NONE', *, *, #38797, .F. ) ;
#81910=LINE ( 'NONE', #24258, #85629 ) ;
#81944=CARTESIAN_POINT ( 'NONE',  ( 10.63868951441825494, 13.01770488547337123, -10.01969491620919328 ) ) ;
#81991=CARTESIAN_POINT ( 'NONE',  ( -10.83414860630037602, 18.76830525476172440, -9.162768138102793003 ) ) ;
#82079=CARTESIAN_POINT ( 'NONE',  ( -10.17607823674123146, 16.00406820528922225, -10.18698793785925005 ) ) ;
#82094=EDGE_LOOP ( 'NONE', ( #85565, #55236, #13980, #78392, #11185, #72935, #19808, #79744 ) ) ;
#82096=CARTESIAN_POINT ( 'NONE',  ( -15.91255636217404756, 3.418437750274899489, 2.532291868554421121 ) ) ;
#82112=CARTESIAN_POINT ( 'NONE',  ( -14.37349357813612372, 2.004823033976885771, 4.269535008073903626 ) ) ;
#82137=AXIS2_PLACEMENT_3D ( 'NONE', #26259, #93614, #34340 ) ;
#82196=AXIS2_PLACEMENT_3D ( 'NONE', #29818, #77278, #69202 ) ;
#82285=CARTESIAN_POINT ( 'NONE',  ( 12.25865980111967701, 17.70980365415343627, 8.828502505339814732 ) ) ;
#82336=( NAMED_UNIT ( * ) PLANE_ANGLE_UNIT ( ) SI_UNIT ( $, .RADIAN. ) );
#82343=DIRECTION ( 'NONE',  ( 0.000000000000000000, -1.000000000000000000, 0.000000000000000000 ) ) ;
#82378=DIRECTION ( 'NONE',  ( 0.000000000000000000, -1.000000000000000000, 0.000000000000000000 ) ) ;
#82404=( NAMED_UNIT ( * ) PLANE_ANGLE_UNIT ( ) SI_UNIT ( $, .RADIAN. ) );
#82437=AXIS2_PLACEMENT_3D ( 'NONE', #85720, #11793, #87834 ) ;
#82468=COLOUR_RGB ( '', 0.72549020, 0.75294118, 0.79215686) ;
#82499=CARTESIAN_POINT ( 'NONE',  ( 13.61336331607695094, 22.69764540326648117, 2.516109114288500592 ) ) ;
#82521=EDGE_CURVE ( 'NONE', #82573, #98241, #103641, .T. ) ;
#82540=CARTESIAN_POINT ( 'NONE',  ( -15.42518680700535505, 22.80197049373886742, -2.000786945160570429 ) ) ;
#82561=FILL_AREA_STYLE ('',( #64786 ) ) ;
#82573=VERTEX_POINT ( 'NONE', #99347 ) ;
#82599=ORIENTED_EDGE ( 'NONE', *, *, #105815, .T. ) ;
#82628=CARTESIAN_POINT ( 'NONE',  ( -14.11595029531626722, 2.410436752329290222, 5.024000119293328126 ) ) ;
#82634=AXIS2_PLACEMENT_3D ( 'NONE', #100505, #1798, #9353 ) ;
#82673=CARTESIAN_POINT ( 'NONE',  ( -14.84266821126132285, 4.606643506689745315, 5.685020543979530494 ) ) ;
#82797=CIRCLE ( 'NONE', #81089, 6.999999999999999112 ) ;
#82823=CARTESIAN_POINT ( 'NONE',  ( 11.61253032626837189, 15.70682449265374458, 9.633805627537904925 ) ) ;
#82860=CARTESIAN_POINT ( 'NONE',  ( 16.00000000000006750, 2.437231117875682695, 5.694551215225515328 ) ) ;
#82945=EDGE_CURVE ( 'NONE', #37313, #51545, #28008, .T. ) ;
#82971=( LENGTH_UNIT ( ) NAMED_UNIT ( * ) SI_UNIT ( .MILLI., .METRE. ) );
#82975=CARTESIAN_POINT ( 'NONE',  ( 15.51004476304982838, 2.604548209198465525, 0.4043569039159928269 ) ) ;
#82996=EDGE_CURVE ( 'NONE', #39650, #5290, #89275, .T. ) ;
#83032=CARTESIAN_POINT ( 'NONE',  ( 13.79606237849683126, 22.99914945738909111, -0.5248391107339340778 ) ) ;
#83072=CARTESIAN_POINT ( 'NONE',  ( -13.42014485437181825, 24.46368817018429453, -2.390721932681278084 ) ) ;
#83092=( NAMED_UNIT ( * ) PLANE_ANGLE_UNIT ( ) SI_UNIT ( $, .RADIAN. ) );
#83099=CARTESIAN_POINT ( 'NONE',  ( -15.51004476305004864, 2.604548209197934838, -0.4043569039035935786 ) ) ;
#83164=EDGE_CURVE ( 'NONE', #29736, #70305, #76148, .T. ) ;
#83197=CARTESIAN_POINT ( 'NONE',  ( 14.87336202480038594, 23.06736695052138586, 1.011328272294861996 ) ) ;
#83209=FILL_AREA_STYLE_COLOUR ( '', #82468 ) ;
#83278=( LENGTH_UNIT ( ) NAMED_UNIT ( * ) SI_UNIT ( .MILLI., .METRE. ) );
#83298=FACE_OUTER_BOUND ( 'NONE', #18864, .T. ) ;
#83310=ORIENTED_EDGE ( 'NONE', *, *, #32310, .F. ) ;
#83344=SURFACE_STYLE_FILL_AREA ( #100589 ) ;
#83350=CARTESIAN_POINT ( 'NONE',  ( 0.000000000000000000, -3.035766082959412415E-15, 0.000000000000000000 ) ) ;
#83442=CARTESIAN_POINT ( 'NONE',  ( 14.90069340504961737, 2.164550790745811248, -1.672538227366102914 ) ) ;
#83454=( GEOMETRIC_REPRESENTATION_CONTEXT ( 3 ) GLOBAL_UNCERTAINTY_ASSIGNED_CONTEXT ( ( #53518 ) ) GLOBAL_UNIT_ASSIGNED_CONTEXT ( ( #26770, #35929, #101147 ) ) REPRESENTATION_CONTEXT ( 'NONE', 'WORKASPACE' ) );
#83480=CARTESIAN_POINT ( 'NONE',  ( 6.984126283073807784, 9.027603028764220383, -0.5389771161762282325 ) ) ;
#83483=CIRCLE ( 'NONE', #50746, 1.999999999999998668 ) ;
#83485=CARTESIAN_POINT ( 'NONE',  ( -15.00099999999999767, 12.99999999999999289, -4.000000000000000000 ) ) ;
#83492=CARTESIAN_POINT ( 'NONE',  ( 15.36292483821380372, 2.971926847719377651, 2.727430453976030122 ) ) ;
#83496=CARTESIAN_POINT ( 'NONE',  ( 15.05785784214676326, 3.824195276769950969, 4.604276673498415740 ) ) ;
#83548=CARTESIAN_POINT ( 'NONE',  ( 14.58597127886924483, 5.499146323186232088, 6.679532531465572909 ) ) ;
#83550=CARTESIAN_POINT ( 'NONE',  ( 11.83150069961154216, 21.33506542399163664, -7.411767003152391453 ) ) ;
#83560=ORIENTED_EDGE ( 'NONE', *, *, #63720, .T. ) ;
#83589=CARTESIAN_POINT ( 'NONE',  ( -15.54016792948419656, 22.94944790772357024, -1.155673903705213057 ) ) ;
#83606=VERTEX_POINT ( 'NONE', #95820 ) ;
#83619=CARTESIAN_POINT ( 'NONE',  ( -15.46209624076597144, 2.722175477911281671, -1.608330402066967979 ) ) ;
#83723=CARTESIAN_POINT ( 'NONE',  ( -14.95520043898599738, 4.194724623223834215, 5.164345506907288552 ) ) ;
#83725=AXIS2_PLACEMENT_3D ( 'NONE', #1981, #11665, #83972 ) ;
#83752=CIRCLE ( 'NONE', #100940, 1.999999999999999334 ) ;
#83754=CARTESIAN_POINT ( 'NONE',  ( 16.01428880459198467, 3.811183212004471521, -1.301242280779890681 ) ) ;
#83777=COLOUR_RGB ( '', 0.40784314, 0.44705882, 0.49803922) ;
#83875=CARTESIAN_POINT ( 'NONE',  ( -15.45341029905986829, 2.829415941280664981, -2.060260514156198486 ) ) ;
#83949=CIRCLE ( 'NONE', #51128, 7.500000000000000000 ) ;
#83972=DIRECTION ( 'NONE',  ( 0.000000000000000000, 0.000000000000000000, 1.000000000000000000 ) ) ;
#83984=CARTESIAN_POINT ( 'NONE',  ( 20.00000000000000000, 12.99999999999999289, 0.000000000000000000 ) ) ;
#83988=FILL_AREA_STYLE_COLOUR ( '', #71957 ) ;
#83993=CIRCLE ( 'NONE', #97757, 1.999999999999998890 ) ;
#84022=CARTESIAN_POINT ( 'NONE',  ( 5.890693798151877658, 11.69020577517987114, 3.781785903083255018 ) ) ;
#84034=CARTESIAN_POINT ( 'NONE',  ( 15.91318055706407186, 3.411564560433875570, 2.528039842346805344 ) ) ;
#84045=ORIENTED_EDGE ( 'NONE', *, *, #106185, .F. ) ;
#84088=EDGE_LOOP ( 'NONE', ( #72340, #81385, #89661, #44702 ) ) ;
#84092=CARTESIAN_POINT ( 'NONE',  ( 16.10173312979568649, 5.477053992168872121, 4.739458514412312695 ) ) ;
#84094=CARTESIAN_POINT ( 'NONE',  ( 13.08928845638972049, 23.86133543384095645, 4.069885106817294762 ) ) ;
#84117=EDGE_CURVE ( 'NONE', #20022, #27771, #2292, .T. ) ;
#84120=ORIENTED_EDGE ( 'NONE', *, *, #21994, .F. ) ;
#84141=CARTESIAN_POINT ( 'NONE',  ( -12.60307481242552896, 22.93430151644087189, -5.613563419561906187 ) ) ;
#84152=SURFACE_STYLE_FILL_AREA ( #10251 ) ;
#84194=CARTESIAN_POINT ( 'NONE',  ( 6.999814028509887542, 16.99967454973588943, 0.2742116757349301048 ) ) ;
#84223=CARTESIAN_POINT ( 'NONE',  ( -16.14595037822616419, 20.23371447306202597, -4.922994507635920947 ) ) ;
#84324=CIRCLE ( 'NONE', #82634, 7.500000000000000000 ) ;
#84353=DIRECTION ( 'NONE',  ( 1.000000000000000000, 0.000000000000000000, 0.000000000000000000 ) ) ;
#84365=CARTESIAN_POINT ( 'NONE',  ( -16.14595037822616419, 12.99999999999999467, -8.749999999999921840 ) ) ;
#84367=EDGE_CURVE ( 'NONE', #91522, #63934, #17051, .T. ) ;
#84416=EDGE_CURVE ( 'NONE', #17545, #105603, #72896, .T. ) ;
#84429=DIRECTION ( 'NONE',  ( 0.000000000000000000, 0.000000000000000000, 1.000000000000000000 ) ) ;
#84480=ORIENTED_EDGE ( 'NONE', *, *, #104587, .T. ) ;
#84483=DIRECTION ( 'NONE',  ( -1.000000000000000000, -0.000000000000000000, -0.000000000000000000 ) ) ;
#84504=DIRECTION ( 'NONE',  ( -1.000000000000000000, 0.000000000000000000, 0.000000000000000000 ) ) ;
#84523=CARTESIAN_POINT ( 'NONE',  ( -16.14595037822616419, 12.99999999999999289, 0.000000000000000000 ) ) ;
#84564=CARTESIAN_POINT ( 'NONE',  ( 6.704772934685585994, 9.540285309610183617, -2.024104295774001194 ) ) ;
#84629=CARTESIAN_POINT ( 'NONE',  ( 12.42199367956279765, 22.57433134022317844, -6.088470440402769412 ) ) ;
#84672=CARTESIAN_POINT ( 'NONE',  ( -12.85466265431899124, 23.42010317047945378, 4.868175573428279890 ) ) ;
#84741=EDGE_CURVE ( 'NONE', #92807, #27686, #18211, .T. ) ;
#84751=CARTESIAN_POINT ( 'NONE',  ( -5.744562646538029504, 13.27102973350405080, 4.000000000000000000 ) ) ;
#84807=CARTESIAN_POINT ( 'NONE',  ( 14.44768974034866993, 5.957293599828272335, 7.129930386717071578 ) ) ;
#84860=CYLINDRICAL_SURFACE ( 'NONE', #88534, 7.500000000000000000 ) ;
#84913=ORIENTED_EDGE ( 'NONE', *, *, #19619, .F. ) ;
#84954=( NAMED_UNIT ( * ) PLANE_ANGLE_UNIT ( ) SI_UNIT ( $, .RADIAN. ) );
#84985=CARTESIAN_POINT ( 'NONE',  ( 18.00000000000000355, 12.99999999999999289, 0.000000000000000000 ) ) ;
#85018=CARTESIAN_POINT ( 'NONE',  ( -13.70721846773710695, 3.095425950693140749, -6.047708547295085779 ) ) ;
#85090=CARTESIAN_POINT ( 'NONE',  ( 5.744562646538029504, 12.99999999999999112, -4.000000000000000000 ) ) ;
#85113=DIRECTION ( 'NONE',  ( 0.000000000000000000, -0.7633528697427716114, -0.6459817305895541040 ) ) ;
#85156=CARTESIAN_POINT ( 'NONE',  ( 14.42243728958148807, 21.45411286276491936, 5.348240395882925213 ) ) ;
#85199=CARTESIAN_POINT ( 'NONE',  ( -13.74817541072891736, 20.46283863168138240, 6.678757362012751386 ) ) ;
#85212=( NAMED_UNIT ( * ) SI_UNIT ( $, .STERADIAN. ) SOLID_ANGLE_UNIT ( ) );
#85313=STYLED_ITEM ( 'NONE', ( #61778 ), #35241 ) ;
#85334=CARTESIAN_POINT ( 'NONE',  ( -13.27507766870887451, 3.850002543425556034, -6.914036890321489714 ) ) ;
#85371=FILL_AREA_STYLE ('',( #19623 ) ) ;
#85407=UNCERTAINTY_MEASURE_WITH_UNIT (LENGTH_MEASURE( 1.000000000000000082E-05 ), #54293, 'distance_accuracy_value', 'NONE');
#85437=CARTESIAN_POINT ( 'NONE',  ( 16.11715839250286919, 21.56713793043144278, -2.163674775856062826 ) ) ;
#85493=PRESENTATION_STYLE_ASSIGNMENT (( #28340 ) ) ;
#85525=DIRECTION ( 'NONE',  ( 0.000000000000000000, 0.000000000000000000, -1.000000000000000000 ) ) ;
#85565=ORIENTED_EDGE ( 'NONE', *, *, #101208, .F. ) ;
#85599=EDGE_CURVE ( 'NONE', #83606, #102396, #31961, .T. ) ;
#85629=VECTOR ( 'NONE', #15060, 1000.000000000000000 ) ;
#85646=SURFACE_STYLE_USAGE ( .BOTH. , #19358 ) ;
#85661=CARTESIAN_POINT ( 'NONE',  ( 14.11571568429345724, 5.211159435664195705, -3.514002131771281068 ) ) ;
#85702=ADVANCED_FACE ( 'NONE', ( #100916 ), #76598, .F. ) ;
#85707=CARTESIAN_POINT ( 'NONE',  ( 10.61645511433041911, 13.94409384998177792, 9.960230482081710690 ) ) ;
#85716=CARTESIAN_POINT ( 'NONE',  ( -19.50000000000000000, 12.99999999999999289, 0.000000000000000000 ) ) ;
#85720=CARTESIAN_POINT ( 'NONE',  ( -16.14595037822616419, 12.99999999999999289, 0.000000000000000000 ) ) ;
#85755=CARTESIAN_POINT ( 'NONE',  ( -13.23614406034744917, 22.05544707748403255, 4.271605316804893526 ) ) ;
#85767=DIRECTION ( 'NONE',  ( 0.000000000000000000, 0.000000000000000000, -1.000000000000000000 ) ) ;
#85814=CARTESIAN_POINT ( 'NONE',  ( -15.00099999999999767, 12.99999999999999289, 0.000000000000000000 ) ) ;
#85831=DIRECTION ( 'NONE',  ( 0.000000000000000000, 0.000000000000000000, 1.000000000000000000 ) ) ;
#85841=CARTESIAN_POINT ( 'NONE',  ( 15.17271185359085983, 5.249115203880597491, -6.324282847316704981 ) ) ;
#85879=( LENGTH_UNIT ( ) NAMED_UNIT ( * ) SI_UNIT ( .MILLI., .METRE. ) );
#85960=MECHANICAL_DESIGN_GEOMETRIC_PRESENTATION_REPRESENTATION('',(#78996),#34299);
#85974=DIRECTION ( 'NONE',  ( 1.000000000000000000, -0.000000000000000000, -0.000000000000000000 ) ) ;
#85982=CARTESIAN_POINT ( 'NONE',  ( -12.82134596817017780, 18.88695635519247773, -8.090906795103039784 ) ) ;
#85990=CARTESIAN_POINT ( 'NONE',  ( 15.79792377994583852, 22.78987439203660159, 0.2434392984428970785 ) ) ;
#86046=CARTESIAN_POINT ( 'NONE',  ( 14.29190075645216851, 7.765108448534480345, -6.049455384114759582 ) ) ;
#86064=SURFACE_STYLE_FILL_AREA ( #52592 ) ;
#86117=DIRECTION ( 'NONE',  ( 1.000000000000000000, -0.000000000000000000, -0.000000000000000000 ) ) ;
#86138=( BOUNDED_SURFACE ( )  B_SPLINE_SURFACE ( 3, 3, ( 
 ( #1902, #27841, #19225, #93058 ),
 ( #2441, #11054, #51523, #52585 ),
 ( #102208, #28356, #69850, #102745 ),
 ( #10534, #28906, #43451, #60712 ) ),
 .UNSPECIFIED., .F., .F., .F. ) 
 B_SPLINE_SURFACE_WITH_KNOTS ( ( 4, 4 ),
 ( 4, 4 ),
 ( 0.02698643027831503644, 0.9670246242088337274 ),
 ( 0.000000000000000000, 1.000000000000000000 ),
 .UNSPECIFIED. ) 
 GEOMETRIC_REPRESENTATION_ITEM ( )  RATIONAL_B_SPLINE_SURFACE ( (
 ( 1.000000000000000000, 0.3333333333333334259, 0.3333333333333334259, 1.000000000000000000),
 ( 1.000000000000000000, 0.3333333333333334259, 0.3333333333333334259, 1.000000000000000000),
 ( 1.000000000000000000, 0.3333333333333334259, 0.3333333333333334259, 1.000000000000000000),
 ( 1.000000000000000000, 0.3333333333333334259, 0.3333333333333334259, 1.000000000000000000) ) ) 
 REPRESENTATION_ITEM ( '' )  SURFACE ( )  );
#86211=DIRECTION ( 'NONE',  ( 1.000000000000000000, 0.000000000000000000, 0.000000000000000000 ) ) ;
#86247=CARTESIAN_POINT ( 'NONE',  ( 13.51895206827688511, 20.10414958935020024, 7.058517651309981211 ) ) ;
#86288=CARTESIAN_POINT ( 'NONE',  ( -13.09871712087400297, 21.81423054753162560, 4.750713512999053201 ) ) ;
#86366=( GEOMETRIC_REPRESENTATION_CONTEXT ( 3 ) GLOBAL_UNCERTAINTY_ASSIGNED_CONTEXT ( ( #27350 ) ) GLOBAL_UNIT_ASSIGNED_CONTEXT ( ( #52303, #20545, #85212 ) ) REPRESENTATION_CONTEXT ( 'NONE', 'WORKASPACE' ) );
#86375=CARTESIAN_POINT ( 'NONE',  ( 12.79866983394184743, 6.544424113613374061, -7.674868532166754242 ) ) ;
#86478=LINE ( 'NONE', #54577, #63149 ) ;
#86523=( LENGTH_UNIT ( ) NAMED_UNIT ( * ) SI_UNIT ( .MILLI., .METRE. ) );
#86525=CARTESIAN_POINT ( 'NONE',  ( 15.72426027928839076, 22.05433369634782181, -3.882282778234776188 ) ) ;
#86538=CARTESIAN_POINT ( 'NONE',  ( 14.38793715987709554, 1.958934843042821505, 4.277839136693246225 ) ) ;
#86665=DIRECTION ( 'NONE',  ( 0.000000000000000000, 0.000000000000000000, 1.000000000000000000 ) ) ;
#86666=EDGE_CURVE ( 'NONE', #71001, #75752, #74510, .T. ) ;
#86668=CARTESIAN_POINT ( 'NONE',  ( -6.241401647512419437, 10.55153228299010593, -3.173604836376809679 ) ) ;
#86671=ORIENTED_EDGE ( 'NONE', *, *, #72608, .T. ) ;
#86700=ADVANCED_FACE ( 'NONE', ( #93913 ), #12677, .F. ) ;
#86776=CARTESIAN_POINT ( 'NONE',  ( 10.18950581449328396, 16.02640291263062622, 10.16991645412965362 ) ) ;
#86813=CARTESIAN_POINT ( 'NONE',  ( -11.45111553290054474, 14.76784682119976289, 9.859086153280458120 ) ) ;
#86865=CARTESIAN_POINT ( 'NONE',  ( 5.835411572216777643, 14.05761036835583333, -3.866789010015639239 ) ) ;
#86890=CARTESIAN_POINT ( 'NONE',  ( -6.560102024233680496, 16.17028887884159971, -2.452861370513718331 ) ) ;
#86894=CARTESIAN_POINT ( 'NONE',  ( 13.66298729346737773, 5.052113668166707150, -6.101274280624832791 ) ) ;
#86911=ORIENTED_EDGE ( 'NONE', *, *, #84117, .T. ) ;
#86943=FACE_OUTER_BOUND ( 'NONE', #54722, .T. ) ;
#86957=CARTESIAN_POINT ( 'NONE',  ( -14.89734172080860297, 1.349300515452548588, 1.760806480411474695 ) ) ;
#86966=UNCERTAINTY_MEASURE_WITH_UNIT (LENGTH_MEASURE( 1.000000000000000082E-05 ), #30600, 'distance_accuracy_value', 'NONE');
#86970=CARTESIAN_POINT ( 'NONE',  ( 16.14595037822613932, 20.23371447307438586, 4.922994507617745263 ) ) ;
#87038=CARTESIAN_POINT ( 'NONE',  ( -12.15584546671134802, 10.26194364132355297, -9.624033779842585901 ) ) ;
#87045=CARTESIAN_POINT ( 'NONE',  ( 14.29190075645433922, 21.26710225494878514, -5.626279437267652561 ) ) ;
#87055=CARTESIAN_POINT ( 'NONE',  ( 14.97625732068849835, 1.268789641109442812, 0.8714310519259138577 ) ) ;
#87076=VERTEX_POINT ( 'NONE', #87705 ) ;
#87089=CARTESIAN_POINT ( 'NONE',  ( -15.68557340203132533, 21.69024387811347054, 4.767881275868345980 ) ) ;
#87144=UNCERTAINTY_MEASURE_WITH_UNIT (LENGTH_MEASURE( 1.000000000000000082E-05 ), #36460, 'distance_accuracy_value', 'NONE');
#87155=CARTESIAN_POINT ( 'NONE',  ( -10.72008664263877620, 18.40195438196344568, -9.341170610878782199 ) ) ;
#87185=CARTESIAN_POINT ( 'NONE',  ( -6.561040333616081632, 9.827807988210597756, -2.450206053579249144 ) ) ;
#87227=CARTESIAN_POINT ( 'NONE',  ( 15.79261075262967573, 4.810720122702399237, -5.431533035175681867 ) ) ;
#87259=DIRECTION ( 'NONE',  ( 0.000000000000000000, 0.000000000000000000, -1.000000000000000000 ) ) ;
#87291=CARTESIAN_POINT ( 'NONE',  ( 11.42362078197221997, 14.22850026525571110, 9.928456956968465974 ) ) ;
#87337=CARTESIAN_POINT ( 'NONE',  ( -11.46727569567480387, 9.426839320540786105, 9.363982917197334999 ) ) ;
#87424=CARTESIAN_POINT ( 'NONE',  ( 13.52444138084156400, 7.616853773666340643, -8.431612038840972545 ) ) ;
#87457=CARTESIAN_POINT ( 'NONE',  ( -15.99999999999008793, 2.437231117890474863, 5.694551215252954712 ) ) ;
#87480=CARTESIAN_POINT ( 'NONE',  ( -14.27029591641004380, 3.391655494187081565, 4.551126452522245458 ) ) ;
#87558=CARTESIAN_POINT ( 'NONE',  ( -13.59109867861701382, 7.493105839183076711, -8.373922924896398001 ) ) ;
#87565=CARTESIAN_POINT ( 'NONE',  ( 16.10099483391905295, 21.87267635329353510, 0.2108314046451076063 ) ) ;
#87617=CARTESIAN_POINT ( 'NONE',  ( -14.81450998444591249, 22.88381389411949485, -2.101451306596820334 ) ) ;
#87636=CARTESIAN_POINT ( 'NONE',  ( 13.54336320516353176, 24.68363219323660473, 1.315439817157240343 ) ) ;
#87684=CARTESIAN_POINT ( 'NONE',  ( -10.37205271324882894, 10.88037002444788115, -10.43000608149194974 ) ) ;
#87705=CARTESIAN_POINT ( 'NONE',  ( 14.29190075645646907, 21.26710225494832329, -5.626279437268317807 ) ) ;
#87759=CARTESIAN_POINT ( 'NONE',  ( 16.13590653351247184, 6.313628335805621106, -5.716602451449240618 ) ) ;
#87762=CARTESIAN_POINT ( 'NONE',  ( 15.90328822607585479, 3.524689239570375499, -2.889827284395872553 ) ) ;
#87807=( NAMED_UNIT ( * ) PLANE_ANGLE_UNIT ( ) SI_UNIT ( $, .RADIAN. ) );
#87825=CARTESIAN_POINT ( 'NONE',  ( 12.11348346901124273, 7.908161531528928201, 8.621634460951579371 ) ) ;
#87833=VERTEX_POINT ( 'NONE', #86970 ) ;
#87834=DIRECTION ( 'NONE',  ( 0.000000000000000000, 0.000000000000000000, 1.000000000000000000 ) ) ;
#87864=CARTESIAN_POINT ( 'NONE',  ( -12.92250098416157478, 4.492494496599526599, 7.510829452561845976 ) ) ;
#87916=CARTESIAN_POINT ( 'NONE',  ( 6.770546484616568605, 16.58436325196198879, -1.794795801736670748 ) ) ;
#87936=ORIENTED_EDGE ( 'NONE', *, *, #84117, .F. ) ;
#87941=CARTESIAN_POINT ( 'NONE',  ( -6.969759372139044729, 16.94689987907234041, -0.6630323575263610270 ) ) ;
#87945=CARTESIAN_POINT ( 'NONE',  ( 11.01150283225517157, 16.91336324511702571, -9.209782235539176298 ) ) ;
#87985=DIRECTION ( 'NONE',  ( 0.06744659395731267271, 0.6445107564549666934, 0.7616146281272467844 ) ) ;
#87992=CARTESIAN_POINT ( 'NONE',  ( 14.38372150811336425, 21.54773996110925083, -5.213918010984154527 ) ) ;
#87994=CARTESIAN_POINT ( 'NONE',  ( -11.80829252637672511, 6.727529389947712879, -9.058755809531316316 ) ) ;
#88032=CARTESIAN_POINT ( 'NONE',  ( -14.95236164053784478, 4.204970931314857552, -5.179833178255818460 ) ) ;
#88092=( NAMED_UNIT ( * ) SI_UNIT ( $, .STERADIAN. ) SOLID_ANGLE_UNIT ( ) );
#88146=CARTESIAN_POINT ( 'NONE',  ( -14.60001457338410269, 22.21450448813268252, 3.985393712994455218 ) ) ;
#88163=CARTESIAN_POINT ( 'NONE',  ( 10.05835083440616273, 14.72912344306572408, 10.42335925054806545 ) ) ;
#88184=( GEOMETRIC_REPRESENTATION_CONTEXT ( 3 ) GLOBAL_UNCERTAINTY_ASSIGNED_CONTEXT ( ( #54915 ) ) GLOBAL_UNIT_ASSIGNED_CONTEXT ( ( #57288, #74544, #620 ) ) REPRESENTATION_CONTEXT ( 'NONE', 'WORKASPACE' ) );
#88196=ORIENTED_EDGE ( 'NONE', *, *, #38797, .T. ) ;
#88210=CARTESIAN_POINT ( 'NONE',  ( -10.02621571918099264, 14.06829240002694092, 10.51410051269792234 ) ) ;
#88291=MANIFOLD_SOLID_BREP ( 'Fillet7', #44631 ) ;
#88292=CARTESIAN_POINT ( 'NONE',  ( 15.91668924485835390, 3.370617522763084128, -2.350968163827917845 ) ) ;
#88340=FACE_BOUND ( 'NONE', #43890, .T. ) ;
#88352=DIRECTION ( 'NONE',  ( -1.000000000000000000, 0.000000000000000000, 0.000000000000000000 ) ) ;
#88356=CARTESIAN_POINT ( 'NONE',  ( 13.04323377975650189, 4.265506859525912020, 7.321301340633940669 ) ) ;
#88374=UNCERTAINTY_MEASURE_WITH_UNIT (LENGTH_MEASURE( 1.000000000000000082E-05 ), #92104, 'distance_accuracy_value', 'NONE');
#88387=CARTESIAN_POINT ( 'NONE',  ( -14.29190075645216851, 12.99999999999999289, 7.999999999999998224 ) ) ;
#88393=CARTESIAN_POINT ( 'NONE',  ( -13.04352499521497855, 4.270345267762509778, 7.309431651496303139 ) ) ;
#88456=CARTESIAN_POINT ( 'NONE',  ( 14.29190075645216673, 6.456385560668102208, 7.561819230143447257 ) ) ;
#88476=CARTESIAN_POINT ( 'NONE',  ( 12.81150014802426362, 18.86618361353973938, -8.103187572974331232 ) ) ;
#88495=CARTESIAN_POINT ( 'NONE',  ( -14.86325825540062517, 23.03589162952219382, 1.252617022373717193 ) ) ;
#88521=FACE_OUTER_BOUND ( 'NONE', #97881, .T. ) ;
#88523=CARTESIAN_POINT ( 'NONE',  ( -11.41577687521523643, 13.93101530882450589, -9.960789481687990943 ) ) ;
#88534=AXIS2_PLACEMENT_3D ( 'NONE', #100501, #93497, #9349 ) ;
#88557=( NAMED_UNIT ( * ) PLANE_ANGLE_UNIT ( ) SI_UNIT ( $, .RADIAN. ) );
#88614=CARTESIAN_POINT ( 'NONE',  ( -16.03050524006218325, 4.255071776854646437, 2.702720838600184639 ) ) ;
#88627=CARTESIAN_POINT ( 'NONE',  ( 14.63960045772751428, 2.604522098972499311, -3.217332696223609290 ) ) ;
#88668=CARTESIAN_POINT ( 'NONE',  ( -16.10335319434544843, 21.83248469006238679, -0.8773453446503929332 ) ) ;
#88687=CARTESIAN_POINT ( 'NONE',  ( 10.14990128296980210, 12.13918606557333568, 10.55440379982475108 ) ) ;
#88761=CARTESIAN_POINT ( 'NONE',  ( -6.085184064390054992, 10.98280286254172999, 3.463681541593110591 ) ) ;
#88778=( NAMED_UNIT ( * ) PLANE_ANGLE_UNIT ( ) SI_UNIT ( $, .RADIAN. ) );
#88813=CARTESIAN_POINT ( 'NONE',  ( 0.000000000000000000, 24.73290587908618932, 14.06164498842270483 ) ) ;
#88841=PRESENTATION_STYLE_ASSIGNMENT (( #72122 ) ) ;
#88845=MECHANICAL_DESIGN_GEOMETRIC_PRESENTATION_REPRESENTATION('',(#56087),#45810);
#88863=CARTESIAN_POINT ( 'NONE',  ( -28.12328997684540610, 24.73290587908618932, 14.06164498842270838 ) ) ;
#88917=CARTESIAN_POINT ( 'NONE',  ( -15.55885900989643389, 4.747722280824520524, 5.673041147144331831 ) ) ;
#88930=EDGE_LOOP ( 'NONE', ( #84120, #15489, #41898, #47203 ) ) ;
#88977=( GEOMETRIC_REPRESENTATION_CONTEXT ( 3 ) GLOBAL_UNCERTAINTY_ASSIGNED_CONTEXT ( ( #99014 ) ) GLOBAL_UNIT_ASSIGNED_CONTEXT ( ( #48405, #73205, #58650 ) ) REPRESENTATION_CONTEXT ( 'NONE', 'WORKASPACE' ) );
#89002=CARTESIAN_POINT ( 'NONE',  ( 11.41130097529988774, 18.22783037506831505, -8.549200310636470235 ) ) ;
#89032=ORIENTED_EDGE ( 'NONE', *, *, #3101, .T. ) ;
#89036=DIRECTION ( 'NONE',  ( 0.000000000000000000, -0.7633528697427404142, -0.6459817305895909634 ) ) ;
#89045=CARTESIAN_POINT ( 'NONE',  ( -10.35691556261526713, 16.96077279230471646, -9.900750464959962471 ) ) ;
#89067=DIRECTION ( 'NONE',  ( 0.000000000000000000, 0.000000000000000000, 1.000000000000000000 ) ) ;
#89087=CARTESIAN_POINT ( 'NONE',  ( -14.58597127886967648, 5.499146323183259355, -6.679532531462420764 ) ) ;
#89102=FACE_OUTER_BOUND ( 'NONE', #104475, .T. ) ;
#89114=CARTESIAN_POINT ( 'NONE',  ( -14.29190075645675861, 21.26710225494873185, 5.626279437267716510 ) ) ;
#89131=CARTESIAN_POINT ( 'NONE',  ( 16.14595037822613932, 12.99999999999999289, 0.000000000000000000 ) ) ;
#89132=CARTESIAN_POINT ( 'NONE',  ( -20.00000000000000000, 12.99999999999999289, 0.000000000000000000 ) ) ;
#89147=CARTESIAN_POINT ( 'NONE',  ( -15.88092429543819151, 3.778118985513345240, 3.597070451772169442 ) ) ;
#89202=CARTESIAN_POINT ( 'NONE',  ( -15.76925030631008262, 22.49347711647530090, 2.473099622738333281 ) ) ;
#89224=CARTESIAN_POINT ( 'NONE',  ( 12.88120258102912885, 4.569062003714924991, -7.577876238213450577 ) ) ;
#89238=CARTESIAN_POINT ( 'NONE',  ( -12.81329827117308007, 8.851410091539614555, 9.103439556559704826 ) ) ;
#89275=B_SPLINE_CURVE_WITH_KNOTS ( 'NONE', 3,
 ( #7561, #15138, #48020, #63717, #80930, #7041, #32416, #81446, #23799, #39957, #72831, #32947, #65285, #56648, #24331, #97635 ),
 .UNSPECIFIED., .F., .F.,
 ( 4, 2, 2, 2, 2, 2, 2, 4 ),
 ( 4.443906512722159927E-18, 0.001337001954496015634, 0.002674003908992026064, 0.005348007817984046057, 0.006685009772480056921, 0.008022011726976066917, 0.009359013681472077781, 0.01069601563596808691 ),
 .UNSPECIFIED. ) ;
#89301=CARTESIAN_POINT ( 'NONE',  ( -5.888319653649580765, 11.68640158625127512, 3.787045357069727558 ) ) ;
#89321=AXIS2_PLACEMENT_3D ( 'NONE', #31400, #76057, #28092 ) ;
#89334=CARTESIAN_POINT ( 'NONE',  ( 12.91142918290874597, 8.665321034538903788, 9.018047713757219697 ) ) ;
#89419=CARTESIAN_POINT ( 'NONE',  ( 10.12940370570886373, 12.28737531179036857, 10.56278064024531282 ) ) ;
#89424=FACE_OUTER_BOUND ( 'NONE', #88930, .T. ) ;
#89454=CARTESIAN_POINT ( 'NONE',  ( -13.95941059228342951, 6.934767921800601975, 7.968035485162160647 ) ) ;
#89537=CARTESIAN_POINT ( 'NONE',  ( 10.52016239807662856, 10.30073425343680782, -10.32006978720601786 ) ) ;
#89551=CARTESIAN_POINT ( 'NONE',  ( -14.47578207976464526, 21.82911064463434059, 4.800479567661631641 ) ) ;
#89581=CARTESIAN_POINT ( 'NONE',  ( -10.13027397392433926, 12.28049385479850741, -10.56248067576192362 ) ) ;
#89592=EDGE_CURVE ( 'NONE', #63934, #70305, #25587, .T. ) ;
#89594=CARTESIAN_POINT ( 'NONE',  ( 11.42048730496502706, 13.43064252417310556, -10.00000000000007994 ) ) ;
#89619=CARTESIAN_POINT ( 'NONE',  ( -15.64030048137867190, 6.456385560667921020, -7.561819230143237647 ) ) ;
#89643=CARTESIAN_POINT ( 'NONE',  ( -11.44242801400452159, 13.21397695474668943, 10.00000000000005507 ) ) ;
#89661=ORIENTED_EDGE ( 'NONE', *, *, #14782, .F. ) ;
#89676=CARTESIAN_POINT ( 'NONE',  ( -16.14595037822616419, 12.99999999999999289, 0.000000000000000000 ) ) ;
#89681=CARTESIAN_POINT ( 'NONE',  ( -16.01290064681822045, 3.743845801208044222, -0.6463026410129599775 ) ) ;
#89687=FILL_AREA_STYLE_COLOUR ( '', #29548 ) ;
#89697=CARTESIAN_POINT ( 'NONE',  ( -14.24890542152424544, 2.189729425908971017, 4.659254830001311021 ) ) ;
#89756=CARTESIAN_POINT ( 'NONE',  ( 11.90409330339966409, 21.49301302430015070, -7.268787543711042076 ) ) ;
#89864=AXIS2_PLACEMENT_3D ( 'NONE', #1161, #74013, #33064 ) ;
#89869=SURFACE_SIDE_STYLE ('',( #24104 ) ) ;
#89904=DIRECTION ( 'NONE',  ( -0.000000000000000000, -1.000000000000000000, -0.000000000000000000 ) ) ;
#89918=SURFACE_STYLE_USAGE ( .BOTH. , #22569 ) ;
#89935=CARTESIAN_POINT ( 'NONE',  ( 13.53516154045776076, 7.599662942191373283, 8.420555603062727101 ) ) ;
#89937=DIRECTION ( 'NONE',  ( 0.000000000000000000, 0.000000000000000000, -1.000000000000000000 ) ) ;
#89938=DIRECTION ( 'NONE',  ( -1.000000000000000000, -0.000000000000000000, -0.000000000000000000 ) ) ;
#89966=CARTESIAN_POINT ( 'NONE',  ( -14.29190075645216851, 12.99999999999999289, 0.000000000000000000 ) ) ;
#90056=CARTESIAN_POINT ( 'NONE',  ( 11.52703303463460749, 20.62217656626097551, -7.985623555383951633 ) ) ;
#90101=CARTESIAN_POINT ( 'NONE',  ( -10.65573454473422998, 18.19277052736382672, -9.438289383338396732 ) ) ;
#90123=SURFACE_SIDE_STYLE ('',( #32446 ) ) ;
#90169=CARTESIAN_POINT ( 'NONE',  ( -11.66952397775300909, 15.93506242127414652, 9.561843478809398889 ) ) ;
#90188=CARTESIAN_POINT ( 'NONE',  ( -10.53539113526819015, 10.21274928881584998, 10.31347537521849311 ) ) ;
#90205=CARTESIAN_POINT ( 'NONE',  ( -15.51015326907006830, 2.604283801340433691, -0.3849796309549803897 ) ) ;
#90206=CARTESIAN_POINT ( 'NONE',  ( 16.14595037814516587, 20.48432867205317365, 4.554748808022611506 ) ) ;
#90277=CARTESIAN_POINT ( 'NONE',  ( 11.77417553695194208, 6.803368766693943748, -9.098819535938051928 ) ) ;
#90440=CARTESIAN_POINT ( 'NONE',  ( 16.10103474921838540, 21.87197452378524787, -0.4486278773448218460 ) ) ;
#90528=PRESENTATION_STYLE_ASSIGNMENT (( #9065 ) ) ;
#90591=CARTESIAN_POINT ( 'NONE',  ( 13.68200042800751426, 22.81115111118363004, 2.014803622706606845 ) ) ;
#90636=CARTESIAN_POINT ( 'NONE',  ( -14.97914546934171653, 22.21797506316305615, 3.886805437593018553 ) ) ;
#90664=CARTESIAN_POINT ( 'NONE',  ( -15.35634750254357428, 2.988828671322287800, 2.785065577037467488 ) ) ;
#90878=ADVANCED_FACE ( 'NONE', ( #73630 ), #61994, .T. ) ;
#90929=CARTESIAN_POINT ( 'NONE',  ( 14.29190075645216496, 21.26710225494213802, 5.626279437277409201 ) ) ;
#90966=DIRECTION ( 'NONE',  ( -0.3048027540940034252, 0.4519649026942579861, 0.8383453988835869453 ) ) ;
#91025=FILL_AREA_STYLE_COLOUR ( '', #45867 ) ;
#91069=CARTESIAN_POINT ( 'NONE',  ( 6.880814520906024079, 9.211466042846859992, 1.310034959478669547 ) ) ;
#91070=DIRECTION ( 'NONE',  ( -0.000000000000000000, -1.000000000000000000, -0.000000000000000000 ) ) ;
#91111=MECHANICAL_DESIGN_GEOMETRIC_PRESENTATION_REPRESENTATION('',(#101414),#30844);
#91142=CARTESIAN_POINT ( 'NONE',  ( 12.32648393225135486, 22.38102541151338087, -6.322412828060416601 ) ) ;
#91188=CARTESIAN_POINT ( 'NONE',  ( -15.54108745661637769, 22.95061784590342668, 1.145812418174521952 ) ) ;
#91327=ORIENTED_EDGE ( 'NONE', *, *, #102621, .F. ) ;
#91344=CIRCLE ( 'NONE', #60411, 10.00000000000000178 ) ;
#91368=DIRECTION ( 'NONE',  ( 0.000000000000000000, 0.000000000000000000, -1.000000000000000000 ) ) ;
#91410=( LENGTH_UNIT ( ) NAMED_UNIT ( * ) SI_UNIT ( .MILLI., .METRE. ) );
#91450=EDGE_CURVE ( 'NONE', #63378, #18205, #58566, .T. ) ;
#91522=VERTEX_POINT ( 'NONE', #98838 ) ;
#91542=EDGE_CURVE ( 'NONE', #15534, #74862, #10361, .T. ) ;
#91558=CARTESIAN_POINT ( 'NONE',  ( 14.97535898699462997, 1.269652431126665260, -0.8876819510628390919 ) ) ;
#91604=ORIENTED_EDGE ( 'NONE', *, *, #6916, .T. ) ;
#91662=EDGE_LOOP ( 'NONE', ( #106276, #37521, #61154, #40793 ) ) ;
#91663=CARTESIAN_POINT ( 'NONE',  ( 16.05785784214672773, 4.775831776474229073, 3.710403933782411734 ) ) ;
#91665=CARTESIAN_POINT ( 'NONE',  ( 15.53945107738913300, 22.94853113541235601, -1.161811152313551920 ) ) ;
#91706=CARTESIAN_POINT ( 'NONE',  ( -12.34875849493573519, 20.40955147515336421, -6.752960215329498972 ) ) ;
#91720=ORIENTED_EDGE ( 'NONE', *, *, #67464, .T. ) ;
#91721=CARTESIAN_POINT ( 'NONE',  ( 13.46465456495261215, 20.01166497731195903, -7.140621403355150498 ) ) ;
#91752=DIRECTION ( 'NONE',  ( 0.000000000000000000, 0.000000000000000000, 1.000000000000000000 ) ) ;
#91757=CARTESIAN_POINT ( 'NONE',  ( 5.887945094627411002, 14.31209784358735249, 3.787642776067695394 ) ) ;
#91778=DIRECTION ( 'NONE',  ( 0.000000000000000000, -0.5626279437298172814, -0.8267102254928009319 ) ) ;
#91812=FACE_OUTER_BOUND ( 'NONE', #56162, .T. ) ;
#91893=UNCERTAINTY_MEASURE_WITH_UNIT (LENGTH_MEASURE( 1.000000000000000082E-05 ), #93905, 'distance_accuracy_value', 'NONE');
#91954=DIRECTION ( 'NONE',  ( -0.000000000000000000, 1.000000000000000000, -0.000000000000000000 ) ) ;
#91971=FILL_AREA_STYLE_COLOUR ( '', #36332 ) ;
#92003=CIRCLE ( 'NONE', #14526, 10.00000000000000178 ) ;
#92068=CARTESIAN_POINT ( 'NONE',  ( 15.50569080111995568, 2.636008032211578200, 0.8338155181783696301 ) ) ;
#92097=DIRECTION ( 'NONE',  ( 0.000000000000000000, 1.000000000000000000, 0.000000000000000000 ) ) ;
#92103=CARTESIAN_POINT ( 'NONE',  ( 6.012758288945200924, 11.20935548165501316, 3.586184577130256734 ) ) ;
#92104=( LENGTH_UNIT ( ) NAMED_UNIT ( * ) SI_UNIT ( .MILLI., .METRE. ) );
#92114=DIRECTION ( 'NONE',  ( 0.000000000000000000, 0.000000000000000000, -1.000000000000000000 ) ) ;
#92171=CARTESIAN_POINT ( 'NONE',  ( 12.03416627641659353, 21.77447360072266846, -6.997134457414010633 ) ) ;
#92197=VERTEX_POINT ( 'NONE', #2679 ) ;
#92207=CARTESIAN_POINT ( 'NONE',  ( -13.14907386255262445, 23.97079872446213855, 3.796718886851553343 ) ) ;
#92238=CARTESIAN_POINT ( 'NONE',  ( -15.05785784214673129, 3.824195276770050445, -4.604276673498571171 ) ) ;
#92261=CARTESIAN_POINT ( 'NONE',  ( 6.770001855160700188, 16.58332918785157872, 1.796682604554741935 ) ) ;
#92268=CYLINDRICAL_SURFACE ( 'NONE', #77008, 10.00000000000000178 ) ;
#92269=CARTESIAN_POINT ( 'NONE',  ( -16.14595037822616419, 20.23371447306202597, -4.922994507635920947 ) ) ;
#92293=CARTESIAN_POINT ( 'NONE',  ( -16.11155731265022339, 21.67754735132975696, -1.749455090966761439 ) ) ;
#92402=AXIS2_PLACEMENT_3D ( 'NONE', #58034, #825, #49945 ) ;
#92456=CIRCLE ( 'NONE', #104462, 2.000000000000000000 ) ;
#92495=CARTESIAN_POINT ( 'NONE',  ( -14.38793715987803878, 1.958934843038082851, -4.277839136690804622 ) ) ;
#92499=CARTESIAN_POINT ( 'NONE',  ( -14.66255430293768569, 22.40929092343608175, -3.546301636274618030 ) ) ;
#92533=AXIS2_PLACEMENT_3D ( 'NONE', #15211, #74505, #58331 ) ;
#92580=ORIENTED_EDGE ( 'NONE', *, *, #69607, .T. ) ;
#92601=CARTESIAN_POINT ( 'NONE',  ( 14.27029591641831274, 3.391655494167682861, 4.551126452496778718 ) ) ;
#92640=CARTESIAN_POINT ( 'NONE',  ( 6.481088301903606741, 9.994875444612373983, -2.652222390170977384 ) ) ;
#92675=AXIS2_PLACEMENT_3D ( 'NONE', #60335, #93208, #19373 ) ;
#92710=CARTESIAN_POINT ( 'NONE',  ( 15.20001342229217123, 22.50991373429433295, -3.104903353136252431 ) ) ;
#92719=( BOUNDED_SURFACE ( )  B_SPLINE_SURFACE ( 3, 2, ( 
 ( #70431, #60236, #61278 ),
 ( #76915, #103327, #3025 ),
 ( #29473, #95240, #36506 ),
 ( #21372, #54210, #46155 ),
 ( #5163, #93104, #19276 ),
 ( #27891, #60758, #93646 ) ),
 .UNSPECIFIED., .F., .F., .F. ) 
 B_SPLINE_SURFACE_WITH_KNOTS ( ( 4, 2, 4 ),
 ( 3, 3 ),
 ( -2.180330568868349417E-15, 0.001801542390186249357, 0.003603084780374679261 ),
 ( 0.000000000000000000, 1.000000000000000000 ),
 .UNSPECIFIED. ) 
 GEOMETRIC_REPRESENTATION_ITEM ( )  RATIONAL_B_SPLINE_SURFACE ( (
 ( 1.000000000000000000, 0.8291561975892046688, 1.000000000000000000),
 ( 1.000000000000000000, 0.8506934603553527596, 1.000000000000000000),
 ( 1.000000000000000000, 0.8671388017650453195, 1.000000000000000000),
 ( 1.000000000000000000, 0.8933560653587880873, 1.000000000000000000),
 ( 1.000000000000000000, 0.9032011672209129260, 1.000000000000000000),
 ( 1.000000000000000000, 0.9115707425103370953, 1.000000000000000000) ) ) 
 REPRESENTATION_ITEM ( '' )  SURFACE ( )  );
#92753=CARTESIAN_POINT ( 'NONE',  ( 20.00000000000000000, 12.99999999999999289, 0.000000000000000000 ) ) ;
#92756=CARTESIAN_POINT ( 'NONE',  ( -13.46110359768981368, 24.53700931164864230, -2.095215872004557944 ) ) ;
#92807=VERTEX_POINT ( 'NONE', #13073 ) ;
#92809=ORIENTED_EDGE ( 'NONE', *, *, #25381, .T. ) ;
#92881=CARTESIAN_POINT ( 'NONE',  ( 14.86288555396978062, 23.03472989906422086, 1.260572299733986101 ) ) ;
#92889=CARTESIAN_POINT ( 'NONE',  ( 14.84266821126072777, 4.606643506668125276, 5.685020543978089869 ) ) ;
#92893=( LENGTH_UNIT ( ) NAMED_UNIT ( * ) SI_UNIT ( .MILLI., .METRE. ) );
#92928=EDGE_CURVE ( 'NONE', #29837, #97818, #39076, .T. ) ;
#92957=UNCERTAINTY_MEASURE_WITH_UNIT (LENGTH_MEASURE( 1.000000000000000082E-05 ), #44299, 'distance_accuracy_value', 'NONE');
#92967=PRESENTATION_STYLE_ASSIGNMENT (( #8851 ) ) ;
#93039=( NAMED_UNIT ( * ) SI_UNIT ( $, .STERADIAN. ) SOLID_ANGLE_UNIT ( ) );
#93058=CARTESIAN_POINT ( 'NONE',  ( 2.979761111870779223E-15, 34.19642918197134662, 12.16579798332631412 ) ) ;
#93080=VERTEX_POINT ( 'NONE', #88456 ) ;
#93088=ORIENTED_EDGE ( 'NONE', *, *, #102621, .T. ) ;
#93104=CARTESIAN_POINT ( 'NONE',  ( -15.82318872385067543, 4.444012391166255682, 4.874853782845832484 ) ) ;
#93142=CARTESIAN_POINT ( 'NONE',  ( 15.47565679866152699, 2.746345986933767858, 1.655435732256164139 ) ) ;
#93161=CARTESIAN_POINT ( 'NONE',  ( 20.00000000000000000, 12.99999999999999467, 6.999999999999999112 ) ) ;
#93165=TOROIDAL_SURFACE ( 'NONE', #50112, 8.000000000000000000, 1.000000000000000000 ) ;
#93180=CARTESIAN_POINT ( 'NONE',  ( 5.744562646538029504, 12.72897026649593855, -4.000000000000000888 ) ) ;
#93181=SURFACE_SIDE_STYLE ('',( #60307 ) ) ;
#93188=FACE_OUTER_BOUND ( 'NONE', #12292, .T. ) ;
#93208=DIRECTION ( 'NONE',  ( 1.000000000000000000, -0.000000000000000000, 1.224646799147353207E-16 ) ) ;
#93239=ORIENTED_EDGE ( 'NONE', *, *, #55341, .F. ) ;
#93240=VERTEX_POINT ( 'NONE', #105160 ) ;
#93250=CARTESIAN_POINT ( 'NONE',  ( 12.78945977464362116, 21.25429375852011660, 5.669412170850756105 ) ) ;
#93298=CARTESIAN_POINT ( 'NONE',  ( -13.02509636762063039, 21.68341507793183354, 4.986677504272470252 ) ) ;
#93332=AXIS2_PLACEMENT_3D ( 'NONE', #27663, #51875, #26596 ) ;
#93356=CARTESIAN_POINT ( 'NONE',  ( 5.744562646538031281, 13.26979259399947964, 4.000000000000000888 ) ) ;
#93378=SURFACE_STYLE_USAGE ( .BOTH. , #59965 ) ;
#93388=CARTESIAN_POINT ( 'NONE',  ( -16.10339698264861497, 21.83175592237823892, -0.8850307878645093940 ) ) ;
#93390=CARTESIAN_POINT ( 'NONE',  ( 12.10323273576600478, 7.930126419769916168, -8.634503244510865372 ) ) ;
#93435=SURFACE_SIDE_STYLE ('',( #12486 ) ) ;
#93438=APPLICATION_CONTEXT ( 'automotive_design' ) ;
#93493=CARTESIAN_POINT ( 'NONE',  ( -16.14595037822608603, 6.785770140112291848, -6.193810554583039973 ) ) ;
#93497=DIRECTION ( 'NONE',  ( 1.000000000000000000, -0.000000000000000000, -0.000000000000000000 ) ) ;
#93522=EDGE_LOOP ( 'NONE', ( #76663, #48744, #43586, #100007 ) ) ;
#93536=CARTESIAN_POINT ( 'NONE',  ( 16.10103572754711720, 21.87195731844753865, -0.4457938393851405556 ) ) ;
#93542=ORIENTED_EDGE ( 'NONE', *, *, #105815, .F. ) ;
#93549=VERTEX_POINT ( 'NONE', #104916 ) ;
#93576=ORIENTED_EDGE ( 'NONE', *, *, #39019, .F. ) ;
#93594=DIRECTION ( 'NONE',  ( 0.000000000000000000, 0.000000000000000000, -1.000000000000000000 ) ) ;
#93607=FACE_OUTER_BOUND ( 'NONE', #100751, .T. ) ;
#93614=DIRECTION ( 'NONE',  ( 0.3048027540940115299, 0.4519649026942716974, -0.8383453988835765092 ) ) ;
#93642=CIRCLE ( 'NONE', #47028, 7.000000000000000000 ) ;
#93646=CARTESIAN_POINT ( 'NONE',  ( -15.05785784214257284, 3.824195276785038011, 4.604276673521291663 ) ) ;
#93657=ORIENTED_EDGE ( 'NONE', *, *, #24251, .F. ) ;
#93668=ORIENTED_EDGE ( 'NONE', *, *, #96759, .T. ) ;
#93784=CARTESIAN_POINT ( 'NONE',  ( 10.24201228536178299, 16.35548964043822195, 10.08355089876082822 ) ) ;
#93829=CARTESIAN_POINT ( 'NONE',  ( -10.64220735762159009, 12.97372309155720416, 10.01974392434693684 ) ) ;
#93885=( NAMED_UNIT ( * ) SI_UNIT ( $, .STERADIAN. ) SOLID_ANGLE_UNIT ( ) );
#93905=( LENGTH_UNIT ( ) NAMED_UNIT ( * ) SI_UNIT ( .MILLI., .METRE. ) );
#93911=CARTESIAN_POINT ( 'NONE',  ( -16.14595037822600432, 20.73084165116604183, 4.192529328840223890 ) ) ;
#93913=FACE_OUTER_BOUND ( 'NONE', #31794, .T. ) ;
#93964=CARTESIAN_POINT ( 'NONE',  ( -12.54804038502308394, 5.196493816364167628, -8.098704251221438000 ) ) ;
#93981=( LENGTH_UNIT ( ) NAMED_UNIT ( * ) SI_UNIT ( .MILLI., .METRE. ) );
#94048=CARTESIAN_POINT ( 'NONE',  ( -11.53880497916332004, 12.39660325957438225, -9.988508027600554229 ) ) ;
#94055=CARTESIAN_POINT ( 'NONE',  ( 15.79412934197706875, 22.74951556322536561, -1.014593669854217950 ) ) ;
#94114=TOROIDAL_SURFACE ( 'NONE', #33862, 8.000000000000000000, 1.000000000000000000 ) ;
#94178=CARTESIAN_POINT ( 'NONE',  ( -13.00575196869246852, 4.333941897774360896, -7.384322708455154149 ) ) ;
#94179=CIRCLE ( 'NONE', #13236, 7.500000000000000000 ) ;
#94212=CARTESIAN_POINT ( 'NONE',  ( -20.00000000000000000, 12.99999999999999467, -6.999999999999999112 ) ) ;
#94222=CIRCLE ( 'NONE', #39176, 7.500000000000000000 ) ;
#94283=CARTESIAN_POINT ( 'NONE',  ( 16.14595037822613932, 12.99999999999999289, 0.000000000000000000 ) ) ;
#94290=EDGE_CURVE ( 'NONE', #49400, #57533, #37568, .T. ) ;
#94326=CARTESIAN_POINT ( 'NONE',  ( 12.80938200527896420, 18.86218302254438939, 8.106113376688432126 ) ) ;
#94356=ORIENTED_EDGE ( 'NONE', *, *, #48252, .F. ) ;
#94368=CARTESIAN_POINT ( 'NONE',  ( -12.86856004683486709, 21.39988744414081268, 5.451043748370874020 ) ) ;
#94427=CARTESIAN_POINT ( 'NONE',  ( 6.925180474901644345, 16.86781820218113026, -1.053794444618463721 ) ) ;
#94458=CARTESIAN_POINT ( 'NONE',  ( 13.76261248551633010, 4.889473877509565192, -5.883208202484460081 ) ) ;
#94503=CARTESIAN_POINT ( 'NONE',  ( 14.82219693887339496, 22.90781324648665063, -1.994990707544676445 ) ) ;
#94519=CARTESIAN_POINT ( 'NONE',  ( -20.00000000000000000, 12.99999999999999289, -4.000000000000000000 ) ) ;
#94566=PRESENTATION_STYLE_ASSIGNMENT (( #46518 ) ) ;
#94602=CARTESIAN_POINT ( 'NONE',  ( -11.48299332337337120, 12.76511049892793181, -10.00418054026044778 ) ) ;
#94608=PRESENTATION_STYLE_ASSIGNMENT (( #102677 ) ) ;
#94662=SURFACE_SIDE_STYLE ('',( #102193 ) ) ;
#94682=CARTESIAN_POINT ( 'NONE',  ( 13.28477689701638731, 24.21911917246261226, 3.176269128160213118 ) ) ;
#94684=SURFACE_SIDE_STYLE ('',( #86064 ) ) ;
#94693=AXIS2_PLACEMENT_3D ( 'NONE', #10654, #45188, #43572 ) ;
#94727=CARTESIAN_POINT ( 'NONE',  ( -11.09178706276765247, 8.457831532506155270, -9.831605721811831344 ) ) ;
#94804=CARTESIAN_POINT ( 'NONE',  ( 15.13304769501646341, 3.593526407993296257, -4.245863293343404621 ) ) ;
#94859=CARTESIAN_POINT ( 'NONE',  ( -16.02749411895511855, 4.188372957640357441, 2.551519145336385463 ) ) ;
#94864=CARTESIAN_POINT ( 'NONE',  ( 10.77037052812252327, 15.77472040317956470, 9.613292503973772440 ) ) ;
#94906=CARTESIAN_POINT ( 'NONE',  ( -14.20297455945173226, 21.13968428940458111, 5.815581957642580235 ) ) ;
#94932=ORIENTED_EDGE ( 'NONE', *, *, #40476, .F. ) ;
#94940=ORIENTED_EDGE ( 'NONE', *, *, #3808, .T. ) ;
#94967=CARTESIAN_POINT ( 'NONE',  ( 8.572527594031473190E-16, 34.00000000000000000, -7.000000000000000000 ) ) ;
#94985=CIRCLE ( 'NONE', #48435, 2.000000000000000000 ) ;
#94986=CARTESIAN_POINT ( 'NONE',  ( -6.084941413214105310, 15.01651929834134336, -3.464128533964753842 ) ) ;
#94991=SURFACE_SIDE_STYLE ('',( #21640 ) ) ;
#95018=VERTEX_POINT ( 'NONE', #43120 ) ;
#95033=CARTESIAN_POINT ( 'NONE',  ( 14.67692467444030235, 22.45409176455828870, -3.436280814760010571 ) ) ;
#95036=PRESENTATION_STYLE_ASSIGNMENT (( #69684 ) ) ;
#95049=CARTESIAN_POINT ( 'NONE',  ( -14.84861631010436689, 2.245468665778625361, 2.074511027887800729 ) ) ;
#95127=DIRECTION ( 'NONE',  ( 0.000000000000000000, 0.000000000000000000, -1.000000000000000000 ) ) ;
#95133=CARTESIAN_POINT ( 'NONE',  ( 16.14327244186471688, 20.71081664948948742, 4.173128809998666533 ) ) ;
#95138=( NAMED_UNIT ( * ) PLANE_ANGLE_UNIT ( ) SI_UNIT ( $, .RADIAN. ) );
#95144=( LENGTH_UNIT ( ) NAMED_UNIT ( * ) SI_UNIT ( .MILLI., .METRE. ) );
#95180=CARTESIAN_POINT ( 'NONE',  ( -14.29190075645414737, 21.26710225494818474, 5.626279437268514094 ) ) ;
#95201=CARTESIAN_POINT ( 'NONE',  ( 11.08215839935742331, 19.47830716714238974, 8.757826482158389325 ) ) ;
#95240=CARTESIAN_POINT ( 'NONE',  ( -15.72218280906577625, 5.595371698627605639, 6.516822309428270010 ) ) ;
#95244=CARTESIAN_POINT ( 'NONE',  ( -11.89787374881586501, 21.47933664795157327, -7.281391404119607280 ) ) ;
#95254=DIRECTION ( 'NONE',  ( 0.000000000000000000, 0.000000000000000000, -1.000000000000000000 ) ) ;
#95272=ADVANCED_FACE ( 'NONE', ( #54114 ), #23296, .F. ) ;
#95277=CARTESIAN_POINT ( 'NONE',  ( -6.322210203194782885, 10.35489075027773254, -3.011395388464981338 ) ) ;
#95279=B_SPLINE_CURVE_WITH_KNOTS ( 'NONE', 3,
 ( #90929, #17040, #7324, #49376, #48841, #24616, #57464, #105506, #7857, #56400, #82285, #73655, #47783, #98985, #82823, #80685, #23555, #49915, #33767, #8922, #24091, #8396, #65579, #40236, #97395, #56934, #41828, #89334, #15426, #41298, #6805, #72601 ),
 .UNSPECIFIED., .F., .F.,
 ( 4, 2, 2, 2, 2, 2, 2, 2, 2, 2, 2, 2, 2, 2, 2, 4 ),
 ( 0.02274979562923905643, 0.02388451199206677311, 0.02501922835489448979, 0.02615394471772220647, 0.02728866108054992315, 0.02842337744337763983, 0.02955809380620535998, 0.03069281016903307666, 0.03182752653186079334, 0.03296224289468851348, 0.03409695925751622669, 0.03523167562034394684, 0.03636639198317166699, 0.03750110834599938714, 0.03863582470882710729, 0.04090525743448254065 ),
 .UNSPECIFIED. ) ;
#95316=SURFACE_STYLE_FILL_AREA ( #11180 ) ;
#95318=CARTESIAN_POINT ( 'NONE',  ( 16.02369196221434677, 4.084267053693343641, -2.245701149433702692 ) ) ;
#95324=SURFACE_SIDE_STYLE ('',( #95857 ) ) ;
#95377=CARTESIAN_POINT ( 'NONE',  ( 11.22265610080591003, 19.85824387651571499, 8.522341943024397182 ) ) ;
#95396=DIRECTION ( 'NONE',  ( 0.000000000000000000, 0.7633528697415662423, -0.6459817305909786311 ) ) ;
#95415=CARTESIAN_POINT ( 'NONE',  ( -10.02817096105811778, 14.31193741560988641, 10.49095716857858029 ) ) ;
#95467=CARTESIAN_POINT ( 'NONE',  ( 5.888319653649583429, 14.31359841374870712, -3.787045357069728446 ) ) ;
#95492=CARTESIAN_POINT ( 'NONE',  ( -6.770548583014333488, 16.58437012435219415, -1.794845940801068629 ) ) ;
#95497=CARTESIAN_POINT ( 'NONE',  ( 12.91023948886108030, 4.515193599548165793, -7.530818612190385508 ) ) ;
#95547=CARTESIAN_POINT ( 'NONE',  ( -13.92884988672090607, 2.721025988440579191, -5.537286027112259035 ) ) ;
#95648=CARTESIAN_POINT ( 'NONE',  ( -12.25900440697833993, 17.71059303037062449, -8.828067291959920126 ) ) ;
#95700=CARTESIAN_POINT ( 'NONE',  ( -15.79785611713298366, 22.78916061418441075, -0.5147589528978404605 ) ) ;
#95704=CIRCLE ( 'NONE', #12991, 1.000000000000000000 ) ;
#95719=CARTESIAN_POINT ( 'NONE',  ( -16.14595037822616419, 12.99999999999999289, 8.749999999999921840 ) ) ;
#95722=CARTESIAN_POINT ( 'NONE',  ( 11.37917810246435657, 20.25992464176842489, 8.251280100175593546 ) ) ;
#95769=CARTESIAN_POINT ( 'NONE',  ( -13.51397627351688513, 24.63143318842911356, 1.638057307426889597 ) ) ;
#95779=CARTESIAN_POINT ( 'NONE',  ( -20.00000000000000000, 12.99999999999999289, 0.000000000000000000 ) ) ;
#95803=CARTESIAN_POINT ( 'NONE',  ( -5.744562646538031281, 12.73020740600051148, -4.000000000000000888 ) ) ;
#95820=CARTESIAN_POINT ( 'NONE',  ( 8.572527594031473190E-16, 0.9999999999999970024, -7.000000000000000000 ) ) ;
#95849=CARTESIAN_POINT ( 'NONE',  ( 16.04706613565588569, 4.602530725767624453, -3.432994500412984262 ) ) ;
#95857=SURFACE_STYLE_FILL_AREA ( #62433 ) ;
#95899=DIRECTION ( 'NONE',  ( 0.000000000000000000, 1.000000000000000000, 0.000000000000000000 ) ) ;
#95908=ORIENTED_EDGE ( 'NONE', *, *, #5617, .F. ) ;
#95913=CARTESIAN_POINT ( 'NONE',  ( 16.00000000000007461, 4.197692598229727956, 4.745459346021252856 ) ) ;
#95922=ORIENTED_EDGE ( 'NONE', *, *, #56826, .T. ) ;
#95956=CARTESIAN_POINT ( 'NONE',  ( -12.30943243785228169, 5.664461549456914824, 8.431530038708269004 ) ) ;
#95997=B_SPLINE_CURVE_WITH_KNOTS ( 'NONE', 3,
 ( #101573, #93493, #52473, #3412, #11475, #44403 ),
 .UNSPECIFIED., .F., .F.,
 ( 4, 2, 4 ),
 ( 0.000000000000000000, 0.001916782365109703659, 0.003833564730219407319 ),
 .UNSPECIFIED. ) ;
#96038=CARTESIAN_POINT ( 'NONE',  ( 11.45536878374885958, 14.80507779433297699, -9.852200945225588313 ) ) ;
#96082=CARTESIAN_POINT ( 'NONE',  ( -12.14823058519115939, 17.46151334162848912, -8.967021852677630633 ) ) ;
#96111=ORIENTED_EDGE ( 'NONE', *, *, #83164, .T. ) ;
#96120=CIRCLE ( 'NONE', #73698, 6.999999999999999112 ) ;
#96184=STYLED_ITEM ( 'NONE', ( #69190 ), #44483 ) ;
#96188=CARTESIAN_POINT ( 'NONE',  ( -16.02800152098323139, 4.194749798104338900, 2.552193233508346371 ) ) ;
#96208=( BOUNDED_SURFACE ( )  B_SPLINE_SURFACE ( 3, 2, ( 
 ( #48135, #98291, #72937 ),
 ( #23371, #56754, #55163 ),
 ( #105845, #80500, #7148 ),
 ( #97746, #81546, #72424 ),
 ( #30944, #15248, #57282 ),
 ( #32529, #81032, #64863 ),
 ( #65400, #24449, #104794 ),
 ( #23913, #105328, #89681 ),
 ( #90205, #8215, #63288 ),
 ( #30401, #41124, #40587 ),
 ( #64354, #16305, #6621 ),
 ( #39548, #71890, #106364 ),
 ( #14172, #49196, #63821 ),
 ( #22318, #15779, #73469 ),
 ( #56209, #82096, #104255 ),
 ( #96711, #39011, #96188 ),
 ( #47076, #55681, #88614 ),
 ( #14704, #89147, #47605 ),
 ( #31471, #97222, #75064 ),
 ( #57817, #74539, #33059 ) ),
 .UNSPECIFIED., .F., .F., .F. ) 
 B_SPLINE_SURFACE_WITH_KNOTS ( ( 4, 2, 2, 2, 2, 2, 2, 2, 2, 4 ),
 ( 3, 3 ),
 ( 0.001112359326657399528, 0.002061628542460812626, 0.003010897758264225940, 0.003960166974067639255, 0.004909436189871052569, 0.005858705405674465884, 0.006807974621477879199, 0.007282609229379585422, 0.007757243837281292513, 0.008706513053084705828 ),
 ( 0.000000000000000000, 1.000000000000000000 ),
 .UNSPECIFIED. ) 
 GEOMETRIC_REPRESENTATION_ITEM ( )  RATIONAL_B_SPLINE_SURFACE ( (
 ( 1.000000000000000000, 0.9115707425106666095, 1.000000000000000000),
 ( 1.000000000000000000, 0.9186010707724077129, 1.000000000000000000),
 ( 1.000000000000000000, 0.9248333139229367728, 1.000000000000000000),
 ( 1.000000000000000000, 0.9351156329915113474, 1.000000000000000000),
 ( 1.000000000000000000, 0.9392288573274951702, 1.000000000000000000),
 ( 1.000000000000000000, 0.9457209207427998976, 1.000000000000000000),
 ( 1.000000000000000000, 0.9480998420263311299, 1.000000000000000000),
 ( 1.000000000000000000, 0.9511999291517323485, 1.000000000000000000),
 ( 1.000000000000000000, 0.9519548416862445572, 1.000000000000000000),
 ( 1.000000000000000000, 0.9519314736513598829, 1.000000000000000000),
 ( 1.000000000000000000, 0.9511539719350848854, 1.000000000000000000),
 ( 1.000000000000000000, 0.9480480161103058689, 1.000000000000000000),
 ( 1.000000000000000000, 0.9457194361326417553, 1.000000000000000000),
 ( 1.000000000000000000, 0.9408176163898155364, 1.000000000000000000),
 ( 1.000000000000000000, 0.9389456878144246676, 1.000000000000000000),
 ( 1.000000000000000000, 0.9347647373043734831, 1.000000000000000000),
 ( 1.000000000000000000, 0.9324473665771305653, 1.000000000000000000),
 ( 1.000000000000000000, 0.9247734139709412604, 1.000000000000000000),
 ( 1.000000000000000000, 0.9186884142190029356, 1.000000000000000000),
 ( 1.000000000000000000, 0.9115707425101438055, 1.000000000000000000) ) ) 
 REPRESENTATION_ITEM ( '' )  SURFACE ( )  );
#96249=CARTESIAN_POINT ( 'NONE',  ( -15.79792377994584029, 22.78987439203835308, 0.2434392984178747332 ) ) ;
#96313=CARTESIAN_POINT ( 'NONE',  ( -10.28098872167596056, 16.62144220248768534, -10.01918470399412797 ) ) ;
#96381=( LENGTH_UNIT ( ) NAMED_UNIT ( * ) SI_UNIT ( .MILLI., .METRE. ) );
#96388=CARTESIAN_POINT ( 'NONE',  ( 14.83882035797308419, 4.620392632310701408, -5.701545570399354723 ) ) ;
#96390=CARTESIAN_POINT ( 'NONE',  ( 15.46466052604960595, 2.715844537110140955, -1.564829471087903379 ) ) ;
#96485=CIRCLE ( 'NONE', #5246, 13.99700487351915612 ) ;
#96486=CARTESIAN_POINT ( 'NONE',  ( -14.21654614743226652, 4.166308247385542174, 4.746652844242380098 ) ) ;
#96496=FILL_AREA_STYLE_COLOUR ( '', #9077 ) ;
#96563=CARTESIAN_POINT ( 'NONE',  ( -6.239948093757999636, 15.44474749025929228, -3.176436098724914281 ) ) ;
#96567=CARTESIAN_POINT ( 'NONE',  ( 11.68626183382240136, 18.93463063567243410, -8.061502991394757345 ) ) ;
#96612=CARTESIAN_POINT ( 'NONE',  ( -12.98756968922270438, 8.529146807383854778, -8.948902651470408642 ) ) ;
#96663=FILL_AREA_STYLE ('',( #63776 ) ) ;
#96711=CARTESIAN_POINT ( 'NONE',  ( -15.31219705631699313, 3.104419271460729490, 3.118400172730193542 ) ) ;
#96725=CARTESIAN_POINT ( 'NONE',  ( 15.36579003345834771, 3.191525062043596872, -3.226546488143007707 ) ) ;
#96759=EDGE_CURVE ( 'NONE', #77575, #32538, #99462, .T. ) ;
#96760=CIRCLE ( 'NONE', #33032, 7.500000000000000000 ) ;
#96787=CARTESIAN_POINT ( 'NONE',  ( 12.29374883903973270, 22.31972738609956153, 6.413658937279785199 ) ) ;
#96869=FILL_AREA_STYLE ('',( #56913 ) ) ;
#96953=ORIENTED_EDGE ( 'NONE', *, *, #35503, .F. ) ;
#96962=CARTESIAN_POINT ( 'NONE',  ( -16.02336867590704728, 4.077607736808446681, 2.243736929358616461 ) ) ;
#96967=CARTESIAN_POINT ( 'NONE',  ( 12.35959284188919938, 9.760562649644960231, 9.476716774057315718 ) ) ;
#96986=UNCERTAINTY_MEASURE_WITH_UNIT (LENGTH_MEASURE( 1.000000000000000082E-05 ), #12661, 'distance_accuracy_value', 'NONE');
#97003=CARTESIAN_POINT ( 'NONE',  ( -13.03847614980558411, 6.113859727637795949, 7.290527864909715383 ) ) ;
#97038=ORIENTED_EDGE ( 'NONE', *, *, #53423, .T. ) ;
#97079=CARTESIAN_POINT ( 'NONE',  ( 10.65963400673390638, 18.20553819351006908, -9.432268096413945813 ) ) ;
#97100=CARTESIAN_POINT ( 'NONE',  ( -14.89113977972644420, 23.12270858405653584, 0.2439221067019188838 ) ) ;
#97107=EDGE_LOOP ( 'NONE', ( #42057, #105211, #34872, #67148 ) ) ;
#97121=( GEOMETRIC_REPRESENTATION_CONTEXT ( 3 ) GLOBAL_UNCERTAINTY_ASSIGNED_CONTEXT ( ( #32755 ) ) GLOBAL_UNIT_ASSIGNED_CONTEXT ( ( #55581, #55058, #79872 ) ) REPRESENTATION_CONTEXT ( 'NONE', 'WORKASPACE' ) );
#97126=CARTESIAN_POINT ( 'NONE',  ( -12.34042576123834500, 7.435900281208858154, -8.326420812669903526 ) ) ;
#97160=CARTESIAN_POINT ( 'NONE',  ( -15.05785784214673306, 3.824195276770051777, -4.604276673498573835 ) ) ;
#97188=CARTESIAN_POINT ( 'NONE',  ( -12.15301166631102703, 17.45470153262807145, 8.961799035703435834 ) ) ;
#97208=FACE_OUTER_BOUND ( 'NONE', #49546, .T. ) ;
#97222=CARTESIAN_POINT ( 'NONE',  ( -15.86714682456782377, 3.932109987709613286, 3.945841262972282326 ) ) ;
#97295=CARTESIAN_POINT ( 'NONE',  ( 10.72709311271703214, 18.42505693645571441, -9.330257298435006064 ) ) ;
#97308=CARTESIAN_POINT ( 'NONE',  ( -11.46409645960823021, 12.99999999999756994, 10.00000000000000178 ) ) ;
#97367=CARTESIAN_POINT ( 'NONE',  ( -6.559876275494355369, 9.830169646080438639, 2.453497130494364686 ) ) ;
#97395=CARTESIAN_POINT ( 'NONE',  ( 12.15653237801438280, 10.26022287888880946, 9.623545464154791063 ) ) ;
#97477=CARTESIAN_POINT ( 'NONE',  ( 12.60067755036020287, 9.254571314429075102, 9.287679252113578698 ) ) ;
#97591=EDGE_CURVE ( 'NONE', #58722, #79056, #676, .T. ) ;
#97597=CARTESIAN_POINT ( 'NONE',  ( 11.99035031454962485, 8.175746249152963330, -8.773473083764660174 ) ) ;
#97615=EDGE_LOOP ( 'NONE', ( #15736, #94940, #13474, #32120 ) ) ;
#97635=CARTESIAN_POINT ( 'NONE',  ( 14.11595029532508860, 2.410436752314647713, 5.024000119269133258 ) ) ;
#97644=CARTESIAN_POINT ( 'NONE',  ( -11.00659270837914683, 16.89444621032363969, -9.217848032971012628 ) ) ;
#97746=CARTESIAN_POINT ( 'NONE',  ( -15.31585736565601508, 3.092902776791752295, -3.111329462075727914 ) ) ;
#97757=AXIS2_PLACEMENT_3D ( 'NONE', #10430, #77306, #68150 ) ;
#97765=CARTESIAN_POINT ( 'NONE',  ( -14.11595029531626722, 2.410436752329290222, 5.024000119293328126 ) ) ;
#97818=VERTEX_POINT ( 'NONE', #22469 ) ;
#97828=COLOUR_RGB ( '', 0.31764706, 0.68627451, 0.89019608) ;
#97832=CARTESIAN_POINT ( 'NONE',  ( 11.42180900222615669, 7.623507745330639018, -9.491908323009569770 ) ) ;
#97881=EDGE_LOOP ( 'NONE', ( #5873, #79139, #105553, #22222 ) ) ;
#97953=EDGE_CURVE ( 'NONE', #54847, #21676, #34280, .T. ) ;
#98024=CARTESIAN_POINT ( 'NONE',  ( 11.56920740162696504, 7.271532733520360559, 9.332439291405307813 ) ) ;
#98029=SURFACE_STYLE_FILL_AREA ( #17130 ) ;
#98070=VERTEX_POINT ( 'NONE', #19037 ) ;
#98132=ORIENTED_EDGE ( 'NONE', *, *, #48425, .T. ) ;
#98142=CARTESIAN_POINT ( 'NONE',  ( 11.12482241898927349, 19.59647781357509899, -8.686708111164573864 ) ) ;
#98187=CARTESIAN_POINT ( 'NONE',  ( -11.46642418865753754, 14.78850670498192166, -9.842947063719719836 ) ) ;
#98241=VERTEX_POINT ( 'NONE', #28184 ) ;
#98275=CARTESIAN_POINT ( 'NONE',  ( -10.99305341285137771, 19.22662180895261486, -8.903504237805147881 ) ) ;
#98291=CARTESIAN_POINT ( 'NONE',  ( -15.85122647056153156, 4.114663126756375355, -4.288211754877433002 ) ) ;
#98297=SURFACE_STYLE_USAGE ( .BOTH. , #58370 ) ;
#98301=EDGE_CURVE ( 'NONE', #75752, #18205, #16272, .T. ) ;
#98425=AXIS2_PLACEMENT_3D ( 'NONE', #4265, #13927, #95396 ) ;
#98435=CARTESIAN_POINT ( 'NONE',  ( -5.744562646538029504, 12.99999999999999289, 4.000000000000000000 ) ) ;
#98520=CARTESIAN_POINT ( 'NONE',  ( 16.14595037822613932, 20.23371447307979665, -4.922994507609789849 ) ) ;
#98552=CARTESIAN_POINT ( 'NONE',  ( -19.50000000000000000, 12.99999999999999289, 6.999999999999999112 ) ) ;
#98578=FILL_AREA_STYLE_COLOUR ( '', #43766 ) ;
#98664=CARTESIAN_POINT ( 'NONE',  ( 13.70298725226294501, 22.84579378370908742, -1.781593527410179956 ) ) ;
#98704=CARTESIAN_POINT ( 'NONE',  ( -13.46984034094769633, 22.45595379590175966, 3.284040074602051718 ) ) ;
#98790=CARTESIAN_POINT ( 'NONE',  ( -12.52541344640442311, 5.240320085686820839, 8.131572623655657139 ) ) ;
#98838=CARTESIAN_POINT ( 'NONE',  ( -16.05785784214753775, 4.775831776487168945, 3.710403933803116949 ) ) ;
#98912=CARTESIAN_POINT ( 'NONE',  ( 0.000000000000000000, 35.00000000000000000, -11.18527996897366528 ) ) ;
#98985=CARTESIAN_POINT ( 'NONE',  ( 11.69631794847444617, 16.06060599891873508, 9.527053589674022049 ) ) ;
#99014=UNCERTAINTY_MEASURE_WITH_UNIT (LENGTH_MEASURE( 1.000000000000000082E-05 ), #48405, 'distance_accuracy_value', 'NONE');
#99066=EDGE_CURVE ( 'NONE', #87833, #53038, #83483, .T. ) ;
#99087=FACE_BOUND ( 'NONE', #9288, .T. ) ;
#99119=CARTESIAN_POINT ( 'NONE',  ( 5.834906339164278144, 11.94543000914187303, -3.867544450381311005 ) ) ;
#99154=DIRECTION ( 'NONE',  ( 0.000000000000000000, 0.000000000000000000, 1.000000000000000000 ) ) ;
#99192=CARTESIAN_POINT ( 'NONE',  ( 14.81305988563250331, 21.99659144501054442, -4.400106377329072060 ) ) ;
#99193=B_SPLINE_CURVE_WITH_KNOTS ( 'NONE', 3,
 ( #55078, #89594, #24356, #58276, #16757, #81466, #25417, #57198, #8657, #73919, #40503, #91721, #74448, #99799, #529, #9712 ),
 .UNSPECIFIED., .F., .F.,
 ( 4, 2, 2, 2, 2, 2, 2, 4 ),
 ( 0.06710770102819928196, 0.06840367950113611373, 0.06969965797407294550, 0.07099563644700979115, 0.07229161491994662292, 0.07488357186582030034, 0.07617955033875714599, 0.07747552881169397776 ),
 .UNSPECIFIED. ) ;
#99236=CARTESIAN_POINT ( 'NONE',  ( -13.10092205524128062, 21.81812862912754980, -4.743381763050468436 ) ) ;
#99327=CARTESIAN_POINT ( 'NONE',  ( 14.44768974034866993, 5.957293599828267006, -7.129930386717066249 ) ) ;
#99347=CARTESIAN_POINT ( 'NONE',  ( 20.00000000000000000, 12.99999999999999289, -4.000000000000000000 ) ) ;
#99362=MECHANICAL_DESIGN_GEOMETRIC_PRESENTATION_REPRESENTATION('',(#102787),#45963);
#99402=CARTESIAN_POINT ( 'NONE',  ( 10.02677674313807366, 14.12742448687086672, -10.50839540146165696 ) ) ;
#99462=LINE ( 'NONE', #18051, #17762 ) ;
#99499=LINE ( 'NONE', #59605, #2016 ) ;
#99543=PLANE ( 'NONE',  #38132 ) ;
#99544=ADVANCED_FACE ( 'NONE', ( #39969 ), #105233, .T. ) ;
#99667=CARTESIAN_POINT ( 'NONE',  ( 6.481071417163344783, 9.994906101799367448, 2.652271756153596449 ) ) ;
#99684=CARTESIAN_POINT ( 'NONE',  ( 15.35634750254599012, 2.988828671316083430, -2.785065577016609506 ) ) ;
#99691=ORIENTED_EDGE ( 'NONE', *, *, #37938, .F. ) ;
#99719=ORIENTED_EDGE ( 'NONE', *, *, #82996, .F. ) ;
#99741=CARTESIAN_POINT ( 'NONE',  ( 13.02840130668396768, 21.68931673238071411, -4.976293656400714305 ) ) ;
#99784=CARTESIAN_POINT ( 'NONE',  ( -14.98510621630312301, 22.22666106603950453, -3.896433925070799553 ) ) ;
#99799=CARTESIAN_POINT ( 'NONE',  ( 13.97101686926742481, 20.79977776867546879, -6.270362741406088958 ) ) ;
#99899=CARTESIAN_POINT ( 'NONE',  ( 16.14595037822613932, 12.99999999999999289, -8.749999999999944933 ) ) ;
#99969=DIRECTION ( 'NONE',  ( -0.000000000000000000, -1.000000000000000000, -0.000000000000000000 ) ) ;
#99980=ORIENTED_EDGE ( 'NONE', *, *, #72608, .F. ) ;
#100007=ORIENTED_EDGE ( 'NONE', *, *, #56826, .F. ) ;
#100019=DIRECTION ( 'NONE',  ( 0.000000000000000000, 0.000000000000000000, -1.000000000000000000 ) ) ;
#100059=SURFACE_SIDE_STYLE ('',( #83344 ) ) ;
#100077=FILL_AREA_STYLE_COLOUR ( '', #50702 ) ;
#100162=( NAMED_UNIT ( * ) SI_UNIT ( $, .STERADIAN. ) SOLID_ANGLE_UNIT ( ) );
#100212=CARTESIAN_POINT ( 'NONE',  ( 15.46526232232250209, 2.714356162036268838, 1.556038473651678578 ) ) ;
#100226=ADVANCED_FACE ( 'NONE', ( #17482 ), #94114, .T. ) ;
#100269=ORIENTED_EDGE ( 'NONE', *, *, #17205, .F. ) ;
#100272=CARTESIAN_POINT ( 'NONE',  ( 15.39024840373160607, 22.75717525244400008, 2.263382330767907735 ) ) ;
#100291=DIRECTION ( 'NONE',  ( -1.000000000000000000, 0.000000000000000000, 0.000000000000000000 ) ) ;
#100310=CARTESIAN_POINT ( 'NONE',  ( -13.70309997686470282, 22.84598062213630598, -1.780770408353728795 ) ) ;
#100331=CARTESIAN_POINT ( 'NONE',  ( -14.29190075645216851, 12.99999999999999289, 0.000000000000000000 ) ) ;
#100337=CARTESIAN_POINT ( 'NONE',  ( -16.13647630347099593, 6.334953579830782111, 5.738861489053475928 ) ) ;
#100435=CARTESIAN_POINT ( 'NONE',  ( -15.05785784214673129, 3.824195276770050445, -4.604276673498571171 ) ) ;
#100501=CARTESIAN_POINT ( 'NONE',  ( -20.00000000000000000, 12.99999999999999289, 0.000000000000000000 ) ) ;
#100505=CARTESIAN_POINT ( 'NONE',  ( 19.50000000000000000, 12.99999999999999289, 0.000000000000000000 ) ) ;
#100589=FILL_AREA_STYLE ('',( #91971 ) ) ;
#100593=CARTESIAN_POINT ( 'NONE',  ( -14.29190075644683589, 21.26710225492821138, -5.626279437300707897 ) ) ;
#100600=ORIENTED_EDGE ( 'NONE', *, *, #76419, .T. ) ;
#100686=CARTESIAN_POINT ( 'NONE',  ( 15.47474416541426478, 2.749750016660005958, -1.674624973602916178 ) ) ;
#100692=FILL_AREA_STYLE ('',( #83988 ) ) ;
#100727=CARTESIAN_POINT ( 'NONE',  ( 5.887588022526042408, 11.68950459799316910, -3.788193301707003080 ) ) ;
#100751=EDGE_LOOP ( 'NONE', ( #48730, #62439, #61801, #24, #78275 ) ) ;
#100794=SURFACE_SIDE_STYLE ('',( #17250 ) ) ;
#100796=CARTESIAN_POINT ( 'NONE',  ( 13.56157340972956682, 22.61046526843750470, -2.795122311634720802 ) ) ;
#100809=ORIENTED_EDGE ( 'NONE', *, *, #84741, .T. ) ;
#100832=( GEOMETRIC_REPRESENTATION_CONTEXT ( 3 ) GLOBAL_UNCERTAINTY_ASSIGNED_CONTEXT ( ( #5927 ) ) GLOBAL_UNIT_ASSIGNED_CONTEXT ( ( #83278, #10967, #43881 ) ) REPRESENTATION_CONTEXT ( 'NONE', 'WORKASPACE' ) );
#100838=CARTESIAN_POINT ( 'NONE',  ( -13.67356607649133693, 22.79711367846607217, -2.036615685936300491 ) ) ;
#100858=EDGE_LOOP ( 'NONE', ( #11306, #50524, #21222, #28161 ) ) ;
#100886=CARTESIAN_POINT ( 'NONE',  ( -18.00000000000000355, 12.99999999999999289, 0.000000000000000000 ) ) ;
#100916=FACE_OUTER_BOUND ( 'NONE', #19942, .T. ) ;
#100926=CARTESIAN_POINT ( 'NONE',  ( -16.13482245078207100, 21.13350007393601970, 3.415357648783710953 ) ) ;
#100940=AXIS2_PLACEMENT_3D ( 'NONE', #21056, #36707, #53895 ) ;
#101001=( GEOMETRIC_REPRESENTATION_CONTEXT ( 3 ) GLOBAL_UNCERTAINTY_ASSIGNED_CONTEXT ( ( #27885 ) ) GLOBAL_UNIT_ASSIGNED_CONTEXT ( ( #26307, #18184, #1965 ) ) REPRESENTATION_CONTEXT ( 'NONE', 'WORKASPACE' ) );
#101056=SURFACE_STYLE_FILL_AREA ( #75171 ) ;
#101121=EDGE_CURVE ( 'NONE', #98070, #72252, #9792, .T. ) ;
#101125=ORIENTED_EDGE ( 'NONE', *, *, #34953, .T. ) ;
#101129=CARTESIAN_POINT ( 'NONE',  ( -15.50532557111765541, 2.637300882401473867, 0.8493220884279345517 ) ) ;
#101145=SURFACE_SIDE_STYLE ('',( #12125 ) ) ;
#101147=( NAMED_UNIT ( * ) SI_UNIT ( $, .STERADIAN. ) SOLID_ANGLE_UNIT ( ) );
#101159=ORIENTED_EDGE ( 'NONE', *, *, #97953, .F. ) ;
#101166=DIRECTION ( 'NONE',  ( 1.000000000000000000, 0.000000000000000000, 0.000000000000000000 ) ) ;
#101178=EDGE_CURVE ( 'NONE', #37313, #91522, #51777, .T. ) ;
#101208=EDGE_CURVE ( 'NONE', #32538, #92197, #83949, .T. ) ;
#101240=CARTESIAN_POINT ( 'NONE',  ( 14.61305944212074692, 1.672740767018813024, 3.460733717104720331 ) ) ;
#101278=CARTESIAN_POINT ( 'NONE',  ( 6.981089760825446078, 9.033170731678344723, 0.5312715680615406333 ) ) ;
#101279=FILL_AREA_STYLE_COLOUR ( '', #2144 ) ;
#101290=( NAMED_UNIT ( * ) SI_UNIT ( $, .STERADIAN. ) SOLID_ANGLE_UNIT ( ) );
#101314=TOROIDAL_SURFACE ( 'NONE', #63454, 7.999999999999998224, 2.000000000000000000 ) ;
#101346=CARTESIAN_POINT ( 'NONE',  ( 11.23676242740048892, 17.72229746334734202, 8.838879072636887102 ) ) ;
#101390=CARTESIAN_POINT ( 'NONE',  ( -10.35489345913581616, 16.95138009610748497, 9.903898274887804831 ) ) ;
#101414=STYLED_ITEM ( 'NONE', ( #27145 ), #43529 ) ;
#101442=CARTESIAN_POINT ( 'NONE',  ( 6.879789419156629116, 16.78666415220166996, 1.315101155215614437 ) ) ;
#101470=CARTESIAN_POINT ( 'NONE',  ( -16.10099529212900649, 21.87266829489404785, 0.2127561331495561314 ) ) ;
#101488=ORIENTED_EDGE ( 'NONE', *, *, #24682, .F. ) ;
#101505=DIRECTION ( 'NONE',  ( 0.3048027540951617209, 0.4519649026962606064, 0.8383453988820862568 ) ) ;
#101541=FILL_AREA_STYLE_COLOUR ( '', #41037 ) ;
#101573=CARTESIAN_POINT ( 'NONE',  ( -16.14595037822608603, 7.274337365584598203, -6.616591826375523233 ) ) ;
#101667=CARTESIAN_POINT ( 'NONE',  ( -15.74121454705215051, 22.21713694095602420, -3.427215416360654743 ) ) ;
#101680=CARTESIAN_POINT ( 'NONE',  ( 0.000000000000000000, 0.9999999999999943379, 0.000000000000000000 ) ) ;
#101694=ORIENTED_EDGE ( 'NONE', *, *, #25381, .F. ) ;
#101729=AXIS2_PLACEMENT_3D ( 'NONE', #63431, #7273, #48788 ) ;
#101792=ADVANCED_FACE ( 'NONE', ( #70323 ), #3034, .F. ) ;
#101802=COLOUR_RGB ( '', 0.72549020, 0.75294118, 0.79215686) ;
#101807=CARTESIAN_POINT ( 'NONE',  ( 15.20081118350077176, 3.404146808184774997, 3.872164105970431258 ) ) ;
#101820=CARTESIAN_POINT ( 'NONE',  ( -15.05785784214673129, 3.824195276770050445, -4.604276673498571171 ) ) ;
#101834=AXIS2_PLACEMENT_3D ( 'NONE', #8881, #40718, #100019 ) ;
#101835=EDGE_LOOP ( 'NONE', ( #13452, #5835, #80022, #99691, #80477, #93576 ) ) ;
#101867=CARTESIAN_POINT ( 'NONE',  ( 10.43259654054523899, 17.30095377175555527, 9.783482319262313709 ) ) ;
#101908=CARTESIAN_POINT ( 'NONE',  ( -13.03669973157214557, 19.28101993133772041, 7.786058856550787333 ) ) ;
#101919=DIRECTION ( 'NONE',  ( 0.000000000000000000, -1.000000000000000000, -0.000000000000000000 ) ) ;
#101989=ORIENTED_EDGE ( 'NONE', *, *, #15999, .F. ) ;
#101992=PRESENTATION_STYLE_ASSIGNMENT (( #37299 ) ) ;
#102034=CARTESIAN_POINT ( 'NONE',  ( 14.62354047171442772, 22.28742650378891810, 3.920645538799723884 ) ) ;
#102037=CARTESIAN_POINT ( 'NONE',  ( -14.04769764157139988, 4.430073480882096071, -5.212240267777101366 ) ) ;
#102041=CARTESIAN_POINT ( 'NONE',  ( 14.95520043898952345, 4.194724623210972503, 5.164345506890690274 ) ) ;
#102131=CARTESIAN_POINT ( 'NONE',  ( -11.59786760126457139, 15.72211884272761750, -9.649684760468234757 ) ) ;
#102140=CARTESIAN_POINT ( 'NONE',  ( 16.13469797932767946, 21.10829079392559393, -3.392296823476807610 ) ) ;
#102175=PRODUCT_CONTEXT ( 'NONE', #1077, 'mechanical' ) ;
#102193=SURFACE_STYLE_FILL_AREA ( #3507 ) ;
#102208=CARTESIAN_POINT ( 'NONE',  ( -1.829579891623863134E-15, 10.71892156097790583, -14.93965356295127478 ) ) ;
#102228=ORIENTED_EDGE ( 'NONE', *, *, #5485, .F. ) ;
#102266=ORIENTED_EDGE ( 'NONE', *, *, #27433, .T. ) ;
#102268=ORIENTED_EDGE ( 'NONE', *, *, #50642, .T. ) ;
#102290=CARTESIAN_POINT ( 'NONE',  ( -6.013174582917088173, 11.20780250015804391, -3.585507868043892987 ) ) ;
#102338=( NAMED_UNIT ( * ) PLANE_ANGLE_UNIT ( ) SI_UNIT ( $, .RADIAN. ) );
#102341=( NAMED_UNIT ( * ) PLANE_ANGLE_UNIT ( ) SI_UNIT ( $, .RADIAN. ) );
#102374=CARTESIAN_POINT ( 'NONE',  ( 16.14595037822608603, 7.274337365584589321, 6.616591826375515240 ) ) ;
#102396=VERTEX_POINT ( 'NONE', #94967 ) ;
#102401=CARTESIAN_POINT ( 'NONE',  ( 10.68792165862781296, 15.17596856234630920, 9.765698129339666522 ) ) ;
#102447=CARTESIAN_POINT ( 'NONE',  ( -13.29977836103240030, 22.16549982817352316, 4.028575465788259535 ) ) ;
#102487=ORIENTED_EDGE ( 'NONE', *, *, #28831, .F. ) ;
#102506=CARTESIAN_POINT ( 'NONE',  ( 6.705175466950450414, 16.46052391487621591, -2.022930269817424076 ) ) ;
#102533=CARTESIAN_POINT ( 'NONE',  ( 15.78881369299498694, 4.458650427774422553, -5.229507541793314118 ) ) ;
#102551=LINE ( 'NONE', #28701, #67398 ) ;
#102603=( NAMED_UNIT ( * ) SI_UNIT ( $, .STERADIAN. ) SOLID_ANGLE_UNIT ( ) );
#102621=EDGE_CURVE ( 'NONE', #79056, #24576, #41258, .T. ) ;
#102638=( LENGTH_UNIT ( ) NAMED_UNIT ( * ) SI_UNIT ( .MILLI., .METRE. ) );
#102671=CARTESIAN_POINT ( 'NONE',  ( -12.01037645372310791, 17.07677055236747421, -9.138074232161729427 ) ) ;
#102677=SURFACE_STYLE_USAGE ( .BOTH. , #36399 ) ;
#102679=CARTESIAN_POINT ( 'NONE',  ( 15.76925030630952485, 22.49347711646982262, 2.473099622756875338 ) ) ;
#102680=CARTESIAN_POINT ( 'NONE',  ( 0.000000000000000000, 34.00000000000000711, -11.18527996897366528 ) ) ;
#102733=CARTESIAN_POINT ( 'NONE',  ( -14.37769637068204709, 21.52932494089419180, -5.240976541736561245 ) ) ;
#102745=CARTESIAN_POINT ( 'NONE',  ( 3.659159783247726268E-15, 10.71892156097790583, 14.93965356295127478 ) ) ;
#102778=AXIS2_PLACEMENT_3D ( 'NONE', #45308, #1623, #34585 ) ;
#102787=STYLED_ITEM ( 'NONE', ( #94608 ), #23974 ) ;
#102800=CIRCLE ( 'NONE', #82137, 1.999999999999999556 ) ;
#102878=CARTESIAN_POINT ( 'NONE',  ( 16.01541666090335880, 3.834101040393494753, -1.299565945645027920 ) ) ;
#102887=ADVANCED_FACE ( 'NONE', ( #1554 ), #23287, .T. ) ;
#102939=CARTESIAN_POINT ( 'NONE',  ( 11.66348175382439578, 15.91712690338637692, 9.569217749563181385 ) ) ;
#102982=CARTESIAN_POINT ( 'NONE',  ( -11.79617940926573993, 16.41796236967441303, 9.402036560305605306 ) ) ;
#102993=FACE_BOUND ( 'NONE', #28250, .T. ) ;
#103061=AXIS2_PLACEMENT_3D ( 'NONE', #74193, #46354, #54411 ) ;
#103065=CARTESIAN_POINT ( 'NONE',  ( -5.763702088647366217, 13.53577993954648662, -3.972887565972252233 ) ) ;
#103069=CARTESIAN_POINT ( 'NONE',  ( 13.38477778458014988, 7.844114667846795896, -8.572480637398566472 ) ) ;
#103129=CARTESIAN_POINT ( 'NONE',  ( 20.00100000000000122, 12.99999999999999289, 0.000000000000000000 ) ) ;
#103145=ORIENTED_EDGE ( 'NONE', *, *, #91542, .F. ) ;
#103213=CARTESIAN_POINT ( 'NONE',  ( 14.45712292643875863, 21.77297462401915951, 4.836555868072715647 ) ) ;
#103216=CARTESIAN_POINT ( 'NONE',  ( -14.29190075645216851, 7.765108448534488339, -6.049455384114764911 ) ) ;
#103227=FILL_AREA_STYLE_COLOUR ( '', #67726 ) ;
#103275=( NAMED_UNIT ( * ) SI_UNIT ( $, .STERADIAN. ) SOLID_ANGLE_UNIT ( ) );
#103286=CARTESIAN_POINT ( 'NONE',  ( 10.07982286427262686, 15.04985694343187141, 10.37301160543360545 ) ) ;
#103327=CARTESIAN_POINT ( 'NONE',  ( -15.68120647348154151, 6.021684053266456615, 7.051923121157602559 ) ) ;
#103331=CARTESIAN_POINT ( 'NONE',  ( -13.71253760832901492, 3.086396204329165727, 6.035735341873747828 ) ) ;
#103404=CARTESIAN_POINT ( 'NONE',  ( 15.94096206886545097, 3.082184004823646184, 0.3571785271892598534 ) ) ;
#103416=VERTEX_POINT ( 'NONE', #66728 ) ;
#103435=AXIS2_PLACEMENT_3D ( 'NONE', #89131, #40046, #33046 ) ;
#103465=CARTESIAN_POINT ( 'NONE',  ( 10.10731083982912004, 15.36174436921201192, 10.31675818847685555 ) ) ;
#103505=CARTESIAN_POINT ( 'NONE',  ( -10.64386978829505814, 14.84064791310457920, 9.848362920724447633 ) ) ;
#103583=CARTESIAN_POINT ( 'NONE',  ( -6.321595794353349618, 15.64364823866884180, -3.012682989575209636 ) ) ;
#103633=CARTESIAN_POINT ( 'NONE',  ( -15.99999999999999645, 4.197692598229818550, -4.745459346021418057 ) ) ;
#103641=CIRCLE ( 'NONE', #93332, 4.000000000000000000 ) ;
#103694=SURFACE_STYLE_FILL_AREA ( #4471 ) ;
#103728=CARTESIAN_POINT ( 'NONE',  ( -11.42114566974704992, 14.07739106013302788, -9.943574220663299101 ) ) ;
#103736=CARTESIAN_POINT ( 'NONE',  ( 16.11127471224495622, 21.68306317500850611, 1.725009018242721792 ) ) ;
#103748=SURFACE_STYLE_USAGE ( .BOTH. , #75887 ) ;
#103814=UNCERTAINTY_MEASURE_WITH_UNIT (LENGTH_MEASURE( 1.000000000000000082E-05 ), #16698, 'distance_accuracy_value', 'NONE');
#103847=CARTESIAN_POINT ( 'NONE',  ( -13.58269433839552676, 24.75340072303480810, 0.6690760600839953387 ) ) ;
#103873=CARTESIAN_POINT ( 'NONE',  ( -6.984140731825568160, 9.027579208887587470, -0.5385323539060862252 ) ) ;
#103887=B_SPLINE_CURVE_WITH_KNOTS ( 'NONE', 3,
 ( #66930, #23841, #17322, #24888, #90664, #15703, #48591, #83099, #50707, #83619, #42639, #75536, #81480, #106293, #73392, #92238 ),
 .UNSPECIFIED., .F., .F.,
 ( 4, 2, 2, 2, 2, 2, 2, 4 ),
 ( 9.697399036122160616E-19, 0.001212534658637846657, 0.002425069317275692447, 0.004850138634551384026, 0.006062673293189230032, 0.007275207951827075172, 0.008487742610464922913, 0.009700277269102768052 ),
 .UNSPECIFIED. ) ;
#103892=EDGE_CURVE ( 'NONE', #20022, #76857, #29586, .T. ) ;
#103923=CARTESIAN_POINT ( 'NONE',  ( 15.94091178690282362, 3.082798537041105291, -0.3736180972855698834 ) ) ;
#103981=CARTESIAN_POINT ( 'NONE',  ( -16.01235146068397697, 3.721755040407972892, -0.3223148954708403013 ) ) ;
#103985=CARTESIAN_POINT ( 'NONE',  ( 11.81070278343545610, 6.722221634647634225, 9.055894994455341518 ) ) ;
#104079=CARTESIAN_POINT ( 'NONE',  ( 6.984567718307133077, 16.97316992422711124, -0.5333114754527591428 ) ) ;
#104128=CARTESIAN_POINT ( 'NONE',  ( -14.47558186359348298, 21.82849871097600314, -4.801378726369249783 ) ) ;
#104147=DIRECTION ( 'NONE',  ( 0.000000000000000000, -0.7633528697427554022, 0.6459817305895730888 ) ) ;
#104153=DIRECTION ( 'NONE',  ( 1.000000000000000000, -0.000000000000000000, -0.000000000000000000 ) ) ;
#104155=CARTESIAN_POINT ( 'NONE',  ( -10.61644205368614280, 13.93655468994954560, -9.960933018827816454 ) ) ;
#104177=UNCERTAINTY_MEASURE_WITH_UNIT (LENGTH_MEASURE( 1.000000000000000082E-05 ), #102638, 'distance_accuracy_value', 'NONE');
#104192=( NAMED_UNIT ( * ) SI_UNIT ( $, .STERADIAN. ) SOLID_ANGLE_UNIT ( ) );
#104255=CARTESIAN_POINT ( 'NONE',  ( -16.02369196221458125, 4.084267053699538685, 2.245701149452017376 ) ) ;
#104257=CARTESIAN_POINT ( 'NONE',  ( 14.66255430294002515, 22.40929092344816809, -3.546301636246186550 ) ) ;
#104298=CIRCLE ( 'NONE', #45799, 8.750000000000033751 ) ;
#104305=CARTESIAN_POINT ( 'NONE',  ( -14.87170168469266329, 23.06219547136248949, 1.058210525625679299 ) ) ;
#104310=CIRCLE ( 'NONE', #64667, 2.000000000000000000 ) ;
#104338=CARTESIAN_POINT ( 'NONE',  ( -14.29190075645648683, 6.456385560661901835, 7.561819230138081771 ) ) ;
#104372=CARTESIAN_POINT ( 'NONE',  ( -10.54854822160233674, 17.80311496882384503, 9.603326997340017712 ) ) ;
#104395=CIRCLE ( 'NONE', #6223, 10.00000000000000178 ) ;
#104438=MECHANICAL_DESIGN_GEOMETRIC_PRESENTATION_REPRESENTATION('',(#73395),#88977);
#104451=CARTESIAN_POINT ( 'NONE',  ( 16.07816244836988417, 5.101897851387931837, -4.232350007286695970 ) ) ;
#104454=CARTESIAN_POINT ( 'NONE',  ( 15.93933706297306507, 3.102176837441567248, 0.7193050692217635156 ) ) ;
#104462=AXIS2_PLACEMENT_3D ( 'NONE', #105583, #15512, #81292 ) ;
#104475=EDGE_LOOP ( 'NONE', ( #68707, #102487, #22329, #41715, #75570, #6328 ) ) ;
#104516=CARTESIAN_POINT ( 'NONE',  ( 14.78767551106102474, 5.758539365854975500, 6.917020875423936843 ) ) ;
#104553=EDGE_CURVE ( 'NONE', #53038, #93080, #95279, .T. ) ;
#104558=CARTESIAN_POINT ( 'NONE',  ( -12.11780882157808037, 7.885269496745385354, 8.622659793487008173 ) ) ;
#104566=AXIS2_PLACEMENT_3D ( 'NONE', #78874, #5002, #21743 ) ;
#104587=EDGE_CURVE ( 'NONE', #38642, #77985, #45128, .T. ) ;
#104637=CARTESIAN_POINT ( 'NONE',  ( -6.560397950766611253, 16.17087793925111328, 2.451970031105680015 ) ) ;
#104642=CARTESIAN_POINT ( 'NONE',  ( 10.76947298832407363, 15.76878063321550982, -9.614905453851129380 ) ) ;
#104648=CARTESIAN_POINT ( 'NONE',  ( 9.797174393178825657E-16, 35.00000000000000000, 8.000000000000000000 ) ) ;
#104690=CARTESIAN_POINT ( 'NONE',  ( -11.77640042769365536, 19.16702799015035197, -7.901857338882000370 ) ) ;
#104750=CARTESIAN_POINT ( 'NONE',  ( -15.00099999999999767, 12.99999999999999289, 0.000000000000000000 ) ) ;
#104769=STYLED_ITEM ( 'NONE', ( #4593 ), #41066 ) ;
#104794=CARTESIAN_POINT ( 'NONE',  ( -16.01537386455369116, 3.832633078741163768, -1.292357405291790773 ) ) ;
#104812=CARTESIAN_POINT ( 'NONE',  ( -14.83962450835064928, 1.409789280633743314, -2.191244623882634635 ) ) ;
#104833=B_SPLINE_CURVE_WITH_KNOTS ( 'NONE', 3,
 ( #43277, #69164, #102034, #76162, #50294, #92881, #83197, #9294, #42204, #75088, #67030, #94503, #53494, #95033, #55062, #37877, #87992, #78816 ),
 .UNSPECIFIED., .F., .F.,
 ( 4, 2, 2, 2, 2, 2, 2, 2, 4 ),
 ( 8.673617379884035472E-19, 0.003013683243355653411, 0.004520524865033480333, 0.005273945675872394011, 0.006027366486711306821, 0.007534208108389134177, 0.009041049730066960666, 0.01054789135174478976, 0.01205473297342261538 ),
 .UNSPECIFIED. ) ;
#104854=CARTESIAN_POINT ( 'NONE',  ( -14.87468076902975334, 23.07153947553970497, -1.073492826241112086 ) ) ;
#104892=CARTESIAN_POINT ( 'NONE',  ( -12.04654684923174912, 10.50803151810102598, 9.704396884749211694 ) ) ;
#104916=CARTESIAN_POINT ( 'NONE',  ( 0.000000000000000000, -3.035766082959412415E-15, -13.99700487351915612 ) ) ;
#104920=CIRCLE ( 'NONE', #1559, 7.000000000000000000 ) ;
#104965=SURFACE_STYLE_USAGE ( .BOTH. , #6240 ) ;
#105031=CARTESIAN_POINT ( 'NONE',  ( 0.000000000000000000, 0.9999999999999943379, 0.000000000000000000 ) ) ;
#105036=CARTESIAN_POINT ( 'NONE',  ( 16.10099529212903846, 21.87266829489345454, 0.2127561331699810987 ) ) ;
#105048=CARTESIAN_POINT ( 'NONE',  ( 1.829579891623863529E-15, 10.71892156097790583, 14.93965356295127478 ) ) ;
#105062=AXIS2_PLACEMENT_3D ( 'NONE', #76910, #84483, #43492 ) ;
#105066=CARTESIAN_POINT ( 'NONE',  ( 13.12502261391177250, 8.285386694269465835, 8.822864485936415591 ) ) ;
#105096=DIRECTION ( 'NONE',  ( 0.000000000000000000, 0.000000000000000000, -1.000000000000000000 ) ) ;
#105103=LINE ( 'NONE', #57058, #67006 ) ;
#105105=CARTESIAN_POINT ( 'NONE',  ( -11.77137377981709498, 11.34323235146788988, 9.877945527872393328 ) ) ;
#105114=SURFACE_STYLE_USAGE ( .BOTH. , #72212 ) ;
#105124=CIRCLE ( 'NONE', #62124, 7.000000000000000000 ) ;
#105134=ORIENTED_EDGE ( 'NONE', *, *, #30378, .F. ) ;
#105160=CARTESIAN_POINT ( 'NONE',  ( 5.744562646538029504, 12.99999999999999112, -4.000000000000000000 ) ) ;
#105176=CARTESIAN_POINT ( 'NONE',  ( -6.075240630612073645, 15.03060843655180001, 3.485377474036336576 ) ) ;
#105182=CARTESIAN_POINT ( 'NONE',  ( 11.44060156327110001, 7.577557493472524719, -9.471991900697743105 ) ) ;
#105211=ORIENTED_EDGE ( 'NONE', *, *, #71778, .T. ) ;
#105230=CARTESIAN_POINT ( 'NONE',  ( -10.88958497527556268, 9.025501054700395542, -10.01831549336726290 ) ) ;
#105233=CYLINDRICAL_SURFACE ( 'NONE', #25082, 10.00000000000000178 ) ;
#105242=DIRECTION ( 'NONE',  ( -1.000000000000000000, -0.000000000000000000, -0.000000000000000000 ) ) ;
#105243=AXIS2_PLACEMENT_3D ( 'NONE', #4759, #47326, #79699 ) ;
#105328=CARTESIAN_POINT ( 'NONE',  ( -15.93933706297316988, 3.102176837440797641, -0.7193050692103517552 ) ) ;
#105340=CARTESIAN_POINT ( 'NONE',  ( 14.11595029532510281, 2.410436752314619735, -5.024000119269086184 ) ) ;
#105382=CARTESIAN_POINT ( 'NONE',  ( -14.45712292644103769, 21.77297462402690087, 4.836555868059321917 ) ) ;
#105440=CARTESIAN_POINT ( 'NONE',  ( 0.000000000000000000, 35.00000000000000000, -8.000000000000000000 ) ) ;
#105483=DIRECTION ( 'NONE',  ( 0.000000000000000000, 0.000000000000000000, 1.000000000000000000 ) ) ;
#105491=ADVANCED_FACE ( 'NONE', ( #11857, #56953 ), #99543, .F. ) ;
#105506=CARTESIAN_POINT ( 'NONE',  ( 12.82140450591726299, 18.88705565487690308, 8.090819087176381430 ) ) ;
#105553=ORIENTED_EDGE ( 'NONE', *, *, #28831, .T. ) ;
#105565=CARTESIAN_POINT ( 'NONE',  ( -29.99397490504468067, 1.005902684993158047, 14.99698745252235099 ) ) ;
#105583=CARTESIAN_POINT ( 'NONE',  ( 18.00000000000000355, 12.99999999999999289, -9.500000000000000000 ) ) ;
#105586=SURFACE_SIDE_STYLE ('',( #98029 ) ) ;
#105603=VERTEX_POINT ( 'NONE', #32179 ) ;
#105619=CARTESIAN_POINT ( 'NONE',  ( -14.23923521226553035, 6.526093643864192551, 7.639870307848205755 ) ) ;
#105699=CARTESIAN_POINT ( 'NONE',  ( 11.94629484552446286, 10.83030812042046520, -9.765882283547693277 ) ) ;
#105742=FILL_AREA_STYLE_COLOUR ( '', #28193 ) ;
#105749=CARTESIAN_POINT ( 'NONE',  ( -10.64016296546354923, 13.00014743456769928, -10.01963642081249617 ) ) ;
#105758=CARTESIAN_POINT ( 'NONE',  ( -15.39795322966403290, 3.054092008348469722, 2.852131183246390034 ) ) ;
#105764=B_SPLINE_CURVE_WITH_KNOTS ( 'NONE', 3,
 ( #71232, #104128, #31348, #22721, #7023, #56630, #72811, #97100, #55559, #15117, #88495, #31861, #23782, #22184, #89551, #15647 ),
 .UNSPECIFIED., .F., .F.,
 ( 4, 2, 2, 2, 2, 2, 2, 4 ),
 ( 2.111010400649636311E-15, 0.003002507059513599523, 0.004503760589269341537, 0.006005014119025082683, 0.006755640883902953690, 0.007506267648780824697, 0.009007521178536564976, 0.01201002823804804380 ),
 .UNSPECIFIED. ) ;
#105815=EDGE_CURVE ( 'NONE', #5290, #39650, #3755, .T. ) ;
#105820=DIRECTION ( 'NONE',  ( -0.000000000000000000, 1.000000000000000000, -0.000000000000000000 ) ) ;
#105832=DIRECTION ( 'NONE',  ( -1.000000000000000000, 0.000000000000000000, 0.000000000000000000 ) ) ;
#105845=CARTESIAN_POINT ( 'NONE',  ( -15.20081118350138993, 3.404146808183821982, -3.872164105968183279 ) ) ;
#105903=CARTESIAN_POINT ( 'NONE',  ( 16.04705908622415933, 4.602417526209643839, -3.432813300957220815 ) ) ;
#105920=CARTESIAN_POINT ( 'NONE',  ( 14.29190075645216851, 12.99999999999999289, 0.000000000000000000 ) ) ;
#105934=( GEOMETRIC_REPRESENTATION_CONTEXT ( 3 ) GLOBAL_UNCERTAINTY_ASSIGNED_CONTEXT ( ( #71719 ) ) GLOBAL_UNIT_ASSIGNED_CONTEXT ( ( #85879, #36287, #29775 ) ) REPRESENTATION_CONTEXT ( 'NONE', 'WORKASPACE' ) );
#106098=CARTESIAN_POINT ( 'NONE',  ( 13.67695886415361350, 5.027398151725734010, 6.085592534666677267 ) ) ;
#106128=SURFACE_STYLE_USAGE ( .BOTH. , #23666 ) ;
#106168=ORIENTED_EDGE ( 'NONE', *, *, #14782, .T. ) ;
#106170=ORIENTED_EDGE ( 'NONE', *, *, #5294, .F. ) ;
#106185=EDGE_CURVE ( 'NONE', #92197, #32538, #96760, .T. ) ;
#106216=CARTESIAN_POINT ( 'NONE',  ( 13.16427862254860770, 19.50489605903024426, -7.599932435955482291 ) ) ;
#106224=AXIS2_PLACEMENT_3D ( 'NONE', #94283, #86211, #87259 ) ;
#106264=CARTESIAN_POINT ( 'NONE',  ( -11.43824633007028702, 13.06272204673569703, -10.01661281870972786 ) ) ;
#106276=ORIENTED_EDGE ( 'NONE', *, *, #73541, .T. ) ;
#106293=CARTESIAN_POINT ( 'NONE',  ( -15.19414944962576186, 3.422781246270885536, -3.910013010457076721 ) ) ;
#106329=CARTESIAN_POINT ( 'NONE',  ( -13.12258126849660478, 19.43509895603041215, 7.664272855090029424 ) ) ;
#106350=CARTESIAN_POINT ( 'NONE',  ( -12.29976574085473473, 22.32620736666799033, -6.386862290538014797 ) ) ;
#106364=CARTESIAN_POINT ( 'NONE',  ( -16.01541666090353999, 3.834101040397206894, 1.299565945660708710 ) ) ;
#106366=CARTESIAN_POINT ( 'NONE',  ( 14.29190075645217028, 21.26710225494214157, 5.626279437277407425 ) ) ;
#106371=PRESENTATION_STYLE_ASSIGNMENT (( #98297 ) ) ;
#106445=CARTESIAN_POINT ( 'NONE',  ( 10.14577494216288400, 12.16872942106264865, -10.55611388860419453 ) ) ;
#106497=ORIENTED_EDGE ( 'NONE', *, *, #99066, .F. ) ;
#106731=CIRCLE ( 'NONE', #105062, 10.00000000000000178 ) ;
#106761=CARTESIAN_POINT ( 'NONE',  ( 15.57101515226550958, 22.98847347788403539, 0.5602172340486083479 ) ) ;
ENDSEC;
END-ISO-10303-21;
